ISO-10303-21;
HEADER;
FILE_DESCRIPTION (('STEP AP214'),
    '1' );
FILE_NAME ('Nut.step',
    '2026-10-21T18:31:44',
    ( '' ),
    ( '' ),
    'SwSTEP 2.0',
    'SolidWorks 2025',
    '' );
FILE_SCHEMA (( 'AUTOMOTIVE_DESIGN' ));
ENDSEC;

DATA;
#9=ADVANCED_FACE ( 'NONE', ( #480 ), #9607, .F. ) ;
#16=DIRECTION ( 'NONE',  ( 0.000000000000000000, 0.000000000000000000, -1.000000000000000000 ) ) ;
#18=EDGE_LOOP ( 'NONE', ( #8634, #13740, #2829, #14978 ) ) ;
#20=CARTESIAN_POINT ( 'NONE',  ( -8.549982208541774191E-16, 26.68000000000000682, 14.19474002721660355 ) ) ;
#23=CARTESIAN_POINT ( 'NONE',  ( -4.171729424061787483, 8.330000000000003624, -12.83926296998457417 ) ) ;
#30=CARTESIAN_POINT ( 'NONE',  ( 7.347880794884122694E-16, 0.000000000000000000, -20.00000000000000000 ) ) ;
#34=( BOUNDED_CURVE ( )  B_SPLINE_CURVE ( 2, ( #9058, #4723, #3556 ),
 .UNSPECIFIED., .F., .F. ) 
 B_SPLINE_CURVE_WITH_KNOTS ( ( 3, 3 ),
 ( 0.6250000000000000000, 0.6258333417219855699 ),
 .UNSPECIFIED. ) 
 CURVE ( )  GEOMETRIC_REPRESENTATION_ITEM ( )  RATIONAL_B_SPLINE_CURVE ( ( 0.9755282581475768211, 0.9755282581475767101, 0.9777307592560633420 ) ) 
 REPRESENTATION_ITEM ( '' )  );
#35=CARTESIAN_POINT ( 'NONE',  ( 13.49999999999999822, 6.279999999999996696, 4.386415899144236796 ) ) ;
#38=ORIENTED_EDGE ( 'NONE', *, *, #7659, .T. ) ;
#40=CARTESIAN_POINT ( 'NONE',  ( 11.76794919243112680, 26.57999999999999829, -3.823638476888993942 ) ) ;
#42=VERTEX_POINT ( 'NONE', #221 ) ;
#44=CARTESIAN_POINT ( 'NONE',  ( 9.520470885617717371, -12.26999999999999602, -6.917026985038131848 ) ) ;
#53=EDGE_CURVE ( 'NONE', #3761, #17169, #15927, .T. ) ;
#56=EDGE_CURVE ( 'NONE', #7801, #2957, #9184, .T. ) ;
#58=DIRECTION ( 'NONE',  ( -0.000000000000000000, -1.000000000000000000, -0.000000000000000000 ) ) ;
#60=DIRECTION ( 'NONE',  ( 0.4999999999999977240, 0.000000000000000000, 0.8660254037844399289 ) ) ;
#62=CARTESIAN_POINT ( 'NONE',  ( 10.92172942406179104, 19.72999999999999687, -7.935100905948385908 ) ) ;
#63=ORIENTED_EDGE ( 'NONE', *, *, #6522, .T. ) ;
#64=CARTESIAN_POINT ( 'NONE',  ( -12.94117117538681683, 4.250271015223984582E-15, -2.797136868549697564 ) ) ;
#67=CARTESIAN_POINT ( 'NONE',  ( -11.76794919243112325, -7.919999999999998153, 3.823638476888994386 ) ) ;
#69=CARTESIAN_POINT ( 'NONE',  ( -4.171729424061791036, -11.47000000000000064, 12.83926296998457239 ) ) ;
#80=AXIS2_PLACEMENT_3D ( 'NONE', #263, #10869, #2892 ) ;
#82=CARTESIAN_POINT ( 'NONE',  ( 2.279995255611139653E-15, 9.179999999999992610, -12.37355403259654985 ) ) ;
#83=CARTESIAN_POINT ( 'NONE',  ( 13.50000000000000000, 4.430000000000003268, 1.734723475976807094E-15 ) ) ;
#85=CARTESIAN_POINT ( 'NONE',  ( 11.76794919243112680, -0.4200000000000027045, -3.823638476888993942 ) ) ;
#89=CARTESIAN_POINT ( 'NONE',  ( -10.92172942406179104, -12.76999999999999602, 7.935100905948385908 ) ) ;
#98=ADVANCED_FACE ( 'NONE', ( #16379 ), #12591, .T. ) ;
#99=CARTESIAN_POINT ( 'NONE',  ( -17.32050807568884210, 7.773118517290098950, 7.999999999999840128 ) ) ;
#100=CARTESIAN_POINT ( 'NONE',  ( 1.108954987895778950E-11, 4.813974596216015200, 12.00000000000000178 ) ) ;
#106=VERTEX_POINT ( 'NONE', #2759 ) ;
#109=CARTESIAN_POINT ( 'NONE',  ( -8.343458848123582072, 14.37999999999998835, 11.48378591275254124 ) ) ;
#110=EDGE_LOOP ( 'NONE', ( #6207, #1537, #1550, #818 ) ) ;
#114=CARTESIAN_POINT ( 'NONE',  ( -8.343458848123576743, 14.47999999999999865, -11.48378591275254301 ) ) ;
#127=AXIS2_PLACEMENT_3D ( 'NONE', #2848, #1623, #9520 ) ;
#129=CARTESIAN_POINT ( 'NONE',  ( -13.14483242576192978, 7.170662809914418290, -16.82677684650047567 ) ) ;
#131=EDGE_LOOP ( 'NONE', ( #5447, #10898, #7879, #3829 ) ) ;
#133=ORIENTED_EDGE ( 'NONE', *, *, #911, .F. ) ;
#134=B_SPLINE_CURVE_WITH_KNOTS ( 'NONE', 3,
 ( #15432, #7424, #3341, #16438 ),
 .UNSPECIFIED., .F., .F.,
 ( 4, 4 ),
 ( 2.376698214938428888E-07, 0.007646667280170321192 ),
 .UNSPECIFIED. ) ;
#135=CARTESIAN_POINT ( 'NONE',  ( -11.76794919243112325, -14.22000000000000242, -3.823638476888998827 ) ) ;
#138=CARTESIAN_POINT ( 'NONE',  ( 7.999999999999904965, 7.773118517290098950, 17.32050807568881368 ) ) ;
#150=CARTESIAN_POINT ( 'NONE',  ( 15.58845726811991916, 7.773118517290098950, -10.99999999999996092 ) ) ;
#154=CARTESIAN_POINT ( 'NONE',  ( -13.39378209699495592, -2.969872329747732787E-15, 1.511216576358205943 ) ) ;
#158=CARTESIAN_POINT ( 'NONE',  ( -7.409984580736203970E-16, -7.320000000000002949, 12.37355403259654985 ) ) ;
#160=EDGE_CURVE ( 'NONE', #16949, #8284, #16780, .T. ) ;
#161=CARTESIAN_POINT ( 'NONE',  ( -4.171729424061791036, -14.46999999999999709, 12.83926296998457239 ) ) ;
#162=AXIS2_PLACEMENT_3D ( 'NONE', #175, #4418, #13594 ) ;
#167=CARTESIAN_POINT ( 'NONE',  ( -16.03540712409196090, 8.027799080943070820, -8.457499700851245805 ) ) ;
#175=CARTESIAN_POINT ( 'NONE',  ( 0.000000000000000000, 0.000000000000000000, 0.000000000000000000 ) ) ;
#177=CARTESIAN_POINT ( 'NONE',  ( 13.49999999999999822, 28.28000000000000114, 4.386415899144237684 ) ) ;
#178=CARTESIAN_POINT ( 'NONE',  ( -11.76794919243112325, 4.080000000000008065, 3.823638476888994386 ) ) ;
#180=CARTESIAN_POINT ( 'NONE',  ( 13.49999999999999822, -17.72000000000000242, 4.386415899144237684 ) ) ;
#185=VECTOR ( 'NONE', #11440, 1000.000000000000000 ) ;
#186=CARTESIAN_POINT ( 'NONE',  ( 0.000000000000000000, 0.000000000000000000, 0.000000000000000000 ) ) ;
#189=FACE_OUTER_BOUND ( 'NONE', #3646, .T. ) ;
#201=VERTEX_POINT ( 'NONE', #13114 ) ;
#205=CARTESIAN_POINT ( 'NONE',  ( 13.50000000000000355, 7.579999999999999183, -4.386415899144233244 ) ) ;
#207=CARTESIAN_POINT ( 'NONE',  ( -3.708203932499367195, 6.196025403784440222, -11.41267819554184548 ) ) ;
#218=CARTESIAN_POINT ( 'NONE',  ( 2.138189944381238661, 5.756881422320270225, 13.49999999999999822 ) ) ;
#220=PLANE ( 'NONE',  #1477 ) ;
#221=CARTESIAN_POINT ( 'NONE',  ( -18.99999999999998224, 0.000000000000000000, -1.732050807569074369 ) ) ;
#222=CARTESIAN_POINT ( 'NONE',  ( -3.636496289402152637, 24.33000000000001961, -11.19198476289190936 ) ) ;
#229=CARTESIAN_POINT ( 'NONE',  ( -9.831838144771234411, 8.007813437504038845, 15.31996850146883382 ) ) ;
#239=ORIENTED_EDGE ( 'NONE', *, *, #2811, .F. ) ;
#249=CARTESIAN_POINT ( 'NONE',  ( 8.343458848123578520, -14.02000000000000135, 11.48378591275254124 ) ) ;
#254=CARTESIAN_POINT ( 'NONE',  ( -15.32106749056504569, 7.956441901775577641, -10.18076046065011475 ) ) ;
#261=CARTESIAN_POINT ( 'NONE',  ( -1.157795017994400766, 7.956106560002618622, -18.35996578475040764 ) ) ;
#262=CARTESIAN_POINT ( 'NONE',  ( -1.900613283894436512, 1.469143981464172022, 12.00000000000000000 ) ) ;
#263=CARTESIAN_POINT ( 'NONE',  ( 0.000000000000000000, 9.000000000000000000, 0.000000000000000000 ) ) ;
#265=CARTESIAN_POINT ( 'NONE',  ( 2.279995255611139653E-15, -2.819999999999999840, -12.37355403259654985 ) ) ;
#267=CARTESIAN_POINT ( 'NONE',  ( -13.49999999999999822, 2.079999999999998295, 4.386415899144235020 ) ) ;
#275=CYLINDRICAL_SURFACE ( 'NONE', #15212, 13.50000000000000000 ) ;
#277=EDGE_CURVE ( 'NONE', #106, #16538, #15358, .T. ) ;
#282=ORIENTED_EDGE ( 'NONE', *, *, #13910, .F. ) ;
#286=ORIENTED_EDGE ( 'NONE', *, *, #1923, .T. ) ;
#290=CARTESIAN_POINT ( 'NONE',  ( 13.50000000000000000, 4.430000000000003268, 1.734723475976807094E-15 ) ) ;
#291=CARTESIAN_POINT ( 'NONE',  ( -7.379696451821980833E-14, 6.046025403784444308, -12.00000000000000000 ) ) ;
#298=CARTESIAN_POINT ( 'NONE',  ( 12.00000000000006217, 8.563974596215590651, 1.734723475976807094E-15 ) ) ;
#303=VECTOR ( 'NONE', #7629, 1000.000000000000000 ) ;
#305=CARTESIAN_POINT ( 'NONE',  ( -17.42428528562830792, 5.918584287042170544, -19.29752010712871169 ) ) ;
#309=VERTEX_POINT ( 'NONE', #1472 ) ;
#322=ORIENTED_EDGE ( 'NONE', *, *, #15118, .T. ) ;
#331=CARTESIAN_POINT ( 'NONE',  ( 8.343458848123578520, -17.01999999999999957, 11.48378591275254124 ) ) ;
#335=CARTESIAN_POINT ( 'NONE',  ( 7.272992578804311492, -18.12000000000000455, -10.01041549318726709 ) ) ;
#340=FACE_OUTER_BOUND ( 'NONE', #15456, .T. ) ;
#347=FACE_OUTER_BOUND ( 'NONE', #6188, .T. ) ;
#348=CARTESIAN_POINT ( 'NONE',  ( 11.76794919243112680, -9.419999999999999929, -3.823638476888993942 ) ) ;
#350=AXIS2_PLACEMENT_3D ( 'NONE', #8881, #10118, #2121 ) ;
#352=B_SPLINE_CURVE_WITH_KNOTS ( 'NONE', 3,
 ( #3485, #13293, #14513, #4996 ),
 .UNSPECIFIED., .F., .F.,
 ( 4, 4 ),
 ( 2.383248697869603246E-07, 0.007646667935218606771 ),
 .UNSPECIFIED. ) ;
#355=ADVANCED_FACE ( 'NONE', ( #5565 ), #16407, .F. ) ;
#359=FACE_OUTER_BOUND ( 'NONE', #797, .T. ) ;
#360=AXIS2_PLACEMENT_3D ( 'NONE', #566, #14158, #6227 ) ;
#362=CARTESIAN_POINT ( 'NONE',  ( -7.416407864998753041, 0.6139745962155744863, -10.20780970022450340 ) ) ;
#363=FACE_OUTER_BOUND ( 'NONE', #6334, .T. ) ;
#367=CARTESIAN_POINT ( 'NONE',  ( 3.636496289402157078, 21.02999999999999403, -11.19198476289190936 ) ) ;
#368=VERTEX_POINT ( 'NONE', #6709 ) ;
#370=FACE_OUTER_BOUND ( 'NONE', #4288, .T. ) ;
#372=CARTESIAN_POINT ( 'NONE',  ( 2.621994543952811015E-15, 4.180000000000005045, -14.19474002721660355 ) ) ;
#376=CARTESIAN_POINT ( 'NONE',  ( -13.49999999999999822, 6.080000000000002736, 4.386415899144235908 ) ) ;
#377=CARTESIAN_POINT ( 'NONE',  ( 1.900613283881106952, 0.2370931738958342305, -12.00000000000433253 ) ) ;
#378=CARTESIAN_POINT ( 'NONE',  ( 17.32050807568878170, 0.000000000000000000, -7.999999999999961808 ) ) ;
#387=CARTESIAN_POINT ( 'NONE',  ( 1.296431213746159106, 7.924856485849745447, -18.46737842244078465 ) ) ;
#393=CARTESIAN_POINT ( 'NONE',  ( -17.42428528562830436, 0.000000000000000000, -19.29752010712870813 ) ) ;
#394=CARTESIAN_POINT ( 'NONE',  ( -7.999999999999776179, 7.773118517290098062, -17.32050807568887762 ) ) ;
#395=EDGE_LOOP ( 'NONE', ( #15239, #541, #10576, #13529, #15146, #9172, #16089, #3558, #4390, #13299, #1334, #7181, #3213, #17164, #13126, #14247, #17014, #6081, #7599, #5297, #13812, #9329, #10126, #2086, #12913, #1173, #1080, #16108, #1978 ) ) ;
#398=CARTESIAN_POINT ( 'NONE',  ( 11.76794919243112325, -15.71999999999999709, 3.823638476888996163 ) ) ;
#401=CARTESIAN_POINT ( 'NONE',  ( -8.349340579021736986, 8.007293667506184320, 16.17792858571905157 ) ) ;
#404=ADVANCED_FACE ( 'NONE', ( #4042 ), #9457, .T. ) ;
#414=CARTESIAN_POINT ( 'NONE',  ( -15.34527529650339872, 7.924527530346060722, 10.35822530491739535 ) ) ;
#415=CARTESIAN_POINT ( 'NONE',  ( 2.207926304393408011E-15, 8.062177826491096155, 17.99999999999999645 ) ) ;
#419=CARTESIAN_POINT ( 'NONE',  ( -11.76794919243112325, 33.93000000000001393, -2.602085213965210642E-15 ) ) ;
#422=EDGE_CURVE ( 'NONE', #9696, #11984, #11941, .T. ) ;
#424=CARTESIAN_POINT ( 'NONE',  ( 11.76794919243112325, -18.72000000000000952, 3.823638476888996163 ) ) ;
#427=CARTESIAN_POINT ( 'NONE',  ( -3.636496289402152637, 0.3299999999999969624, -11.19198476289190936 ) ) ;
#429=CARTESIAN_POINT ( 'NONE',  ( 9.708203932499388955, 2.263974596215569512, 7.053423027509694521 ) ) ;
#436=CARTESIAN_POINT ( 'NONE',  ( -10.92172942406179104, 30.23000000000000753, 7.935100905948385908 ) ) ;
#437=CARTESIAN_POINT ( 'NONE',  ( 9.520470885617715595, -9.869999999999997442, 6.917026985038135400 ) ) ;
#439=CARTESIAN_POINT ( 'NONE',  ( 13.50000000000000000, -17.56999999999999673, 1.734723475976807094E-15 ) ) ;
#449=FACE_OUTER_BOUND ( 'NONE', #15937, .T. ) ;
#450=CYLINDRICAL_SURFACE ( 'NONE', #1302, 1.999999999999998224 ) ;
#454=CARTESIAN_POINT ( 'NONE',  ( -3.636496289402156190, 19.53000000000001890, 11.19198476289190758 ) ) ;
#460=CARTESIAN_POINT ( 'NONE',  ( 8.343458848123583849, 3.879999999999999449, -11.48378591275253768 ) ) ;
#462=CARTESIAN_POINT ( 'NONE',  ( -7.409984580736203970E-16, 28.67999999999999972, 12.37355403259654985 ) ) ;
#465=CARTESIAN_POINT ( 'NONE',  ( -4.171729424061787483, -0.6700000000000039257, -12.83926296998457417 ) ) ;
#474=CARTESIAN_POINT ( 'NONE',  ( -8.000000000000197176, 0.000000000000000000, 24.73863375370590134 ) ) ;
#476=CARTESIAN_POINT ( 'NONE',  ( -11.61452348585071803, 10.00000000000000000, -3.545951533830508762 ) ) ;
#479=CARTESIAN_POINT ( 'NONE',  ( -1.747636201723826943, 10.00000000000000000, 12.72100980577129015 ) ) ;
#480=FACE_OUTER_BOUND ( 'NONE', #14679, .T. ) ;
#481=CARTESIAN_POINT ( 'NONE',  ( 9.520470885617717371, 23.73000000000000043, -6.917026985038131848 ) ) ;
#486=CARTESIAN_POINT ( 'NONE',  ( 2.279995255611139653E-15, -14.82000000000000384, -12.37355403259654985 ) ) ;
#498=EDGE_CURVE ( 'NONE', #15482, #11876, #15501, .T. ) ;
#504=LINE ( 'NONE', #6976, #14193 ) ;
#506=CARTESIAN_POINT ( 'NONE',  ( -3.636496289402152637, 30.32999999999999474, -11.19198476289190936 ) ) ;
#511=CARTESIAN_POINT ( 'NONE',  ( -15.50029318102132336, 8.062211461649205546, -9.152478727637765488 ) ) ;
#512=CARTESIAN_POINT ( 'NONE',  ( -3.636496289402156190, -4.469999999999994422, 11.19198476289190758 ) ) ;
#518=DIRECTION ( 'NONE',  ( -0.5000000000000074385, 0.000000000000000000, 0.8660254037844342667 ) ) ;
#520=CARTESIAN_POINT ( 'NONE',  ( 3.708203932499371192, 8.896025403784447505, -11.41267819554184548 ) ) ;
#523=CARTESIAN_POINT ( 'NONE',  ( 11.76794919243112325, -6.569999999999999396, 1.734723475976807094E-15 ) ) ;
#528=AXIS2_PLACEMENT_3D ( 'NONE', #15251, #16589, #5659 ) ;
#534=DIRECTION ( 'NONE',  ( -3.741588754404567345E-15, 0.000000000000000000, 1.000000000000000000 ) ) ;
#540=CARTESIAN_POINT ( 'NONE',  ( 7.272992578804311492, 17.87999999999999190, -10.01041549318726709 ) ) ;
#541=ORIENTED_EDGE ( 'NONE', *, *, #14987, .T. ) ;
#545=CARTESIAN_POINT ( 'NONE',  ( -8.343458848123582072, 5.379999999999996341, 11.48378591275254124 ) ) ;
#546=VERTEX_POINT ( 'NONE', #930 ) ;
#548=CARTESIAN_POINT ( 'NONE',  ( -4.171729424061791036, 0.5300000000000026912, 12.83926296998457239 ) ) ;
#558=EDGE_CURVE ( 'NONE', #9583, #2472, #6171, .T. ) ;
#561=CARTESIAN_POINT ( 'NONE',  ( -3.708203932499369859, 7.663974596215570756, 11.41267819554184193 ) ) ;
#566=CARTESIAN_POINT ( 'NONE',  ( 10.99999999999990941, 0.000000000000000000, 15.58845726811995824 ) ) ;
#572=CARTESIAN_POINT ( 'NONE',  ( 13.50000000000000000, 33.43000000000001393, 1.734723475976807094E-15 ) ) ;
#575=CARTESIAN_POINT ( 'NONE',  ( -10.68872673103600945, 7.854708401161940579, 15.43494339453333808 ) ) ;
#578=LINE ( 'NONE', #12865, #13885 ) ;
#583=ORIENTED_EDGE ( 'NONE', *, *, #1031, .T. ) ;
#588=CARTESIAN_POINT ( 'NONE',  ( -16.03410433562986981, 8.027996319639555622, 8.458421099448614200 ) ) ;
#589=CARTESIAN_POINT ( 'NONE',  ( 0.000000000000000000, 0.000000000000000000, 0.000000000000000000 ) ) ;
#592=CARTESIAN_POINT ( 'NONE',  ( 7.272992578804308828, 28.98000000000000398, 10.01041549318726709 ) ) ;
#595=EDGE_CURVE ( 'NONE', #8209, #16817, #10586, .T. ) ;
#599=CARTESIAN_POINT ( 'NONE',  ( 9.520470885617715595, -6.869999999999993889, 6.917026985038135400 ) ) ;
#601=CARTESIAN_POINT ( 'NONE',  ( 12.00000000000003020, 2.713974596215575463, -3.899036354794882531 ) ) ;
#602=DIRECTION ( 'NONE',  ( -0.000000000000000000, -1.000000000000000000, -0.000000000000000000 ) ) ;
#605=( BOUNDED_CURVE ( )  B_SPLINE_CURVE ( 2, ( #15515, #15602, #7008, #4844, #16768, #4340, #16347, #4676, #13692, #10167, #14112, #1591, #12384 ),
 .UNSPECIFIED., .F., .F. ) 
 B_SPLINE_CURVE_WITH_KNOTS ( ( 3, 2, 2, 2, 2, 2, 3 ),
 ( 0.5416666666666666297, 0.5444444444444443976, 0.5500000000000000444, 0.5555555555555555802, 0.5611111111111111160, 0.5666666666666666519, 0.5694444444444444198 ),
 .UNSPECIFIED. ) 
 CURVE ( )  GEOMETRIC_REPRESENTATION_ITEM ( )  RATIONAL_B_SPLINE_CURVE ( ( 0.9755282581475768211, 0.9755282581475768211, 1.000000000000000000, 0.9510565162951535312, 1.000000000000000000, 0.9510565162951535312, 1.000000000000000000, 0.9510565162951535312, 1.000000000000000000, 0.9510565162951535312, 1.000000000000000000, 0.9755282581475768211, 0.9755282581475768211 ) ) 
 REPRESENTATION_ITEM ( '' )  );
#608=CARTESIAN_POINT ( 'NONE',  ( 20.00000000000000000, 0.000000000000000000, 7.056441485635107799E-14 ) ) ;
#609=CARTESIAN_POINT ( 'NONE',  ( 10.92172942406179104, 25.73000000000000398, -7.935100905948385908 ) ) ;
#610=CARTESIAN_POINT ( 'NONE',  ( 11.76794919243112325, -3.569999999999996732, 1.734723475976807094E-15 ) ) ;
#614=CARTESIAN_POINT ( 'NONE',  ( 1.653273178848926472E-15, 30.93000000000001393, 13.50000000000000000 ) ) ;
#619=DIRECTION ( 'NONE',  ( -0.000000000000000000, 1.000000000000000000, -0.000000000000000000 ) ) ;
#627=CARTESIAN_POINT ( 'NONE',  ( 9.520470885617715595, 23.13000000000001322, 6.917026985038135400 ) ) ;
#633=CARTESIAN_POINT ( 'NONE',  ( -13.35138662365028317, 1.798999282680476490E-09, 1.996909364337476678 ) ) ;
#636=LINE ( 'NONE', #804, #6795 ) ;
#640=EDGE_CURVE ( 'NONE', #17255, #13655, #11147, .T. ) ;
#644=CARTESIAN_POINT ( 'NONE',  ( -21.14483242576211453, 7.170662809914417402, -2.970370385949514080 ) ) ;
#653=ORIENTED_EDGE ( 'NONE', *, *, #15929, .T. ) ;
#654=VECTOR ( 'NONE', #10791, 1000.000000000000000 ) ;
#655=EDGE_LOOP ( 'NONE', ( #16025, #4531, #10556, #1146 ) ) ;
#656=CARTESIAN_POINT ( 'NONE',  ( 8.050218389484046000, -18.96812680894470304, 8.940655939244130934 ) ) ;
#663=CARTESIAN_POINT ( 'NONE',  ( 9.205343071196221416, 2.875466159201993104E-15, -7.970107636079089453 ) ) ;
#664=CARTESIAN_POINT ( 'NONE',  ( -1.296431213746256139, 7.924856485849755217, 18.46737842244074201 ) ) ;
#665=DIRECTION ( 'NONE',  ( -0.000000000000000000, 1.000000000000000000, -0.000000000000000000 ) ) ;
#671=CARTESIAN_POINT ( 'NONE',  ( 2.138189944381238661, 8.756881422320265784, 13.49999999999999822 ) ) ;
#673=CARTESIAN_POINT ( 'NONE',  ( -8.343458848123576743, 17.48000000000000753, -11.48378591275254301 ) ) ;
#676=CARTESIAN_POINT ( 'NONE',  ( -17.32050807568884210, 7.773118517290098950, 7.999999999999840128 ) ) ;
#677=CARTESIAN_POINT ( 'NONE',  ( 15.50029318102139086, 8.062211461649205546, 9.152478727637658906 ) ) ;
#680=CARTESIAN_POINT ( 'NONE',  ( 11.76794919243112325, 26.28000000000000824, 3.823638476888996163 ) ) ;
#683=CARTESIAN_POINT ( 'NONE',  ( 9.520470885617717371, -15.26999999999999957, -6.917026985038131848 ) ) ;
#685=CARTESIAN_POINT ( 'NONE',  ( 19.00000000000000711, 7.773118517290098062, -1.732050807568807249 ) ) ;
#686=CARTESIAN_POINT ( 'NONE',  ( 11.76794919243112325, -0.5699999999999871836, 1.734723475976807094E-15 ) ) ;
#689=CARTESIAN_POINT ( 'NONE',  ( 15.58845726811984811, 7.773118517290097174, 11.00000000000007283 ) ) ;
#693=CARTESIAN_POINT ( 'NONE',  ( 9.708203932499369415, 7.996025403784436492, 7.053423027509680310 ) ) ;
#694=CARTESIAN_POINT ( 'NONE',  ( 8.000000000000021316, 7.804634910649121515, -17.19094712553552284 ) ) ;
#695=CARTESIAN_POINT ( 'NONE',  ( -13.49999999999999822, 27.07999999999999474, 4.386415899144235908 ) ) ;
#696=EDGE_CURVE ( 'NONE', #8605, #6168, #15766, .T. ) ;
#697=ORIENTED_EDGE ( 'NONE', *, *, #1901, .T. ) ;
#710=CARTESIAN_POINT ( 'NONE',  ( -10.99999999999979394, 0.000000000000000000, -15.58845726812003996 ) ) ;
#715=CARTESIAN_POINT ( 'NONE',  ( 9.520470885617715595, 11.13000000000000078, 6.917026985038135400 ) ) ;
#716=FACE_OUTER_BOUND ( 'NONE', #17365, .T. ) ;
#722=CARTESIAN_POINT ( 'NONE',  ( -9.520470885617717371, 31.23000000000000753, 6.917026985038133624 ) ) ;
#730=CARTESIAN_POINT ( 'NONE',  ( 10.92172942406179104, 7.730000000000014637, -7.935100905948385908 ) ) ;
#734=CARTESIAN_POINT ( 'NONE',  ( 1.541208229742722979, 7.854057316169015479, 18.71369360505684298 ) ) ;
#746=CARTESIAN_POINT ( 'NONE',  ( -7.272992578804307939, -17.52000000000000313, -10.01041549318726886 ) ) ;
#752=AXIS2_PLACEMENT_3D ( 'NONE', #7158, #4411, #9822 ) ;
#754=CARTESIAN_POINT ( 'NONE',  ( 5.441113646577481866, 0.000000000000000000, -25.42428528562854595 ) ) ;
#759=DIRECTION ( 'NONE',  ( -0.000000000000000000, 1.000000000000000000, -0.000000000000000000 ) ) ;
#765=DIRECTION ( 'NONE',  ( -1.000000000000000000, 0.000000000000000000, -7.483177508809139424E-15 ) ) ;
#766=CARTESIAN_POINT ( 'NONE',  ( -2.138189944381195584, 5.256881422320269337, -13.50000000000001599 ) ) ;
#768=CARTESIAN_POINT ( 'NONE',  ( -3.636496289402156190, 31.53000000000000114, 11.19198476289190758 ) ) ;
#773=EDGE_CURVE ( 'NONE', #2050, #13044, #10025, .T. ) ;
#776=CARTESIAN_POINT ( 'NONE',  ( 7.329991333342587012, -1.736202706843530252E-17, -9.501117147637041072 ) ) ;
#779=CARTESIAN_POINT ( 'NONE',  ( 13.14483242576216782, 7.170662809914417402, -16.82677684650029093 ) ) ;
#780=DIRECTION ( 'NONE',  ( -0.000000000000000000, 1.000000000000000000, -0.000000000000000000 ) ) ;
#781=ORIENTED_EDGE ( 'NONE', *, *, #5478, .F. ) ;
#786=LINE ( 'NONE', #15444, #1757 ) ;
#791=DIRECTION ( 'NONE',  ( 1.000000000000000000, 0.000000000000000000, 3.741588754404567345E-15 ) ) ;
#793=CARTESIAN_POINT ( 'NONE',  ( -7.999999999999776179, 0.000000000000000000, -17.32050807568887762 ) ) ;
#796=CARTESIAN_POINT ( 'NONE',  ( -3.636496289402152637, 15.33000000000001073, -11.19198476289190936 ) ) ;
#797=EDGE_LOOP ( 'NONE', ( #2942, #3741, #4895, #12420 ) ) ;
#801=CARTESIAN_POINT ( 'NONE',  ( -7.409984580736203970E-16, 31.68000000000000682, 12.37355403259654985 ) ) ;
#804=CARTESIAN_POINT ( 'NONE',  ( -24.73863375370587292, 0.000000000000000000, -8.000000000000280664 ) ) ;
#805=( BOUNDED_CURVE ( )  B_SPLINE_CURVE ( 2, ( #9577, #16439, #10803, #7009, #13693, #13777, #8514, #4341, #15187, #362, #5767, #5414, #1592 ),
 .UNSPECIFIED., .F., .F. ) 
 B_SPLINE_CURVE_WITH_KNOTS ( ( 3, 2, 2, 2, 2, 2, 3 ),
 ( 0.2049045012548912914, 0.2086589264430994406, 0.2161677768195154337, 0.2236766271959315655, 0.2311854775723475863, 0.2386943279487635516, 0.2424487531369445559 ),
 .UNSPECIFIED. ) 
 CURVE ( )  GEOMETRIC_REPRESENTATION_ITEM ( )  RATIONAL_B_SPLINE_CURVE ( ( 0.9755282581475768211, 0.9755282581475758219, 1.000000000000000000, 0.9510565162951536422, 1.000000000000000000, 0.9510565162951536422, 1.000000000000000000, 0.9510565162951536422, 1.000000000000000000, 0.9510565162951536422, 1.000000000000000000, 0.9755282581477529025, 0.9755282581475768211 ) ) 
 REPRESENTATION_ITEM ( '' )  );
#810=ADVANCED_FACE ( 'NONE', ( #7365 ), #1474, .F. ) ;
#811=FACE_OUTER_BOUND ( 'NONE', #15308, .T. ) ;
#818=ORIENTED_EDGE ( 'NONE', *, *, #16024, .T. ) ;
#822=CARTESIAN_POINT ( 'NONE',  ( -4.171729424061787483, 28.32999999999999474, -12.83926296998457417 ) ) ;
#830=CARTESIAN_POINT ( 'NONE',  ( 2.222800136090958073E-15, 3.046025403784441643, -12.00000000000000000 ) ) ;
#837=CARTESIAN_POINT ( 'NONE',  ( 7.347880794884122694E-16, 0.000000000000000000, -18.00000000000000000 ) ) ;
#839=CARTESIAN_POINT ( 'NONE',  ( 16.64104048077464171, 7.924936010579561874, -8.111079018422952203 ) ) ;
#848=EDGE_CURVE ( 'NONE', #6168, #7996, #5214, .T. ) ;
#849=DIRECTION ( 'NONE',  ( 0.000000000000000000, 0.000000000000000000, 1.000000000000000000 ) ) ;
#859=CARTESIAN_POINT ( 'NONE',  ( -8.343458848123576743, 23.48000000000000398, -11.48378591275254301 ) ) ;
#860=VERTEX_POINT ( 'NONE', #5757 ) ;
#862=FACE_OUTER_BOUND ( 'NONE', #9261, .T. ) ;
#866=CARTESIAN_POINT ( 'NONE',  ( -13.50000000000000000, -0.06999999999998673950, -3.469446951953614189E-15 ) ) ;
#874=CARTESIAN_POINT ( 'NONE',  ( 3.708203932499368527, 1.696025403784435781, 11.41267819554184371 ) ) ;
#879=CARTESIAN_POINT ( 'NONE',  ( 11.76794919243112325, 14.28000000000000647, 3.823638476888996163 ) ) ;
#880=DIRECTION ( 'NONE',  ( 0.000000000000000000, -1.000000000000000000, 0.000000000000000000 ) ) ;
#881=ORIENTED_EDGE ( 'NONE', *, *, #14946, .T. ) ;
#884=CARTESIAN_POINT ( 'NONE',  ( -17.32050807568865736, 0.000000000000000000, -10.00000000000020428 ) ) ;
#885=CARTESIAN_POINT ( 'NONE',  ( -8.343458848123582072, -0.6200000000000037703, 11.48378591275254124 ) ) ;
#888=CARTESIAN_POINT ( 'NONE',  ( 0.000000000000000000, 9.000000000000000000, 0.000000000000000000 ) ) ;
#905=CARTESIAN_POINT ( 'NONE',  ( 11.76794919243112325, 5.430000000000004157, 1.734723475976807094E-15 ) ) ;
#908=VERTEX_POINT ( 'NONE', #12466 ) ;
#909=CARTESIAN_POINT ( 'NONE',  ( -10.92172942406178926, 31.63000000000002032, -7.935100905948389460 ) ) ;
#911=EDGE_CURVE ( 'NONE', #7559, #9213, #3287, .T. ) ;
#917=CARTESIAN_POINT ( 'NONE',  ( 8.120631507080247502, 3.937340487231679721E-15, -8.939559169390870252 ) ) ;
#920=DIRECTION ( 'NONE',  ( 0.000000000000000000, 1.000000000000000000, 0.000000000000000000 ) ) ;
#925=ORIENTED_EDGE ( 'NONE', *, *, #16490, .T. ) ;
#927=ORIENTED_EDGE ( 'NONE', *, *, #8049, .F. ) ;
#928=CARTESIAN_POINT ( 'NONE',  ( -10.92172942406178926, 16.63000000000000611, -7.935100905948389460 ) ) ;
#930=CARTESIAN_POINT ( 'NONE',  ( 25.42428528562856727, 0.000000000000000000, -5.441113646577394825 ) ) ;
#932=CARTESIAN_POINT ( 'NONE',  ( 8.000000000000023093, 0.000000000000000000, -17.32050807568876394 ) ) ;
#933=EDGE_CURVE ( 'NONE', #11898, #2603, #4937, .T. ) ;
#934=CARTESIAN_POINT ( 'NONE',  ( -2.138187238715951288, 6.603118674965478441, 13.50000087912394520 ) ) ;
#946=CARTESIAN_POINT ( 'NONE',  ( -4.171729424061787483, 23.33000000000001606, -12.83926296998457417 ) ) ;
#949=CYLINDRICAL_SURFACE ( 'NONE', #11715, 12.00000000000000178 ) ;
#951=ADVANCED_FACE ( 'NONE', ( #862 ), #949, .F. ) ;
#955=CARTESIAN_POINT ( 'NONE',  ( 13.50000000000000000, -10.56999999999999673, 1.734723475976807094E-15 ) ) ;
#968=CARTESIAN_POINT ( 'NONE',  ( -7.409984580736203970E-16, 13.67999999999999616, 12.37355403259654985 ) ) ;
#969=DIRECTION ( 'NONE',  ( -0.000000000000000000, -1.000000000000000000, -0.000000000000000000 ) ) ;
#977=VECTOR ( 'NONE', #10428, 999.9999999999998863 ) ;
#980=CARTESIAN_POINT ( 'NONE',  ( -3.708203932499385846, 9.463974596215601665, -11.41267819554190233 ) ) ;
#995=CARTESIAN_POINT ( 'NONE',  ( 9.520470885617715595, 2.129999999999992788, 6.917026985038135400 ) ) ;
#998=ORIENTED_EDGE ( 'NONE', *, *, #4773, .T. ) ;
#999=CARTESIAN_POINT ( 'NONE',  ( 2.621994543952811015E-15, 25.17999999999999616, -14.19474002721660355 ) ) ;
#1002=VECTOR ( 'NONE', #7762, 1000.000000000000000 ) ;
#1008=CARTESIAN_POINT ( 'NONE',  ( -1.403940416332137451E-13, 0.000000000000000000, 19.99999999999999289 ) ) ;
#1012=CARTESIAN_POINT ( 'NONE',  ( 15.58845726811984811, 0.000000000000000000, 11.00000000000007283 ) ) ;
#1016=ORIENTED_EDGE ( 'NONE', *, *, #3206, .T. ) ;
#1017=( BOUNDED_CURVE ( )  B_SPLINE_CURVE ( 2, ( #15588, #5906, #8648, #13915, #8735, #6084, #14094, #11285, #16662, #671, #3228 ),
 .UNSPECIFIED., .F., .F. ) 
 B_SPLINE_CURVE_WITH_KNOTS ( ( 3, 2, 2, 2, 2, 3 ),
 ( 0.4616868741582292324, 0.4666666666666666741, 0.4722222222222222099, 0.4777777777777778012, 0.4833333333333333370, 0.4861111111111111049 ),
 .UNSPECIFIED. ) 
 CURVE ( )  GEOMETRIC_REPRESENTATION_ITEM ( )  RATIONAL_B_SPLINE_CURVE ( ( 0.9909066287976675547, 0.9561288891717594218, 1.000000000000000000, 0.9510565162951535312, 1.000000000000000000, 0.9510565162951535312, 1.000000000000000000, 0.9510565162951535312, 1.000000000000000000, 0.9755282581475768211, 0.9755282581475768211 ) ) 
 REPRESENTATION_ITEM ( '' )  );
#1020=CARTESIAN_POINT ( 'NONE',  ( -10.92172942406178926, 13.63000000000000256, -7.935100905948389460 ) ) ;
#1031=EDGE_CURVE ( 'NONE', #4554, #3828, #15695, .T. ) ;
#1033=CARTESIAN_POINT ( 'NONE',  ( 7.272992578804308828, 19.98000000000000043, 10.01041549318726709 ) ) ;
#1035=AXIS2_PLACEMENT_3D ( 'NONE', #6946, #16466, #10917 ) ;
#1043=CARTESIAN_POINT ( 'NONE',  ( 8.343458848123578520, -8.020000000000003126, 11.48378591275254124 ) ) ;
#1049=EDGE_CURVE ( 'NONE', #17099, #6127, #17123, .T. ) ;
#1054=DIRECTION ( 'NONE',  ( 1.426480712616743731E-14, 0.000000000000000000, -1.000000000000000000 ) ) ;
#1056=ORIENTED_EDGE ( 'NONE', *, *, #8622, .T. ) ;
#1057=CARTESIAN_POINT ( 'NONE',  ( 11.76794919243112325, 8.429999999999992610, 1.734723475976807094E-15 ) ) ;
#1062=CARTESIAN_POINT ( 'NONE',  ( 4.171729424061791924, -4.969999999999995310, -12.83926296998457239 ) ) ;
#1072=DIRECTION ( 'NONE',  ( -0.000000000000000000, -1.000000000000000000, -0.000000000000000000 ) ) ;
#1079=AXIS2_PLACEMENT_3D ( 'NONE', #1741, #4228, #11215 ) ;
#1080=ORIENTED_EDGE ( 'NONE', *, *, #8622, .F. ) ;
#1083=CARTESIAN_POINT ( 'NONE',  ( -11.76794919243112325, 3.930000000000002824, -2.602085213965210642E-15 ) ) ;
#1085=ORIENTED_EDGE ( 'NONE', *, *, #13634, .F. ) ;
#1086=CARTESIAN_POINT ( 'NONE',  ( 10.92172942406179104, 21.73000000000000043, -7.935100905948385908 ) ) ;
#1093=CARTESIAN_POINT ( 'NONE',  ( 5.441113646577480978, 5.918584287042170544, -25.42428528562854595 ) ) ;
#1094=AXIS2_PLACEMENT_3D ( 'NONE', #11321, #3086, #15360 ) ;
#1096=CARTESIAN_POINT ( 'NONE',  ( 3.122018999846114085, 10.00000000000000000, -13.05075980765145438 ) ) ;
#1110=EDGE_CURVE ( 'NONE', #10472, #4018, #13395, .T. ) ;
#1114=CIRCLE ( 'NONE', #11015, 26.00000000000000355 ) ;
#1118=CARTESIAN_POINT ( 'NONE',  ( 0.000000000000000000, 9.999999999999998224, 0.000000000000000000 ) ) ;
#1119=CARTESIAN_POINT ( 'NONE',  ( 7.272992578804311492, 20.87999999999999545, -10.01041549318726709 ) ) ;
#1123=ORIENTED_EDGE ( 'NONE', *, *, #10137, .T. ) ;
#1126=CARTESIAN_POINT ( 'NONE',  ( 3.636496289402157078, 27.02999999999999758, -11.19198476289190936 ) ) ;
#1128=DIRECTION ( 'NONE',  ( 0.000000000000000000, 0.000000000000000000, -1.000000000000000000 ) ) ;
#1131=CARTESIAN_POINT ( 'NONE',  ( 13.50000000000000000, -7.570000000000000284, 1.734723475976807094E-15 ) ) ;
#1142=CARTESIAN_POINT ( 'NONE',  ( -3.636496289402156190, 13.53000000000001357, 11.19198476289190758 ) ) ;
#1144=ORIENTED_EDGE ( 'NONE', *, *, #3312, .F. ) ;
#1145=CARTESIAN_POINT ( 'NONE',  ( 7.272992578804311492, 2.880000000000001670, -10.01041549318726709 ) ) ;
#1146=ORIENTED_EDGE ( 'NONE', *, *, #15825, .T. ) ;
#1150=CARTESIAN_POINT ( 'NONE',  ( -8.343458848123576743, -4.520000000000004903, -11.48378591275254301 ) ) ;
#1152=EDGE_CURVE ( 'NONE', #3134, #1210, #16777, .T. ) ;
#1153=PLANE ( 'NONE',  #8823 ) ;
#1161=CYLINDRICAL_SURFACE ( 'NONE', #15110, 26.00000000000000355 ) ;
#1162=LINE ( 'NONE', #9576, #6487 ) ;
#1168=VERTEX_POINT ( 'NONE', #1555 ) ;
#1171=CARTESIAN_POINT ( 'NONE',  ( 11.76794919243112325, 2.280000000000006466, 3.823638476888996163 ) ) ;
#1172=VERTEX_POINT ( 'NONE', #415 ) ;
#1173=ORIENTED_EDGE ( 'NONE', *, *, #13007, .F. ) ;
#1174=CARTESIAN_POINT ( 'NONE',  ( -13.49999999999999822, 20.08000000000001251, 4.386415899144235908 ) ) ;
#1185=CARTESIAN_POINT ( 'NONE',  ( -0.2535909892785384590, 9.999999999999994671, -13.17844121984262173 ) ) ;
#1187=CARTESIAN_POINT ( 'NONE',  ( 7.347880794884122694E-16, 0.000000000000000000, -20.00000000000000000 ) ) ;
#1190=ORIENTED_EDGE ( 'NONE', *, *, #13167, .F. ) ;
#1191=VERTEX_POINT ( 'NONE', #11032 ) ;
#1193=VERTEX_POINT ( 'NONE', #16404 ) ;
#1197=CARTESIAN_POINT ( 'NONE',  ( 10.85009556066085423, 7.815224736851130949, 15.50190989971483191 ) ) ;
#1200=VECTOR ( 'NONE', #2937, 1000.000000000000000 ) ;
#1205=CARTESIAN_POINT ( 'NONE',  ( -7.409984580736203970E-16, 16.68000000000000327, 12.37355403259654985 ) ) ;
#1207=ADVANCED_FACE ( 'NONE', ( #6254 ), #4748, .F. ) ;
#1210=VERTEX_POINT ( 'NONE', #13050 ) ;
#1211=CARTESIAN_POINT ( 'NONE',  ( -15.58845726811999910, 0.000000000000000000, 10.99999999999985256 ) ) ;
#1213=CARTESIAN_POINT ( 'NONE',  ( 15.28534784291390203, 6.548267719634619510, 18.06260399879755951 ) ) ;
#1214=CARTESIAN_POINT ( 'NONE',  ( -3.636496289402152637, -11.66999999999999993, -11.19198476289190936 ) ) ;
#1216=CARTESIAN_POINT ( 'NONE',  ( 2.621994543952811015E-15, -9.820000000000003837, -14.19474002721660355 ) ) ;
#1224=EDGE_CURVE ( 'NONE', #6427, #1193, #9016, .T. ) ;
#1229=CARTESIAN_POINT ( 'NONE',  ( -7.409984580736203970E-16, 4.680000000000003268, 12.37355403259654985 ) ) ;
#1232=CARTESIAN_POINT ( 'NONE',  ( 2.138189814981843906, 9.756881417667548462, 13.50000004204441062 ) ) ;
#1233=CARTESIAN_POINT ( 'NONE',  ( 13.49999999999999822, -11.72000000000000064, 4.386415899144237684 ) ) ;
#1234=CARTESIAN_POINT ( 'NONE',  ( -9.999999999999776179, 0.000000000000000000, -17.32050807568890605 ) ) ;
#1236=DIRECTION ( 'NONE',  ( -0.5000000000000074385, 0.000000000000000000, 0.8660254037844342667 ) ) ;
#1241=CARTESIAN_POINT ( 'NONE',  ( 0.000000000000000000, 5.918584287042170544, 0.000000000000000000 ) ) ;
#1249=ORIENTED_EDGE ( 'NONE', *, *, #6676, .T. ) ;
#1253=ORIENTED_EDGE ( 'NONE', *, *, #3103, .F. ) ;
#1254=CARTESIAN_POINT ( 'NONE',  ( -4.171729424061787483, 19.33000000000001251, -12.83926296998457417 ) ) ;
#1255=CARTESIAN_POINT ( 'NONE',  ( 7.999999999999904965, 7.773118517290098950, 17.32050807568881368 ) ) ;
#1257=CARTESIAN_POINT ( 'NONE',  ( 13.50000000000000355, 13.57999999999999652, -4.386415899144233244 ) ) ;
#1266=CARTESIAN_POINT ( 'NONE',  ( -5.314818182906294375, 10.00000000000000888, -11.69530585927466326 ) ) ;
#1268=( BOUNDED_CURVE ( )  B_SPLINE_CURVE ( 2, ( #11581, #16956, #5937, #11317, #16695, #10178, #14294, #15355, #14038, #3259, #6277, #15703, #8593 ),
 .UNSPECIFIED., .F., .F. ) 
 B_SPLINE_CURVE_WITH_KNOTS ( ( 3, 2, 2, 2, 2, 2, 3 ),
 ( 0.5694444444444444198, 0.5722222222222221877, 0.5777777777777777235, 0.5833333333333333703, 0.5888888888888889062, 0.5944444444444444420, 0.5972222222222222099 ),
 .UNSPECIFIED. ) 
 CURVE ( )  GEOMETRIC_REPRESENTATION_ITEM ( )  RATIONAL_B_SPLINE_CURVE ( ( 0.9755282581475768211, 0.9755282581475768211, 1.000000000000000000, 0.9510565162951535312, 1.000000000000000000, 0.9510565162951535312, 1.000000000000000000, 0.9510565162951535312, 1.000000000000000000, 0.9510565162951535312, 1.000000000000000000, 0.9755282581475768211, 0.9755282581475768211 ) ) 
 REPRESENTATION_ITEM ( '' )  );
#1269=DIRECTION ( 'NONE',  ( -0.000000000000000000, 1.000000000000000000, -0.000000000000000000 ) ) ;
#1275=VERTEX_POINT ( 'NONE', #10069 ) ;
#1278=CARTESIAN_POINT ( 'NONE',  ( -19.00000000000001776, 7.773118517290098950, 1.732050807568674466 ) ) ;
#1285=CARTESIAN_POINT ( 'NONE',  ( -3.636496289402156190, 16.53000000000001535, 11.19198476289190758 ) ) ;
#1294=CARTESIAN_POINT ( 'NONE',  ( 2.279995255611139653E-15, -8.820000000000000284, -12.37355403259654985 ) ) ;
#1295=CARTESIAN_POINT ( 'NONE',  ( -11.00000000000012612, 0.000000000000000000, 15.58845726811980725 ) ) ;
#1296=CARTESIAN_POINT ( 'NONE',  ( 2.621994543952811015E-15, -3.820000000000004281, -14.19474002721660355 ) ) ;
#1298=ADVANCED_FACE ( 'NONE', ( #12702 ), #4575, .F. ) ;
#1302=AXIS2_PLACEMENT_3D ( 'NONE', #3178, #5860, #10015 ) ;
#1311=CARTESIAN_POINT ( 'NONE',  ( 2.279995255611139653E-15, 0.1800000000000001044, -12.37355403259654985 ) ) ;
#1315=CARTESIAN_POINT ( 'NONE',  ( 13.50000000000000000, -5.569999999999998508, 1.734723475976807094E-15 ) ) ;
#1318=CYLINDRICAL_SURFACE ( 'NONE', #16121, 26.00000000000000355 ) ;
#1322=CARTESIAN_POINT ( 'NONE',  ( -12.00000000000000178, 9.895771319534587107, 2.592753011680899000 ) ) ;
#1329=CARTESIAN_POINT ( 'NONE',  ( -18.11515225121977579, 8.027996313748971602, -0.6918446750616502605 ) ) ;
#1333=ORIENTED_EDGE ( 'NONE', *, *, #12837, .T. ) ;
#1334=ORIENTED_EDGE ( 'NONE', *, *, #1418, .F. ) ;
#1335=CARTESIAN_POINT ( 'NONE',  ( 13.50000000000000000, 18.43000000000000327, 1.734723475976807094E-15 ) ) ;
#1338=CARTESIAN_POINT ( 'NONE',  ( -13.50000000000000000, 14.92999999999999972, -3.469446951953614189E-15 ) ) ;
#1341=ADVANCED_FACE ( 'NONE', ( #8997 ), #4231, .T. ) ;
#1347=CARTESIAN_POINT ( 'NONE',  ( 7.416407864998777910, 9.013974596215598822, -10.20780970022453182 ) ) ;
#1349=CARTESIAN_POINT ( 'NONE',  ( 0.000000000000000000, 30.93000000000001393, 0.000000000000000000 ) ) ;
#1351=CARTESIAN_POINT ( 'NONE',  ( -8.291044507619272909E-14, 7.180000000000005045, -13.50000000000000000 ) ) ;
#1357=ORIENTED_EDGE ( 'NONE', *, *, #595, .F. ) ;
#1378=CARTESIAN_POINT ( 'NONE',  ( -10.16733827920521804, 1.259542957514475215E-16, -7.849773118324066878 ) ) ;
#1381=CARTESIAN_POINT ( 'NONE',  ( 11.76794919243112680, -12.42000000000000171, -3.823638476888993942 ) ) ;
#1383=CARTESIAN_POINT ( 'NONE',  ( -8.343458848123582072, -11.62000000000000632, 11.48378591275254124 ) ) ;
#1385=EDGE_CURVE ( 'NONE', #4199, #17188, #4662, .T. ) ;
#1396=CARTESIAN_POINT ( 'NONE',  ( -7.272992578804307939, 9.480000000000009308, -10.01041549318726886 ) ) ;
#1399=CARTESIAN_POINT ( 'NONE',  ( -11.76794919243112325, 3.780000000000002913, -3.823638476888998827 ) ) ;
#1403=CARTESIAN_POINT ( 'NONE',  ( -10.92172942406179104, -6.769999999999997797, 7.935100905948385908 ) ) ;
#1413=CARTESIAN_POINT ( 'NONE',  ( -19.00000000000001776, 0.000000000000000000, 1.732050807568674466 ) ) ;
#1418=EDGE_CURVE ( 'NONE', #7389, #9499, #14638, .T. ) ;
#1419=VERTEX_POINT ( 'NONE', #2071 ) ;
#1421=LINE ( 'NONE', #2827, #9613 ) ;
#1422=CARTESIAN_POINT ( 'NONE',  ( -4.171729424061787483, 16.33000000000001251, -12.83926296998457417 ) ) ;
#1423=ORIENTED_EDGE ( 'NONE', *, *, #12269, .F. ) ;
#1427=CARTESIAN_POINT ( 'NONE',  ( 13.50000000000000000, 10.42999999999999439, 1.734723475976807094E-15 ) ) ;
#1428=CARTESIAN_POINT ( 'NONE',  ( -1.900613283894436512, 7.469143981464171134, 12.00000000000000000 ) ) ;
#1435=CARTESIAN_POINT ( 'NONE',  ( 9.708203932499419153, 8.263974596215597046, 7.053423027509715837 ) ) ;
#1442=CARTESIAN_POINT ( 'NONE',  ( -7.999999999999777955, 7.836096772789082010, -17.06161034813192146 ) ) ;
#1443=CARTESIAN_POINT ( 'NONE',  ( -9.520470885617717371, 25.23000000000000398, 6.917026985038133624 ) ) ;
#1445=ORIENTED_EDGE ( 'NONE', *, *, #3312, .T. ) ;
#1447=ORIENTED_EDGE ( 'NONE', *, *, #6481, .T. ) ;
#1451=VECTOR ( 'NONE', #8697, 1000.000000000000000 ) ;
#1459=CIRCLE ( 'NONE', #14167, 1.999999999999998224 ) ;
#1463=ORIENTED_EDGE ( 'NONE', *, *, #1049, .T. ) ;
#1471=CARTESIAN_POINT ( 'NONE',  ( -11.76794919243112325, -8.070000000000000284, -2.602085213965210642E-15 ) ) ;
#1472=CARTESIAN_POINT ( 'NONE',  ( 5.441113646577305119, 0.000000000000000000, 25.42428528562857792 ) ) ;
#1473=CARTESIAN_POINT ( 'NONE',  ( -8.343458848123576743, -15.52000000000000668, -11.48378591275254301 ) ) ;
#1474=( BOUNDED_SURFACE ( )  B_SPLINE_SURFACE ( 1, 2, ( 
 ( #12835, #2432, #5956, #8696, #15373, #12918, #10109, #3279, #12745, #14056, #6043, #15461, #14142, #2030, #3540, #801, #10280, #4793, #722, #6131, #10194, #11598, #14227, #11511, #16886, #15547, #8873, #3459, #14547, #7538, #6212, #7864, #16975, #4877, #15631, #462, #5209, #10599, #11918, #2520, #17296, #9282, #15962, #13238, #14634, #3867, #1126, #6538, #8519, #40, #12650, #15100, #16707, #9846, #1853, #11243, #15281, #8429, #16194, #16622, #8780, #12481, #5445, #5864, #5949, #11329, #3093, #5772, #16532, #3182, #10832, #4106, #627, #1681, #13956, #7097, #9755, #12568, #4439, #2999, #15367, #14136, #2024, #15193, #4612, #13783, #367, #11156, #1937, #4699, #13869, #1771, #7180, #9932, #8690, #10019, #454, #6038, #16793, #7266, #10104, #4525, #8604, #15455, #12152, #3365, #12739, #540, #3273, #14049, #7360, #11421, #11678, #4787, #15895, #12912, #2105, #4871, #6469, #10274, #6206, #17054, #15541, #8948, #796, #6291, #3803, #6126, #14390, #3453, #11505, #879, #12997, #7449, #17141, #968, #4959, #7706, #7532, #10362, #16881, #2193, #13082, #14567, #10187, #7800, #8868, #11592, #14220, #10448, #13171, #16968, #715, #15625, #9037, #2366, #3533, #14306, #7621, #15716, #3620, #2279, #6382, #11765, #5050, #15807, #3711, #9129, #14478, #5140, #1057, #11855, #17230, #10532, #9215, #12828, #11936, #17317, #3974, #2451, #2541, #2625, #4241, #14653, #9473, #8236, #9650, #5230, #13507, #1492, #17401, #9561, #5490, #3885, #17485, #1229, #10615, #12022, #12192, #178, #13422, #1399, #7969, #7881, #8058, #16150, #13258, #1145, #4058, #15982, #9302, #6556, #10871, #9386, #13338, #6641, #5316, #6815, #10700, #16240, #16068, #4149, #14737, #16333, #13596, #1311, #6726, #14821, #12104, #85, #5400, #10784, #14911, #10965, #2715, #8144, #2804, #6907, #5584, #12283, #16775, #6996, #5845, #16425, #9737, #265, #16688, #8413, #2893, #1665, #610, #10002, #7340, #1833, #15263, #9915, #7250, #8675, #11311, #2982, #9830, #15083, #5931, #7165, #6019, #4595, #16514, #4683, #3251, #3075, #523, #4329, #8501, #12551, #7080, #11402, #12464, #15349, #13851, #15000, #12634, #13939, #8325, #13764, #11139, #13680, #3161, #5673, #14032, #348, #4509, #1754, #437, #11053, #1578, #11228, #12371, #5755, #4421, #16602, #8588, #1920, #15175, #12723, #2499, #16028, #6431, #11815, #44, #11985, #16198, #7758, #6867, #2944, #12332, #5541, #16565, #9961, #8195, #16385, #1715, #135, #10925, #4201, #15226, #486, #4289, #9700, #8373, #16473, #4471, #398, #13729, #13901, #13558, #15134, #7045, #12424, #4379, #3031, #8462, #12514, #3123, #746, #14248, #12767, #11361, #13986, #2053, #12682, #6320, #3305, #10048, #656, #14333, #6065, #14078 ),
 ( #12856, #15398, #2134, #5979, #11620, #13027, #4901, #14164, #7651, #3214, #572, #10215, #8635, #7560, #1881, #16822, #6233, #11706, #8718, #7476, #16995, #1965, #909, #2222, #17083, #7297, #6155, #16736, #7390, #4642, #10300, #4729, #10130, #11532, #15483, #3394, #8807, #16910, #4988, #4813, #15568, #3479, #8893, #12938, #822, #15311, #15653, #3563, #8977, #10643, #10477, #9245, #9067, #5170, #16007, #20, #14420, #10726, #2308, #15837, #7736, #13365, #16091, #13112, #3655, #999, #11966, #5341, #6412, #3742, #11795, #15922, #13286, #3830, #17172, #5082, #7911, #9158, #9330, #14505, #6665, #8084, #17426, #14598, #2655, #13449, #2393, #13200, #1086, #6500, #11883, #10390, #17258, #10562, #12131, #2478, #17346, #3999, #15744, #1174, #3913, #9415, #6585, #14763, #1254, #5257, #14680, #2567, #7997, #12049, #1335, #6751, #9176, #14846, #9087, #5605, #3764, #11900, #8993, #14350, #5190, #13046, #928, #15672, #1422, #10494, #2239, #6338, #17100, #2739, #10406, #6839, #15763, #12215, #14440, #12306, #9586, #109, #7757, #6928, #14936, #13132, #1020, #6520, #6430, #11814, #17191, #5514, #15857, #14524, #2411, #10810, #4083, #9498, #8169, #13532, #10897, #16267, #4173, #2828, #8259, #16537, #10987, #3187, #4530, #8524, #11248, #11075, #9851, #9673, #5777, #16627, #4263, #2916, #11334, #8346, #16448, #13702, #13961, #16712, #1602, #7018, #12396, #12573, #5954, #4351, #9760, #15105, #4444, #13874, #15198, #3004, #8434, #1776, #13788, #9937, #1686, #545, #8695, #4617, #3098, #3278, #14055, #7102, #12486, #372, #11162, #460, #5869, #8609, #10024, #12744, #15372, #1942, #17146, #7805, #14141, #17059, #5055, #3458, #13089, #9042, #7454, #3538, #4792, #2029, #15546, #3625, #3716, #16974, #10367, #11510, #13176, #11597, #2198, #4704, #15460, #885, #3371, #12834, #10193, #7711, #12917, #14226, #2110, #6211, #10453, #4876, #15812, #10279, #9134, #15630, #8953, #14483, #14311, #6297, #11683, #6474, #5404, #11860, #15985, #9478, #9564, #1150, #17405, #6645, #1062, #10788, #12108, #16072, #1315, #6561, #5320, #17235, #13342, #6730, #8239, #5145, #1403, #10537, #11942, #15899, #4063, #6819, #3808, #9221, #14572, #2630, #13511, #2456, #17322, #7886, #12026, #3978, #10704, #13263, #5234, #9390, #10619, #3115, #3889, #14825, #16245, #8148, #14741, #10875, #4152, #9306, #14657, #2545, #7973, #1233, #8062, #13426, #16154, #2808, #2719, #12196, #89, #5494, #14914, #7167, #12637, #11055, #3163, #16605, #15002, #11141, #12374, #16335, #5675, #5847, #11313, #7082, #12553, #1580, #3255, #1668, #9832, #1495, #12285, #15177, #5587, #10967, #13599, #9917, #2984, #6909, #4243, #15352, #439, #180, #15267, #9652, #8590, #2895, #10005 ) ),
 .UNSPECIFIED., .F., .F., .F. ) 
 B_SPLINE_SURFACE_WITH_KNOTS ( ( 2, 2 ),
 ( 3, 2, 2, 2, 2, 2, 2, 2, 2, 2, 2, 2, 2, 2, 2, 2, 2, 2, 2, 2, 2, 2, 2, 2, 2, 2, 2, 2, 2, 2, 2, 2, 2, 2, 2, 2, 2, 2, 2, 2, 2, 2, 2, 2, 2, 2, 2, 2, 2, 2, 2, 2, 2, 2, 2, 2, 2, 2, 2, 2, 2, 2, 2, 2, 2, 2, 2, 2, 2, 2, 2, 2, 2, 2, 2, 2, 2, 2, 2, 2, 2, 2, 2, 2, 2, 2, 2, 2, 2, 2, 2, 2, 2, 2, 2, 2, 2, 2, 2, 2, 2, 2, 2, 2, 2, 2, 2, 2, 2, 2, 2, 2, 2, 2, 2, 2, 2, 2, 2, 2, 2, 2, 2, 2, 2, 2, 2, 2, 2, 2, 2, 2, 2, 2, 2, 2, 2, 2, 2, 2, 2, 2, 2, 2, 2, 2, 2, 2, 2, 2, 2, 2, 2, 2, 2, 2, 2, 2, 2, 2, 2, 2, 2, 2, 2, 2, 2, 2, 2, 2, 2, 2, 2, 2, 2, 2, 2, 2, 3 ),
 ( 0.000000000000000000, 1.000000000000000000 ),
 ( 0.000000000000000000, 0.005555555555555555768, 0.01111111111111111154, 0.01666666666666666644, 0.02222222222222222307, 0.02777777777777777624, 0.03333333333333333287, 0.03888888888888888951, 0.04444444444444444614, 0.05000000000000000278, 0.05555555555555555247, 0.06111111111111110911, 0.06666666666666666574, 0.07222222222222221544, 0.07777777777777777901, 0.08333333333333332871, 0.08888888888888889228, 0.09444444444444444198, 0.1000000000000000056, 0.1055555555555555552, 0.1111111111111111049, 0.1166666666666666685, 0.1222222222222222182, 0.1277777777777777679, 0.1333333333333333315, 0.1388888888888888951, 0.1444444444444444309, 0.1499999999999999944, 0.1555555555555555580, 0.1611111111111111216, 0.1666666666666666574, 0.1722222222222222210, 0.1777777777777777846, 0.1833333333333333204, 0.1888888888888888840, 0.1944444444444444475, 0.2000000000000000111, 0.2055555555555555469, 0.2111111111111111105, 0.2166666666666666741, 0.2222222222222222099, 0.2277777777777777735, 0.2333333333333333370, 0.2388888888888889006, 0.2444444444444444364, 0.2500000000000000000, 0.2555555555555555358, 0.2611111111111111271, 0.2666666666666666630, 0.2722222222222221988, 0.2777777777777777901, 0.2833333333333333259, 0.2888888888888888618, 0.2944444444444444531, 0.2999999999999999889, 0.3055555555555555802, 0.3111111111111111160, 0.3166666666666666519, 0.3222222222222222432, 0.3277777777777777790, 0.3333333333333333148, 0.3388888888888889062, 0.3444444444444444420, 0.3499999999999999778, 0.3555555555555555691, 0.3611111111111111049, 0.3666666666666666408, 0.3722222222222222321, 0.3777777777777777679, 0.3833333333333333592, 0.3888888888888888951, 0.3944444444444444309, 0.4000000000000000222, 0.4055555555555555580, 0.4111111111111110938, 0.4166666666666666852, 0.4222222222222222210, 0.4277777777777777568, 0.4333333333333333481, 0.4388888888888888840, 0.4444444444444444198, 0.4500000000000000111, 0.4555555555555555469, 0.4611111111111111382, 0.4666666666666666741, 0.4722222222222222099, 0.4777777777777778012, 0.4833333333333333370, 0.4888888888888888729, 0.4944444444444444642, 0.5000000000000000000, 0.5055555555555555358, 0.5111111111111110716, 0.5166666666666667185, 0.5222222222222222543, 0.5277777777777777901, 0.5333333333333333259, 0.5388888888888888618, 0.5444444444444443976, 0.5500000000000000444, 0.5555555555555555802, 0.5611111111111111160, 0.5666666666666666519, 0.5722222222222221877, 0.5777777777777777235, 0.5833333333333333703, 0.5888888888888889062, 0.5944444444444444420, 0.5999999999999999778, 0.6055555555555555136, 0.6111111111111111605, 0.6166666666666666963, 0.6222222222222222321, 0.6277777777777777679, 0.6333333333333333037, 0.6388888888888888395, 0.6444444444444444864, 0.6500000000000000222, 0.6555555555555555580, 0.6611111111111110938, 0.6666666666666666297, 0.6722222222222222765, 0.6777777777777778123, 0.6833333333333333481, 0.6888888888888888840, 0.6944444444444444198, 0.6999999999999999556, 0.7055555555555556024, 0.7111111111111111382, 0.7166666666666666741, 0.7222222222222222099, 0.7277777777777777457, 0.7333333333333332815, 0.7388888888888889284, 0.7444444444444444642, 0.7500000000000000000, 0.7555555555555555358, 0.7611111111111110716, 0.7666666666666667185, 0.7722222222222222543, 0.7777777777777777901, 0.7833333333333333259, 0.7888888888888888618, 0.7944444444444443976, 0.8000000000000000444, 0.8055555555555555802, 0.8111111111111111160, 0.8166666666666666519, 0.8222222222222221877, 0.8277777777777777235, 0.8333333333333333703, 0.8388888888888889062, 0.8444444444444444420, 0.8499999999999999778, 0.8555555555555555136, 0.8611111111111111605, 0.8666666666666666963, 0.8722222222222222321, 0.8777777777777777679, 0.8833333333333333037, 0.8888888888888888395, 0.8944444444444444864, 0.9000000000000000222, 0.9055555555555555580, 0.9111111111111110938, 0.9166666666666666297, 0.9222222222222222765, 0.9277777777777778123, 0.9333333333333333481, 0.9388888888888888840, 0.9444444444444444198, 0.9499999999999999556, 0.9555555555555556024, 0.9611111111111111382, 0.9666666666666666741, 0.9722222222222222099, 0.9777777777777777457, 0.9814746766279994761, 0.9912894233942795008 ),
 .UNSPECIFIED. ) 
 GEOMETRIC_REPRESENTATION_ITEM ( )  RATIONAL_B_SPLINE_SURFACE ( (
 ( 1.000000000000000000, 0.9510565162951535312, 1.000000000000000000, 0.9510565162951535312, 1.000000000000000000, 0.9510565162951535312, 1.000000000000000000, 0.9510565162951535312, 1.000000000000000000, 0.9510565162951535312, 1.000000000000000000, 0.9510565162951535312, 1.000000000000000000, 0.9510565162951535312, 1.000000000000000000, 0.9510565162951535312, 1.000000000000000000, 0.9510565162951535312, 1.000000000000000000, 0.9510565162951535312, 1.000000000000000000, 0.9510565162951535312, 1.000000000000000000, 0.9510565162951535312, 1.000000000000000000, 0.9510565162951535312, 1.000000000000000000, 0.9510565162951535312, 1.000000000000000000, 0.9510565162951535312, 1.000000000000000000, 0.9510565162951535312, 1.000000000000000000, 0.9510565162951535312, 1.000000000000000000, 0.9510565162951535312, 1.000000000000000000, 0.9510565162951535312, 1.000000000000000000, 0.9510565162951535312, 1.000000000000000000, 0.9510565162951535312, 1.000000000000000000, 0.9510565162951535312, 1.000000000000000000, 0.9510565162951535312, 1.000000000000000000, 0.9510565162951535312, 1.000000000000000000, 0.9510565162951535312, 1.000000000000000000, 0.9510565162951535312, 1.000000000000000000, 0.9510565162951535312, 1.000000000000000000, 0.9510565162951535312, 1.000000000000000000, 0.9510565162951535312, 1.000000000000000000, 0.9510565162951535312, 1.000000000000000000, 0.9510565162951535312, 1.000000000000000000, 0.9510565162951535312, 1.000000000000000000, 0.9510565162951535312, 1.000000000000000000, 0.9510565162951535312, 1.000000000000000000, 0.9510565162951535312, 1.000000000000000000, 0.9510565162951535312, 1.000000000000000000, 0.9510565162951535312, 1.000000000000000000, 0.9510565162951535312, 1.000000000000000000, 0.9510565162951535312, 1.000000000000000000, 0.9510565162951535312, 1.000000000000000000, 0.9510565162951535312, 1.000000000000000000, 0.9510565162951535312, 1.000000000000000000, 0.9510565162951535312, 1.000000000000000000, 0.9510565162951535312, 1.000000000000000000, 0.9510565162951535312, 1.000000000000000000, 0.9510565162951535312, 1.000000000000000000, 0.9510565162951535312, 1.000000000000000000, 0.9510565162951535312, 1.000000000000000000, 0.9510565162951535312, 1.000000000000000000, 0.9510565162951535312, 1.000000000000000000, 0.9510565162951535312, 1.000000000000000000, 0.9510565162951535312, 1.000000000000000000, 0.9510565162951535312, 1.000000000000000000, 0.9510565162951535312, 1.000000000000000000, 0.9510565162951535312, 1.000000000000000000, 0.9510565162951535312, 1.000000000000000000, 0.9510565162951535312, 1.000000000000000000, 0.9510565162951535312, 1.000000000000000000, 0.9510565162951535312, 1.000000000000000000, 0.9510565162951535312, 1.000000000000000000, 0.9510565162951535312, 1.000000000000000000, 0.9510565162951535312, 1.000000000000000000, 0.9510565162951535312, 1.000000000000000000, 0.9510565162951535312, 1.000000000000000000, 0.9510565162951535312, 1.000000000000000000, 0.9510565162951535312, 1.000000000000000000, 0.9510565162951535312, 1.000000000000000000, 0.9510565162951535312, 1.000000000000000000, 0.9510565162951535312, 1.000000000000000000, 0.9510565162951535312, 1.000000000000000000, 0.9510565162951535312, 1.000000000000000000, 0.9510565162951535312, 1.000000000000000000, 0.9510565162951535312, 1.000000000000000000, 0.9510565162951535312, 1.000000000000000000, 0.9510565162951535312, 1.000000000000000000, 0.9510565162951535312, 1.000000000000000000, 0.9510565162951535312, 1.000000000000000000, 0.9510565162951535312, 1.000000000000000000, 0.9510565162951535312, 1.000000000000000000, 0.9510565162951535312, 1.000000000000000000, 0.9510565162951535312, 1.000000000000000000, 0.9510565162951535312, 1.000000000000000000, 0.9510565162951535312, 1.000000000000000000, 0.9510565162951535312, 1.000000000000000000, 0.9510565162951535312, 1.000000000000000000, 0.9510565162951535312, 1.000000000000000000, 0.9510565162951535312, 1.000000000000000000, 0.9510565162951535312, 1.000000000000000000, 0.9510565162951535312, 1.000000000000000000, 0.9510565162951535312, 1.000000000000000000, 0.9510565162951535312, 1.000000000000000000, 0.9510565162951535312, 1.000000000000000000, 0.9510565162951535312, 1.000000000000000000, 0.9510565162951535312, 1.000000000000000000, 0.9510565162951535312, 1.000000000000000000, 0.9510565162951535312, 1.000000000000000000, 0.9510565162951535312, 1.000000000000000000, 0.9510565162951535312, 1.000000000000000000, 0.9510565162951535312, 1.000000000000000000, 0.9510565162951535312, 1.000000000000000000, 0.9510565162951535312, 1.000000000000000000, 0.9510565162951535312, 1.000000000000000000, 0.9510565162951535312, 1.000000000000000000, 0.9510565162951535312, 1.000000000000000000, 0.9510565162951535312, 1.000000000000000000, 0.9510565162951535312, 1.000000000000000000, 0.9510565162951535312, 1.000000000000000000, 0.9510565162951535312, 1.000000000000000000, 0.9510565162951535312, 1.000000000000000000, 0.9510565162951535312, 1.000000000000000000, 0.9510565162951535312, 1.000000000000000000, 0.9510565162951535312, 1.000000000000000000, 0.9510565162951535312, 1.000000000000000000, 0.9510565162951535312, 1.000000000000000000, 0.9510565162951535312, 1.000000000000000000, 0.9510565162951535312, 1.000000000000000000, 0.9510565162951535312, 1.000000000000000000, 0.9510565162951535312, 1.000000000000000000, 0.9510565162951535312, 1.000000000000000000, 0.9510565162951535312, 1.000000000000000000, 0.9510565162951535312, 1.000000000000000000, 0.9510565162951535312, 1.000000000000000000, 0.9510565162951535312, 1.000000000000000000, 0.9510565162951535312, 1.000000000000000000, 0.9510565162951535312, 1.000000000000000000, 0.9510565162951535312, 1.000000000000000000, 0.9510565162951535312, 1.000000000000000000, 0.9510565162951535312, 1.000000000000000000, 0.9510565162951535312, 1.000000000000000000, 0.9510565162951535312, 1.000000000000000000, 0.9510565162951535312, 1.000000000000000000, 0.9510565162951535312, 1.000000000000000000, 0.9510565162951535312, 1.000000000000000000, 0.9510565162951535312, 1.000000000000000000, 0.9510565162951535312, 1.000000000000000000, 0.9510565162951535312, 1.000000000000000000, 0.9510565162951535312, 1.000000000000000000, 0.9510565162951535312, 1.000000000000000000, 0.9510565162951535312, 1.000000000000000000, 0.9510565162951535312, 1.000000000000000000, 0.9510565162951535312, 1.000000000000000000, 0.9510565162951535312, 1.000000000000000000, 0.9510565162951535312, 1.000000000000000000, 0.9510565162951535312, 1.000000000000000000, 0.9510565162951535312, 1.000000000000000000, 0.9510565162951535312, 1.000000000000000000, 0.9510565162951535312, 1.000000000000000000, 0.9510565162951535312, 1.000000000000000000, 0.9510565162951535312, 1.000000000000000000, 0.9510565162951535312, 1.000000000000000000, 0.9510565162951535312, 1.000000000000000000, 0.9510565162951535312, 1.000000000000000000, 0.9510565162951535312, 1.000000000000000000, 0.9510565162951535312, 1.000000000000000000, 0.9510565162951535312, 1.000000000000000000, 0.9510565162951535312, 1.000000000000000000, 0.9510565162951535312, 1.000000000000000000, 0.9510565162951535312, 1.000000000000000000, 0.9510565162951535312, 1.000000000000000000, 0.9510565162951535312, 1.000000000000000000, 0.9510565162951535312, 1.000000000000000000, 0.9510565162951535312, 1.000000000000000000, 0.9510565162951535312, 1.000000000000000000, 0.9510565162951535312, 1.000000000000000000, 0.9510565162951535312, 1.000000000000000000, 0.9510565162951535312, 1.000000000000000000, 0.9510565162951535312, 1.000000000000000000, 0.9510565162951535312, 1.000000000000000000, 0.9510565162951535312, 1.000000000000000000, 0.9510565162951535312, 1.000000000000000000, 0.9510565162951535312, 1.000000000000000000, 0.9510565162951535312, 1.000000000000000000, 0.9510565162951535312, 1.000000000000000000, 0.9510565162951535312, 1.000000000000000000, 0.9510565162951535312, 1.000000000000000000, 0.9510565162951535312, 1.000000000000000000, 0.9674309604458272149, 0.9782075210486875783, 0.9782075210486875783, 0.9782075210486875783),
 ( 1.000000000000000000, 0.9510565162951535312, 1.000000000000000000, 0.9510565162951535312, 1.000000000000000000, 0.9510565162951535312, 1.000000000000000000, 0.9510565162951535312, 1.000000000000000000, 0.9510565162951535312, 1.000000000000000000, 0.9510565162951535312, 1.000000000000000000, 0.9510565162951535312, 1.000000000000000000, 0.9510565162951535312, 1.000000000000000000, 0.9510565162951535312, 1.000000000000000000, 0.9510565162951535312, 1.000000000000000000, 0.9510565162951535312, 1.000000000000000000, 0.9510565162951535312, 1.000000000000000000, 0.9510565162951535312, 1.000000000000000000, 0.9510565162951535312, 1.000000000000000000, 0.9510565162951535312, 1.000000000000000000, 0.9510565162951535312, 1.000000000000000000, 0.9510565162951535312, 1.000000000000000000, 0.9510565162951535312, 1.000000000000000000, 0.9510565162951535312, 1.000000000000000000, 0.9510565162951535312, 1.000000000000000000, 0.9510565162951535312, 1.000000000000000000, 0.9510565162951535312, 1.000000000000000000, 0.9510565162951535312, 1.000000000000000000, 0.9510565162951535312, 1.000000000000000000, 0.9510565162951535312, 1.000000000000000000, 0.9510565162951535312, 1.000000000000000000, 0.9510565162951535312, 1.000000000000000000, 0.9510565162951535312, 1.000000000000000000, 0.9510565162951535312, 1.000000000000000000, 0.9510565162951535312, 1.000000000000000000, 0.9510565162951535312, 1.000000000000000000, 0.9510565162951535312, 1.000000000000000000, 0.9510565162951535312, 1.000000000000000000, 0.9510565162951535312, 1.000000000000000000, 0.9510565162951535312, 1.000000000000000000, 0.9510565162951535312, 1.000000000000000000, 0.9510565162951535312, 1.000000000000000000, 0.9510565162951535312, 1.000000000000000000, 0.9510565162951535312, 1.000000000000000000, 0.9510565162951535312, 1.000000000000000000, 0.9510565162951535312, 1.000000000000000000, 0.9510565162951535312, 1.000000000000000000, 0.9510565162951535312, 1.000000000000000000, 0.9510565162951535312, 1.000000000000000000, 0.9510565162951535312, 1.000000000000000000, 0.9510565162951535312, 1.000000000000000000, 0.9510565162951535312, 1.000000000000000000, 0.9510565162951535312, 1.000000000000000000, 0.9510565162951535312, 1.000000000000000000, 0.9510565162951535312, 1.000000000000000000, 0.9510565162951535312, 1.000000000000000000, 0.9510565162951535312, 1.000000000000000000, 0.9510565162951535312, 1.000000000000000000, 0.9510565162951535312, 1.000000000000000000, 0.9510565162951535312, 1.000000000000000000, 0.9510565162951535312, 1.000000000000000000, 0.9510565162951535312, 1.000000000000000000, 0.9510565162951535312, 1.000000000000000000, 0.9510565162951535312, 1.000000000000000000, 0.9510565162951535312, 1.000000000000000000, 0.9510565162951535312, 1.000000000000000000, 0.9510565162951535312, 1.000000000000000000, 0.9510565162951535312, 1.000000000000000000, 0.9510565162951535312, 1.000000000000000000, 0.9510565162951535312, 1.000000000000000000, 0.9510565162951535312, 1.000000000000000000, 0.9510565162951535312, 1.000000000000000000, 0.9510565162951535312, 1.000000000000000000, 0.9510565162951535312, 1.000000000000000000, 0.9510565162951535312, 1.000000000000000000, 0.9510565162951535312, 1.000000000000000000, 0.9510565162951535312, 1.000000000000000000, 0.9510565162951535312, 1.000000000000000000, 0.9510565162951535312, 1.000000000000000000, 0.9510565162951535312, 1.000000000000000000, 0.9510565162951535312, 1.000000000000000000, 0.9510565162951535312, 1.000000000000000000, 0.9510565162951535312, 1.000000000000000000, 0.9510565162951535312, 1.000000000000000000, 0.9510565162951535312, 1.000000000000000000, 0.9510565162951535312, 1.000000000000000000, 0.9510565162951535312, 1.000000000000000000, 0.9510565162951535312, 1.000000000000000000, 0.9510565162951535312, 1.000000000000000000, 0.9510565162951535312, 1.000000000000000000, 0.9510565162951535312, 1.000000000000000000, 0.9510565162951535312, 1.000000000000000000, 0.9510565162951535312, 1.000000000000000000, 0.9510565162951535312, 1.000000000000000000, 0.9510565162951535312, 1.000000000000000000, 0.9510565162951535312, 1.000000000000000000, 0.9510565162951535312, 1.000000000000000000, 0.9510565162951535312, 1.000000000000000000, 0.9510565162951535312, 1.000000000000000000, 0.9510565162951535312, 1.000000000000000000, 0.9510565162951535312, 1.000000000000000000, 0.9510565162951535312, 1.000000000000000000, 0.9510565162951535312, 1.000000000000000000, 0.9510565162951535312, 1.000000000000000000, 0.9510565162951535312, 1.000000000000000000, 0.9510565162951535312, 1.000000000000000000, 0.9510565162951535312, 1.000000000000000000, 0.9510565162951535312, 1.000000000000000000, 0.9510565162951535312, 1.000000000000000000, 0.9510565162951535312, 1.000000000000000000, 0.9510565162951535312, 1.000000000000000000, 0.9510565162951535312, 1.000000000000000000, 0.9510565162951535312, 1.000000000000000000, 0.9510565162951535312, 1.000000000000000000, 0.9510565162951535312, 1.000000000000000000, 0.9510565162951535312, 1.000000000000000000, 0.9510565162951535312, 1.000000000000000000, 0.9510565162951535312, 1.000000000000000000, 0.9510565162951535312, 1.000000000000000000, 0.9510565162951535312, 1.000000000000000000, 0.9510565162951535312, 1.000000000000000000, 0.9510565162951535312, 1.000000000000000000, 0.9510565162951535312, 1.000000000000000000, 0.9510565162951535312, 1.000000000000000000, 0.9510565162951535312, 1.000000000000000000, 0.9510565162951535312, 1.000000000000000000, 0.9510565162951535312, 1.000000000000000000, 0.9510565162951535312, 1.000000000000000000, 0.9510565162951535312, 1.000000000000000000, 0.9510565162951535312, 1.000000000000000000, 0.9510565162951535312, 1.000000000000000000, 0.9510565162951535312, 1.000000000000000000, 0.9510565162951535312, 1.000000000000000000, 0.9510565162951535312, 1.000000000000000000, 0.9510565162951535312, 1.000000000000000000, 0.9510565162951535312, 1.000000000000000000, 0.9510565162951535312, 1.000000000000000000, 0.9510565162951535312, 1.000000000000000000, 0.9510565162951535312, 1.000000000000000000, 0.9510565162951535312, 1.000000000000000000, 0.9510565162951535312, 1.000000000000000000, 0.9510565162951535312, 1.000000000000000000, 0.9510565162951535312, 1.000000000000000000, 0.9510565162951535312, 1.000000000000000000, 0.9510565162951535312, 1.000000000000000000, 0.9510565162951535312, 1.000000000000000000, 0.9510565162951535312, 1.000000000000000000, 0.9510565162951535312, 1.000000000000000000, 0.9510565162951535312, 1.000000000000000000, 0.9510565162951535312, 1.000000000000000000, 0.9510565162951535312, 1.000000000000000000, 0.9510565162951535312, 1.000000000000000000, 0.9510565162951535312, 1.000000000000000000, 0.9510565162951535312, 1.000000000000000000, 0.9510565162951535312, 1.000000000000000000, 0.9510565162951535312, 1.000000000000000000, 0.9510565162951535312, 1.000000000000000000, 0.9510565162951535312, 1.000000000000000000, 0.9510565162951535312, 1.000000000000000000, 0.9510565162951535312, 1.000000000000000000, 0.9510565162951535312, 1.000000000000000000, 0.9510565162951535312, 1.000000000000000000, 0.9510565162951535312, 1.000000000000000000, 0.9510565162951535312, 1.000000000000000000, 0.9510565162951535312, 1.000000000000000000, 0.9510565162951535312, 1.000000000000000000, 0.9510565162951535312, 1.000000000000000000, 0.9510565162951535312, 1.000000000000000000, 0.9510565162951535312, 1.000000000000000000, 0.9510565162951535312, 1.000000000000000000, 0.9510565162951535312, 1.000000000000000000, 0.9510565162951535312, 1.000000000000000000, 0.9510565162951535312, 1.000000000000000000, 0.9510565162951535312, 1.000000000000000000, 0.9510565162951535312, 1.000000000000000000, 0.9510565162951535312, 1.000000000000000000, 0.9510565162951535312, 1.000000000000000000, 0.9510565162951535312, 1.000000000000000000, 0.9510565162951535312, 1.000000000000000000, 0.9510565162951535312, 1.000000000000000000, 0.9510565162951535312, 1.000000000000000000, 0.9674309604458272149, 0.9782075210486875783, 0.9782075210486875783, 0.9782075210486875783) ) ) 
 REPRESENTATION_ITEM ( '' )  SURFACE ( )  );
#1477=AXIS2_PLACEMENT_3D ( 'NONE', #16468, #5800, #3117 ) ;
#1480=CARTESIAN_POINT ( 'NONE',  ( -17.14741290055372147, 7.815224843475952810, -8.000000000000202505 ) ) ;
#1488=EDGE_CURVE ( 'NONE', #17140, #14888, #10411, .T. ) ;
#1492=CARTESIAN_POINT ( 'NONE',  ( 11.76794919243112680, 5.580000000000004512, -3.823638476888993942 ) ) ;
#1495=CARTESIAN_POINT ( 'NONE',  ( -13.49999999999999822, -15.91999999999999815, 4.386415899144235908 ) ) ;
#1496=DIRECTION ( 'NONE',  ( 0.8660254037844430375, 0.000000000000000000, -0.4999999999999925060 ) ) ;
#1503=DIRECTION ( 'NONE',  ( 0.000000000000000000, 1.000000000000000000, 0.000000000000000000 ) ) ;
#1513=ORIENTED_EDGE ( 'NONE', *, *, #13823, .F. ) ;
#1515=CARTESIAN_POINT ( 'NONE',  ( -25.42428528562860279, 0.000000000000000000, 5.441113646577211860 ) ) ;
#1517=CARTESIAN_POINT ( 'NONE',  ( -8.343458848123576743, 8.480000000000000426, -11.48378591275254301 ) ) ;
#1526=CARTESIAN_POINT ( 'NONE',  ( 3.708203932499389843, 9.163974596215608059, -11.41267819554190233 ) ) ;
#1530=DIRECTION ( 'NONE',  ( -0.000000000000000000, 1.000000000000000000, -0.000000000000000000 ) ) ;
#1533=CARTESIAN_POINT ( 'NONE',  ( -9.869785582228594478, 9.999999999999998224, 7.125699818525842666 ) ) ;
#1534=CARTESIAN_POINT ( 'NONE',  ( -9.354252080082858356, 8.052096965364873071, -15.42305849549719454 ) ) ;
#1535=ORIENTED_EDGE ( 'NONE', *, *, #4716, .F. ) ;
#1537=ORIENTED_EDGE ( 'NONE', *, *, #4951, .F. ) ;
#1540=CARTESIAN_POINT ( 'NONE',  ( -9.152478727637712197, 8.062211461649205546, 15.50029318102135356 ) ) ;
#1548=CARTESIAN_POINT ( 'NONE',  ( -3.636496289402152637, 15.33000000000001073, -11.19198476289190936 ) ) ;
#1550=ORIENTED_EDGE ( 'NONE', *, *, #498, .T. ) ;
#1554=CARTESIAN_POINT ( 'NONE',  ( -2.229658519546948270, -3.026718717157248455E-15, -12.03768796296077248 ) ) ;
#1555=CARTESIAN_POINT ( 'NONE',  ( -10.99999999999979394, 0.000000000000000000, -15.58845726812003996 ) ) ;
#1559=CARTESIAN_POINT ( 'NONE',  ( -10.92172942406179104, -14.76999999999999780, 7.935100905948385908 ) ) ;
#1565=ADVANCED_FACE ( 'NONE', ( #9091, #14444 ), #2980, .F. ) ;
#1568=CARTESIAN_POINT ( 'NONE',  ( 2.222800136090958861E-15, 3.313974596215566670, -12.00000000000000355 ) ) ;
#1569=CARTESIAN_POINT ( 'NONE',  ( 12.00000000000000355, 5.446025403784441998, -3.899036354794874093 ) ) ;
#1572=VECTOR ( 'NONE', #14237, 1000.000000000000000 ) ;
#1575=CARTESIAN_POINT ( 'NONE',  ( -12.00000000000000178, 0.6460254037844337383, -3.899036354794879422 ) ) ;
#1576=FACE_OUTER_BOUND ( 'NONE', #7475, .T. ) ;
#1577=CARTESIAN_POINT ( 'NONE',  ( 8.343458848123583849, 31.87999999999999901, -11.48378591275253768 ) ) ;
#1578=CARTESIAN_POINT ( 'NONE',  ( 3.636496289402154414, -10.16999999999999815, 11.19198476289190758 ) ) ;
#1580=CARTESIAN_POINT ( 'NONE',  ( -8.549982208541774191E-16, -15.32000000000000384, 14.19474002721660355 ) ) ;
#1591=CARTESIAN_POINT ( 'NONE',  ( -2.138189944381236884, 4.256881422320271113, -13.50000000000000000 ) ) ;
#1592=CARTESIAN_POINT ( 'NONE',  ( -2.734444271416374749E-11, 0.3139745962166686777, -12.00000000000000000 ) ) ;
#1602=CARTESIAN_POINT ( 'NONE',  ( -13.50000000000000000, 7.930000000000006821, -3.469446951953614189E-15 ) ) ;
#1607=CARTESIAN_POINT ( 'NONE',  ( 10.92172942406179104, 13.72999999999999154, -7.935100905948385908 ) ) ;
#1613=ADVANCED_FACE ( 'NONE', ( #9827 ), #13677, .F. ) ;
#1616=CARTESIAN_POINT ( 'NONE',  ( -1.363343349470708815E-11, 9.313974596216114676, -12.00000000000000355 ) ) ;
#1622=CARTESIAN_POINT ( 'NONE',  ( -7.999999999999776179, 7.773118517290098062, -17.32050807568887762 ) ) ;
#1623=DIRECTION ( 'NONE',  ( -0.4999999999999986677, 0.000000000000000000, -0.8660254037844394848 ) ) ;
#1624=ORIENTED_EDGE ( 'NONE', *, *, #3286, .F. ) ;
#1626=EDGE_LOOP ( 'NONE', ( #8430, #17034, #13447, #11158, #1445, #7828, #14784, #17343, #6290, #8389, #15047, #5250, #10214, #2496, #10921, #9873, #239 ) ) ;
#1628=EDGE_CURVE ( 'NONE', #1880, #8869, #15379, .T. ) ;
#1630=CARTESIAN_POINT ( 'NONE',  ( 9.832031499013087483, 0.06660297321671654336, 9.434941428760371451 ) ) ;
#1639=CARTESIAN_POINT ( 'NONE',  ( 15.43183772185602898, 8.055054230040790131, -9.319033143235071037 ) ) ;
#1641=AXIS2_PLACEMENT_3D ( 'NONE', #15428, #12801, #849 ) ;
#1642=ORIENTED_EDGE ( 'NONE', *, *, #9399, .F. ) ;
#1648=CARTESIAN_POINT ( 'NONE',  ( -13.49999999999999822, -15.22000000000000064, -4.386415899144240349 ) ) ;
#1653=CARTESIAN_POINT ( 'NONE',  ( -15.50189495701162379, 7.815232006635826956, -10.85006967914028131 ) ) ;
#1662=CARTESIAN_POINT ( 'NONE',  ( 19.00000000000000711, 0.000000000000000000, -1.732050807568807027 ) ) ;
#1663=CYLINDRICAL_SURFACE ( 'NONE', #9125, 1.999999999999998224 ) ;
#1664=CARTESIAN_POINT ( 'NONE',  ( 4.171729424061789260, 30.82999999999999474, 12.83926296998457239 ) ) ;
#1665=CARTESIAN_POINT ( 'NONE',  ( 11.76794919243112680, -3.420000000000002593, -3.823638476888993942 ) ) ;
#1666=EDGE_CURVE ( 'NONE', #14305, #16949, #5815, .T. ) ;
#1668=CARTESIAN_POINT ( 'NONE',  ( -8.343458848123582072, -15.62000000000000099, 11.48378591275254124 ) ) ;
#1681=CARTESIAN_POINT ( 'NONE',  ( 7.272992578804308828, 22.98000000000001108, 10.01041549318726709 ) ) ;
#1686=CARTESIAN_POINT ( 'NONE',  ( -4.171729424061791036, 5.530000000000007354, 12.83926296998457239 ) ) ;
#1687=VERTEX_POINT ( 'NONE', #15172 ) ;
#1688=ADVANCED_FACE ( 'NONE', ( #3072 ), #1751, .T. ) ;
#1692=CARTESIAN_POINT ( 'NONE',  ( 2.621994543952811015E-15, 2.179999999999994831, -14.19474002721660355 ) ) ;
#1693=LINE ( 'NONE', #11253, #4859 ) ;
#1701=CARTESIAN_POINT ( 'NONE',  ( 1.539363535742641842, 7.854661454367251494, -18.71158131929044544 ) ) ;
#1707=AXIS2_PLACEMENT_3D ( 'NONE', #9878, #15401, #13115 ) ;
#1709=CARTESIAN_POINT ( 'NONE',  ( -17.32050807568867512, 7.773118517290098062, -8.000000000000207834 ) ) ;
#1713=VERTEX_POINT ( 'NONE', #1662 ) ;
#1715=CARTESIAN_POINT ( 'NONE',  ( -11.76794919243112325, -14.06999999999999851, -2.602085213965210642E-15 ) ) ;
#1718=CARTESIAN_POINT ( 'NONE',  ( 8.343458848123583849, 0.8799999999999997824, -11.48378591275253768 ) ) ;
#1725=VERTEX_POINT ( 'NONE', #9734 ) ;
#1726=CARTESIAN_POINT ( 'NONE',  ( 15.49921147158543633, 8.062143943920768052, -9.154805866618465515 ) ) ;
#1731=CARTESIAN_POINT ( 'NONE',  ( -15.58845726811999910, 7.773118517290098950, 10.99999999999985256 ) ) ;
#1735=CARTESIAN_POINT ( 'NONE',  ( 10.92172942406178926, -19.86999999999999744, 7.935100905948385908 ) ) ;
#1738=CARTESIAN_POINT ( 'NONE',  ( 11.76794919243112680, -18.42000000000000171, -3.823638476888993942 ) ) ;
#1740=AXIS2_PLACEMENT_3D ( 'NONE', #9483, #6389, #3810 ) ;
#1741=CARTESIAN_POINT ( 'NONE',  ( 0.000000000000000000, 9.000000000000000000, 0.000000000000000000 ) ) ;
#1742=EDGE_CURVE ( 'NONE', #14262, #11444, #8498, .T. ) ;
#1743=CARTESIAN_POINT ( 'NONE',  ( -9.520470885617715595, -5.370000000000000107, -6.917026985038136289 ) ) ;
#1750=CARTESIAN_POINT ( 'NONE',  ( -3.556480217745532916E-14, 9.046025403784437202, -12.00000000000000000 ) ) ;
#1751=CYLINDRICAL_SURFACE ( 'NONE', #6109, 14.50000000000000000 ) ;
#1752=CARTESIAN_POINT ( 'NONE',  ( 8.343458848123580296, 3.979999999999996430, 11.48378591275253768 ) ) ;
#1753=CARTESIAN_POINT ( 'NONE',  ( -13.50000000000000000, 29.93000000000001393, -3.469446951953614189E-15 ) ) ;
#1754=CARTESIAN_POINT ( 'NONE',  ( 11.76794919243112325, -9.720000000000005969, 3.823638476888996163 ) ) ;
#1756=CARTESIAN_POINT ( 'NONE',  ( 12.00000000000000355, 5.713974596215566137, -3.899036354794874093 ) ) ;
#1757=VECTOR ( 'NONE', #6026, 1000.000000000000000 ) ;
#1763=EDGE_CURVE ( 'NONE', #1210, #13044, #4062, .T. ) ;
#1771=CARTESIAN_POINT ( 'NONE',  ( 11.76794919243112325, 20.28000000000000824, 3.823638476888996163 ) ) ;
#1776=CARTESIAN_POINT ( 'NONE',  ( 8.343458848123578520, 5.980000000000005755, 11.48378591275254124 ) ) ;
#1777=ORIENTED_EDGE ( 'NONE', *, *, #8596, .F. ) ;
#1779=CARTESIAN_POINT ( 'NONE',  ( 8.343458848123578520, 3.979999999999996430, 11.48378591275254124 ) ) ;
#1793=CARTESIAN_POINT ( 'NONE',  ( -6.987110303422327640, 10.00000000000000000, 10.35626373279682788 ) ) ;
#1796=VERTEX_POINT ( 'NONE', #1830 ) ;
#1800=CARTESIAN_POINT ( 'NONE',  ( -8.457499700851188962, 8.027799080943070820, 16.03540712409199642 ) ) ;
#1808=ORIENTED_EDGE ( 'NONE', *, *, #10473, .F. ) ;
#1809=CARTESIAN_POINT ( 'NONE',  ( 16.47733079524782340, 7.956441929884684683, -8.178053476330095606 ) ) ;
#1813=DIRECTION ( 'NONE',  ( -0.000000000000000000, -1.000000000000000000, -0.000000000000000000 ) ) ;
#1816=CARTESIAN_POINT ( 'NONE',  ( 3.636496289402157078, 27.02999999999999758, -11.19198476289190936 ) ) ;
#1821=CARTESIAN_POINT ( 'NONE',  ( -8.891200544363830713E-16, 8.679999999999999716, 13.49999999999999822 ) ) ;
#1822=CARTESIAN_POINT ( 'NONE',  ( -9.520470885617715595, -2.369999999999996998, -6.917026985038136289 ) ) ;
#1830=CARTESIAN_POINT ( 'NONE',  ( -5.441113646577473872, 0.000000000000000000, -25.42428528562855305 ) ) ;
#1831=CARTESIAN_POINT ( 'NONE',  ( -10.92172942406179104, 3.230000000000010640, 7.935100905948385908 ) ) ;
#1832=CARTESIAN_POINT ( 'NONE',  ( 10.92172942406179104, 28.73000000000000398, -7.935100905948385908 ) ) ;
#1833=CARTESIAN_POINT ( 'NONE',  ( 7.272992578804308828, -4.019999999999998685, 10.01041549318726709 ) ) ;
#1837=CARTESIAN_POINT ( 'NONE',  ( 3.708203932499371192, 6.163974596215569868, -11.41267819554184548 ) ) ;
#1839=CARTESIAN_POINT ( 'NONE',  ( -17.32050807568867512, 7.773118517290098062, -8.000000000000207834 ) ) ;
#1840=EDGE_CURVE ( 'NONE', #3933, #9499, #5487, .T. ) ;
#1842=( NAMED_UNIT ( * ) SI_UNIT ( $, .STERADIAN. ) SOLID_ANGLE_UNIT ( ) );
#1848=CARTESIAN_POINT ( 'NONE',  ( 25.42428528562856727, 5.918584287042170544, -5.441113646577394825 ) ) ;
#1851=LINE ( 'NONE', #16705, #8572 ) ;
#1853=CARTESIAN_POINT ( 'NONE',  ( 3.636496289402154414, 25.83000000000001961, 11.19198476289190758 ) ) ;
#1854=ORIENTED_EDGE ( 'NONE', *, *, #7375, .T. ) ;
#1858=ORIENTED_EDGE ( 'NONE', *, *, #1666, .F. ) ;
#1862=CARTESIAN_POINT ( 'NONE',  ( -10.92172942406179104, 3.230000000000010640, 7.935100905948385908 ) ) ;
#1873=VECTOR ( 'NONE', #7755, 1000.000000000000000 ) ;
#1876=CARTESIAN_POINT ( 'NONE',  ( 2.096029675345698173, 10.00000000000000178, 12.94816314436808469 ) ) ;
#1880=VERTEX_POINT ( 'NONE', #13487 ) ;
#1881=CARTESIAN_POINT ( 'NONE',  ( 4.171729424061789260, 32.82999999999999829, 12.83926296998457239 ) ) ;
#1883=ADVANCED_FACE ( 'NONE', ( #6789 ), #16399, .F. ) ;
#1895=ORIENTED_EDGE ( 'NONE', *, *, #10755, .F. ) ;
#1901=EDGE_CURVE ( 'NONE', #13655, #5466, #6883, .T. ) ;
#1904=CARTESIAN_POINT ( 'NONE',  ( -7.272992578804307939, 33.47999999999999687, -10.01041549318726886 ) ) ;
#1908=CARTESIAN_POINT ( 'NONE',  ( -9.520470885617715595, -14.37000000000000099, -6.917026985038136289 ) ) ;
#1910=CYLINDRICAL_SURFACE ( 'NONE', #7871, 1.999999999999998224 ) ;
#1911=CARTESIAN_POINT ( 'NONE',  ( 2.279995255611139653E-15, -5.820000000000007390, -12.37355403259654985 ) ) ;
#1917=CARTESIAN_POINT ( 'NONE',  ( -17.42428528562871293, 0.000000000000000000, 19.29752010712834220 ) ) ;
#1919=CARTESIAN_POINT ( 'NONE',  ( 4.171729424061791924, 29.03000000000000114, -12.83926296998457239 ) ) ;
#1920=CARTESIAN_POINT ( 'NONE',  ( -11.76794919243112325, -11.22000000000000242, -3.823638476888998827 ) ) ;
#1922=CARTESIAN_POINT ( 'NONE',  ( -13.14483242576228506, 7.170662809914417402, 16.82677684650020211 ) ) ;
#1923=EDGE_CURVE ( 'NONE', #16171, #1419, #14105, .T. ) ;
#1937=CARTESIAN_POINT ( 'NONE',  ( 9.520470885617717371, 20.72999999999999687, -6.917026985038131848 ) ) ;
#1942=CARTESIAN_POINT ( 'NONE',  ( 8.343458848123578520, 2.979999999999998650, 11.48378591275254124 ) ) ;
#1950=AXIS2_PLACEMENT_3D ( 'NONE', #2650, #9585, #14676 ) ;
#1965=CARTESIAN_POINT ( 'NONE',  ( -13.49999999999999822, 31.78000000000000469, -4.386415899144240349 ) ) ;
#1970=CARTESIAN_POINT ( 'NONE',  ( 10.15710352110371240, -3.110307960253506586E-15, -6.885784913371308491 ) ) ;
#1972=EDGE_CURVE ( 'NONE', #10231, #6836, #1017, .T. ) ;
#1973=CARTESIAN_POINT ( 'NONE',  ( -15.58845726811999910, 7.773118517290098950, 10.99999999999985256 ) ) ;
#1978=ORIENTED_EDGE ( 'NONE', *, *, #1049, .F. ) ;
#1979=LINE ( 'NONE', #4570, #6376 ) ;
#1983=CARTESIAN_POINT ( 'NONE',  ( 16.97734196418687702, 7.854010772509913529, 8.022095340454528767 ) ) ;
#1984=DIRECTION ( 'NONE',  ( 0.000000000000000000, 0.000000000000000000, 1.000000000000000000 ) ) ;
#1987=CARTESIAN_POINT ( 'NONE',  ( 9.520470885617717371, 26.73000000000000398, -6.917026985038131848 ) ) ;
#1991=CARTESIAN_POINT ( 'NONE',  ( 11.76794919243112680, -15.41999999999999993, -3.823638476888993942 ) ) ;
#1994=CARTESIAN_POINT ( 'NONE',  ( -11.76794919243112325, 0.7799999999999955858, -3.823638476888998827 ) ) ;
#1997=ADVANCED_FACE ( 'NONE', ( #12697 ), #7223, .T. ) ;
#2002=CARTESIAN_POINT ( 'NONE',  ( 11.00000000000001599, 7.773118517290098062, -15.58845726811988364 ) ) ;
#2004=CARTESIAN_POINT ( 'NONE',  ( 13.49999999999999822, 25.28000000000000824, 4.386415899144237684 ) ) ;
#2006=CARTESIAN_POINT ( 'NONE',  ( 7.416407864998736166, 5.113974596215570045, 10.20780970022447853 ) ) ;
#2010=DIRECTION ( 'NONE',  ( 0.000000000000000000, -1.000000000000000000, 0.000000000000000000 ) ) ;
#2017=DIRECTION ( 'NONE',  ( 0.000000000000000000, 0.000000000000000000, -1.000000000000000000 ) ) ;
#2019=VECTOR ( 'NONE', #7571, 1000.000000000000000 ) ;
#2024=CARTESIAN_POINT ( 'NONE',  ( -9.520470885617715595, 21.63000000000000966, -6.917026985038136289 ) ) ;
#2029=CARTESIAN_POINT ( 'NONE',  ( 2.621994543952811015E-15, 1.180000000000004601, -14.19474002721660355 ) ) ;
#2030=CARTESIAN_POINT ( 'NONE',  ( 7.272992578804308828, 31.98000000000000043, 10.01041549318726709 ) ) ;
#2031=CARTESIAN_POINT ( 'NONE',  ( -8.000000000000143885, 7.773118517290097174, 17.32050807568870709 ) ) ;
#2036=CARTESIAN_POINT ( 'NONE',  ( 8.343458848123583849, 7.880000000000003446, -11.48378591275253768 ) ) ;
#2048=EDGE_LOOP ( 'NONE', ( #10560, #17210, #15194, #3651, #15479 ) ) ;
#2050=VERTEX_POINT ( 'NONE', #14002 ) ;
#2052=ORIENTED_EDGE ( 'NONE', *, *, #12150, .T. ) ;
#2053=CARTESIAN_POINT ( 'NONE',  ( 9.520470885617717371, -18.27000000000000313, -6.917026985038131848 ) ) ;
#2057=EDGE_CURVE ( 'NONE', #3274, #106, #1979, .T. ) ;
#2060=CARTESIAN_POINT ( 'NONE',  ( 10.59082145838073075, -1.242015572811692772E-15, 8.046083559367682270 ) ) ;
#2063=CARTESIAN_POINT ( 'NONE',  ( 11.76794919243112680, 14.57999999999999474, -3.823638476888993942 ) ) ;
#2064=ORIENTED_EDGE ( 'NONE', *, *, #15044, .F. ) ;
#2065=LINE ( 'NONE', #7666, #1873 ) ;
#2070=FACE_OUTER_BOUND ( 'NONE', #2391, .T. ) ;
#2071=CARTESIAN_POINT ( 'NONE',  ( 17.32050807568878170, 7.773118517290099838, -7.999999999999961808 ) ) ;
#2072=CYLINDRICAL_SURFACE ( 'NONE', #9913, 1.999999999999998224 ) ;
#2074=CARTESIAN_POINT ( 'NONE',  ( -7.272992578804310604, 31.38000000000002032, 10.01041549318726709 ) ) ;
#2078=CARTESIAN_POINT ( 'NONE',  ( 18.18340077413957090, 8.007813497946154158, 0.8546369493909243831 ) ) ;
#2084=CYLINDRICAL_SURFACE ( 'NONE', #12693, 12.00000000000000178 ) ;
#2085=CARTESIAN_POINT ( 'NONE',  ( 8.099236140987171595, 7.915750619362869500, -16.68483048229433763 ) ) ;
#2086=ORIENTED_EDGE ( 'NONE', *, *, #16024, .F. ) ;
#2087=FACE_OUTER_BOUND ( 'NONE', #4655, .T. ) ;
#2093=CARTESIAN_POINT ( 'NONE',  ( -18.99999999999998224, 0.000000000000000000, -1.732050807569074369 ) ) ;
#2100=CARTESIAN_POINT ( 'NONE',  ( 2.222800136090958073E-15, 3.046025403784441643, -12.00000000000000000 ) ) ;
#2105=CARTESIAN_POINT ( 'NONE',  ( -3.636496289402156190, 16.53000000000001535, 11.19198476289190758 ) ) ;
#2110=CARTESIAN_POINT ( 'NONE',  ( -4.171729424061787483, -1.669999999999997931, -12.83926296998457417 ) ) ;
#2113=EDGE_CURVE ( 'NONE', #4811, #9433, #3784, .T. ) ;
#2117=AXIS2_PLACEMENT_3D ( 'NONE', #6969, #60, #5464 ) ;
#2121=DIRECTION ( 'NONE',  ( -0.5000000000000005551, 0.000000000000000000, 0.8660254037844382635 ) ) ;
#2125=DIRECTION ( 'NONE',  ( 0.000000000000000000, 0.000000000000000000, 1.000000000000000000 ) ) ;
#2127=DIRECTION ( 'NONE',  ( 0.000000000000000000, 1.000000000000000000, 0.000000000000000000 ) ) ;
#2129=ORIENTED_EDGE ( 'NONE', *, *, #8131, .F. ) ;
#2131=VECTOR ( 'NONE', #10887, 1000.000000000000000 ) ;
#2134=CARTESIAN_POINT ( 'NONE',  ( -10.92172942406178926, 34.62999999999999545, -7.935100905948389460 ) ) ;
#2152=DIRECTION ( 'NONE',  ( 0.000000000000000000, 0.000000000000000000, -1.000000000000000000 ) ) ;
#2156=CARTESIAN_POINT ( 'NONE',  ( 0.000000000000000000, 0.000000000000000000, 0.000000000000000000 ) ) ;
#2163=DIRECTION ( 'NONE',  ( -0.000000000000000000, 1.000000000000000000, -0.000000000000000000 ) ) ;
#2170=CARTESIAN_POINT ( 'NONE',  ( 12.00000000000000178, 8.296025403784431873, 1.734723475976807094E-15 ) ) ;
#2171=CARTESIAN_POINT ( 'NONE',  ( 9.352804080103156892, 8.052183443614390868, -15.42355852573366448 ) ) ;
#2172=CARTESIAN_POINT ( 'NONE',  ( 2.621994543952811015E-15, 26.18000000000001037, -14.19474002721660355 ) ) ;
#2174=CARTESIAN_POINT ( 'NONE',  ( -2.138190073780635636, 9.603118573027019877, 13.49999995795558760 ) ) ;
#2179=CARTESIAN_POINT ( 'NONE',  ( 10.92172942406178926, -1.869999999999996554, 7.935100905948385908 ) ) ;
#2187=EDGE_CURVE ( 'NONE', #13170, #1168, #11343, .T. ) ;
#2193=CARTESIAN_POINT ( 'NONE',  ( -11.76794919243112325, 12.78000000000000824, -3.823638476888998827 ) ) ;
#2197=DIRECTION ( 'NONE',  ( -0.000000000000000000, -1.000000000000000000, -0.000000000000000000 ) ) ;
#2198=CARTESIAN_POINT ( 'NONE',  ( 4.171729424061789260, -0.1700000000000034817, 12.83926296998457239 ) ) ;
#2209=CARTESIAN_POINT ( 'NONE',  ( 0.000000000000000000, 9.000000000000000000, 0.000000000000000000 ) ) ;
#2212=EDGE_CURVE ( 'NONE', #6426, #3760, #8836, .T. ) ;
#2217=ORIENTED_EDGE ( 'NONE', *, *, #4456, .F. ) ;
#2219=CARTESIAN_POINT ( 'NONE',  ( 2.279995255611139653E-15, 6.179999999999999716, -12.37355403259654985 ) ) ;
#2220=VERTEX_POINT ( 'NONE', #4969 ) ;
#2222=CARTESIAN_POINT ( 'NONE',  ( -8.343458848123576743, 31.48000000000000398, -11.48378591275254301 ) ) ;
#2228=CARTESIAN_POINT ( 'NONE',  ( 12.74897295140808140, 2.734769208434736086E-15, -0.2137157648261680254 ) ) ;
#2229=CARTESIAN_POINT ( 'NONE',  ( 4.206197538246464696, 6.548267719634618622, -23.28534784291399973 ) ) ;
#2236=EDGE_LOOP ( 'NONE', ( #1144, #7992, #14842, #6317 ) ) ;
#2237=FACE_OUTER_BOUND ( 'NONE', #11787, .T. ) ;
#2238=ORIENTED_EDGE ( 'NONE', *, *, #11600, .T. ) ;
#2239=CARTESIAN_POINT ( 'NONE',  ( 4.171729424061791924, 16.03000000000001535, -12.83926296998457239 ) ) ;
#2244=CARTESIAN_POINT ( 'NONE',  ( -13.50000000000000000, 5.930000000000005045, -3.469446951953614189E-15 ) ) ;
#2248=CARTESIAN_POINT ( 'NONE',  ( 17.32050807568873552, 7.773118517290098062, 8.000000000000083489 ) ) ;
#2255=DIRECTION ( 'NONE',  ( -1.000000000000000000, -0.000000000000000000, -2.806191565803427284E-15 ) ) ;
#2257=CARTESIAN_POINT ( 'NONE',  ( -4.171729424061791036, 24.52999999999999758, 12.83926296998457239 ) ) ;
#2258=VERTEX_POINT ( 'NONE', #2375 ) ;
#2260=CARTESIAN_POINT ( 'NONE',  ( 1.775737858763662015E-15, 9.000000000000000000, 14.50000000000000000 ) ) ;
#2264=CARTESIAN_POINT ( 'NONE',  ( 4.171729424061791924, -0.9699999999999986411, -12.83926296998457239 ) ) ;
#2279=CARTESIAN_POINT ( 'NONE',  ( -11.76794919243112325, 9.780000000000002913, -3.823638476888998827 ) ) ;
#2280=ORIENTED_EDGE ( 'NONE', *, *, #11024, .T. ) ;
#2287=EDGE_CURVE ( 'NONE', #5098, #6231, #2807, .T. ) ;
#2293=VECTOR ( 'NONE', #9477, 1000.000000000000000 ) ;
#2304=CARTESIAN_POINT ( 'NONE',  ( 3.636496289402157078, 9.030000000000010019, -11.19198476289190936 ) ) ;
#2308=CARTESIAN_POINT ( 'NONE',  ( -10.92172942406179104, 26.23000000000000398, 7.935100905948385908 ) ) ;
#2311=AXIS2_PLACEMENT_3D ( 'NONE', #2914, #13700, #13872 ) ;
#2315=CARTESIAN_POINT ( 'NONE',  ( 12.71634493074430594, -4.622062490413149683E-15, 2.191283809529018356 ) ) ;
#2317=CARTESIAN_POINT ( 'NONE',  ( 2.970370385949292036, 7.170662809914417402, -21.14483242576214650 ) ) ;
#2321=VECTOR ( 'NONE', #780, 1000.000000000000000 ) ;
#2325=VERTEX_POINT ( 'NONE', #17241 ) ;
#2326=VERTEX_POINT ( 'NONE', #13349 ) ;
#2328=VERTEX_POINT ( 'NONE', #9048 ) ;
#2331=CARTESIAN_POINT ( 'NONE',  ( -17.32050807568867512, 0.000000000000000000, -8.000000000000207834 ) ) ;
#2332=CARTESIAN_POINT ( 'NONE',  ( -19.29752010712865129, 5.918584287042170544, 17.42428528562837542 ) ) ;
#2341=CARTESIAN_POINT ( 'NONE',  ( -7.272992578804307939, 18.48000000000000398, -10.01041549318726886 ) ) ;
#2344=CARTESIAN_POINT ( 'NONE',  ( 10.68680102524458242, 7.855179386613375669, -15.43414541437280185 ) ) ;
#2346=CARTESIAN_POINT ( 'NONE',  ( 8.343458848123583849, 19.87999999999999901, -11.48378591275253768 ) ) ;
#2347=ORIENTED_EDGE ( 'NONE', *, *, #3035, .T. ) ;
#2353=CARTESIAN_POINT ( 'NONE',  ( -4.171729424061787483, -6.669999999999995488, -12.83926296998457417 ) ) ;
#2361=CARTESIAN_POINT ( 'NONE',  ( 1.900613283894437622, 2.969143981464173798, -12.00000000000000000 ) ) ;
#2366=CARTESIAN_POINT ( 'NONE',  ( -7.409984580736203970E-16, 10.68000000000000149, 12.37355403259654985 ) ) ;
#2375=CARTESIAN_POINT ( 'NONE',  ( 2.222800136090958861E-15, 3.313974596215566670, -12.00000000000000355 ) ) ;
#2383=CARTESIAN_POINT ( 'NONE',  ( 18.99999999999999289, 7.773118517290098062, 1.732050807568941586 ) ) ;
#2390=CARTESIAN_POINT ( 'NONE',  ( -9.520470885617715595, 3.629999999999994564, -6.917026985038136289 ) ) ;
#2391=EDGE_LOOP ( 'NONE', ( #13742, #12043, #3122, #7756 ) ) ;
#2393=CARTESIAN_POINT ( 'NONE',  ( 4.171729424061791924, 22.02999999999999403, -12.83926296998457239 ) ) ;
#2395=VECTOR ( 'NONE', #8790, 1000.000000000000227 ) ;
#2399=CARTESIAN_POINT ( 'NONE',  ( 8.343458848123580296, 0.9799999999999967626, 11.48378591275253768 ) ) ;
#2400=CARTESIAN_POINT ( 'NONE',  ( -1.732050807569007977, 7.773118517290099838, 18.99999999999998224 ) ) ;
#2401=CARTESIAN_POINT ( 'NONE',  ( 4.988803385412796665, 9.999999999999996447, -12.54439479535357371 ) ) ;
#2404=DIRECTION ( 'NONE',  ( 0.000000000000000000, -1.000000000000000000, 0.000000000000000000 ) ) ;
#2406=ORIENTED_EDGE ( 'NONE', *, *, #10160, .T. ) ;
#2408=ORIENTED_EDGE ( 'NONE', *, *, #9356, .F. ) ;
#2410=ORIENTED_EDGE ( 'NONE', *, *, #10270, .T. ) ;
#2411=CARTESIAN_POINT ( 'NONE',  ( 13.50000000000000000, 12.42999999999999616, 1.734723475976807094E-15 ) ) ;
#2422=CARTESIAN_POINT ( 'NONE',  ( 9.520470885617715595, 20.13000000000000966, 6.917026985038135400 ) ) ;
#2429=CARTESIAN_POINT ( 'NONE',  ( 13.49999999999999822, 22.28000000000000469, 4.386415899144237684 ) ) ;
#2431=CARTESIAN_POINT ( 'NONE',  ( -4.171729424061787483, 8.330000000000003624, -12.83926296998457417 ) ) ;
#2432=CARTESIAN_POINT ( 'NONE',  ( -11.76794919243112325, 33.78000000000000824, -3.823638476888998827 ) ) ;
#2446=ADVANCED_FACE ( 'NONE', ( #10542 ), #15904, .F. ) ;
#2451=CARTESIAN_POINT ( 'NONE',  ( -11.76794919243112325, 7.080000000000000959, 3.823638476888994386 ) ) ;
#2455=DIRECTION ( 'NONE',  ( 0.000000000000000000, 0.000000000000000000, 1.000000000000000000 ) ) ;
#2456=CARTESIAN_POINT ( 'NONE',  ( 13.50000000000000355, -8.420000000000003482, -4.386415899144233244 ) ) ;
#2458=FACE_OUTER_BOUND ( 'NONE', #12783, .T. ) ;
#2466=CARTESIAN_POINT ( 'NONE',  ( -15.58845726811999910, 0.000000000000000000, 10.99999999999985256 ) ) ;
#2472=VERTEX_POINT ( 'NONE', #9226 ) ;
#2475=CARTESIAN_POINT ( 'NONE',  ( -3.636496289402156190, 1.530000000000003579, 11.19198476289190758 ) ) ;
#2476=ORIENTED_EDGE ( 'NONE', *, *, #14586, .F. ) ;
#2478=CARTESIAN_POINT ( 'NONE',  ( -8.549982208541774191E-16, 20.68000000000001037, 14.19474002721660355 ) ) ;
#2486=CIRCLE ( 'NONE', #12391, 1.999999999999998224 ) ;
#2492=FACE_OUTER_BOUND ( 'NONE', #6519, .T. ) ;
#2495=ORIENTED_EDGE ( 'NONE', *, *, #5631, .F. ) ;
#2496=ORIENTED_EDGE ( 'NONE', *, *, #12815, .F. ) ;
#2499=CARTESIAN_POINT ( 'NONE',  ( -3.636496289402152637, -11.66999999999999993, -11.19198476289190936 ) ) ;
#2507=EDGE_CURVE ( 'NONE', #16109, #6836, #11947, .T. ) ;
#2512=CARTESIAN_POINT ( 'NONE',  ( 9.520470885617715595, 17.13000000000000611, 6.917026985038135400 ) ) ;
#2516=CARTESIAN_POINT ( 'NONE',  ( 4.171729424061791924, 20.02999999999999403, -12.83926296998457239 ) ) ;
#2517=ORIENTED_EDGE ( 'NONE', *, *, #2212, .F. ) ;
#2519=CARTESIAN_POINT ( 'NONE',  ( -15.58845726811976817, 0.000000000000000000, -11.00000000000018296 ) ) ;
#2520=CARTESIAN_POINT ( 'NONE',  ( -11.76794919243112325, 28.08000000000000540, 3.823638476888994386 ) ) ;
#2523=CARTESIAN_POINT ( 'NONE',  ( -11.76794919243112325, -8.220000000000004192, -3.823638476888998827 ) ) ;
#2525=CARTESIAN_POINT ( 'NONE',  ( -13.49999999999999822, -8.920000000000001705, 4.386415899144235908 ) ) ;
#2530=EDGE_CURVE ( 'NONE', #3828, #4826, #7231, .T. ) ;
#2535=CARTESIAN_POINT ( 'NONE',  ( 12.00000000000000178, 2.296025403784453189, 1.734723475976807094E-15 ) ) ;
#2538=CARTESIAN_POINT ( 'NONE',  ( -7.409984580736203970E-16, 10.68000000000000149, 12.37355403259654985 ) ) ;
#2541=CARTESIAN_POINT ( 'NONE',  ( -11.76794919243112325, 6.930000000000005933, -2.602085213965210642E-15 ) ) ;
#2545=CARTESIAN_POINT ( 'NONE',  ( 13.50000000000000355, -11.42000000000000526, -4.386415899144233244 ) ) ;
#2550=DIRECTION ( 'NONE',  ( -1.000000000000000000, 0.000000000000000000, -2.806191565803427284E-15 ) ) ;
#2555=CARTESIAN_POINT ( 'NONE',  ( -19.79695994079635213, 7.170708369609773314, 7.999999999999814371 ) ) ;
#2562=VERTEX_POINT ( 'NONE', #2260 ) ;
#2565=VERTEX_POINT ( 'NONE', #15440 ) ;
#2566=ORIENTED_EDGE ( 'NONE', *, *, #13461, .F. ) ;
#2567=CARTESIAN_POINT ( 'NONE',  ( 8.343458848123583849, 18.88000000000000256, -11.48378591275253768 ) ) ;
#2570=CARTESIAN_POINT ( 'NONE',  ( -13.49999999999999822, 15.07999999999999297, 4.386415899144235908 ) ) ;
#2578=CARTESIAN_POINT ( 'NONE',  ( -4.448365178832009548, 10.00000000000000888, -12.11652676267665463 ) ) ;
#2587=VECTOR ( 'NONE', #6830, 1000.000000000000000 ) ;
#2591=CARTESIAN_POINT ( 'NONE',  ( 8.458421099448676372, 8.027996319639555622, 16.03410433562983428 ) ) ;
#2594=( BOUNDED_CURVE ( )  B_SPLINE_CURVE ( 2, ( #15576, #14255, #5177, #17001, #3750, #10307, #7569, #14340, #9075, #2399, #13207, #8984, #17265 ),
 .UNSPECIFIED., .F., .F. ) 
 B_SPLINE_CURVE_WITH_KNOTS ( ( 3, 2, 2, 2, 2, 2, 3 ),
 ( 0.5801927019965731347, 0.5830229102989955559, 0.5886833269038401761, 0.5943437435086847964, 0.6000041601135294167, 0.6056645767183740370, 0.6084947812034886550 ),
 .UNSPECIFIED. ) 
 CURVE ( )  GEOMETRIC_REPRESENTATION_ITEM ( )  RATIONAL_B_SPLINE_CURVE ( ( 0.9755282581475767101, 0.9755282581475757109, 1.000000000000000000, 0.9510565162951535312, 1.000000000000000000, 0.9510565162951535312, 1.000000000000000000, 0.9510565162951535312, 1.000000000000000000, 0.9510565162951535312, 1.000000000000000000, 0.9755282911543938784, 0.9755282581476212300 ) ) 
 REPRESENTATION_ITEM ( '' )  );
#2599=CARTESIAN_POINT ( 'NONE',  ( 11.76794919243112325, 17.28000000000001535, 3.823638476888996163 ) ) ;
#2603=VERTEX_POINT ( 'NONE', #17036 ) ;
#2607=CARTESIAN_POINT ( 'NONE',  ( 11.76794919243112325, -9.720000000000005969, 3.823638476888996163 ) ) ;
#2609=CARTESIAN_POINT ( 'NONE',  ( -13.49999999999999822, -9.220000000000002416, -4.386415899144240349 ) ) ;
#2622=CARTESIAN_POINT ( 'NONE',  ( 7.272992578804311492, 11.88000000000000966, -10.01041549318726709 ) ) ;
#2624=CARTESIAN_POINT ( 'NONE',  ( -4.171729424061791036, 8.530000000000010019, 12.83926296998457239 ) ) ;
#2625=CARTESIAN_POINT ( 'NONE',  ( -11.76794919243112325, 6.779999999999995808, -3.823638476888998827 ) ) ;
#2630=CARTESIAN_POINT ( 'NONE',  ( 8.343458848123583849, -8.119999999999999218, -11.48378591275253768 ) ) ;
#2631=EDGE_CURVE ( 'NONE', #11029, #1687, #13403, .T. ) ;
#2635=CARTESIAN_POINT ( 'NONE',  ( -1.732050807569007977, 0.000000000000000000, 18.99999999999998224 ) ) ;
#2639=DIRECTION ( 'NONE',  ( -0.000000000000000000, -1.000000000000000000, -0.000000000000000000 ) ) ;
#2641=CARTESIAN_POINT ( 'NONE',  ( 1.108954987895778950E-11, 4.813974596216015200, 12.00000000000000178 ) ) ;
#2645=B_SPLINE_CURVE_WITH_KNOTS ( 'NONE', 3,
 ( #6921, #7091, #9750, #14836 ),
 .UNSPECIFIED., .F., .F.,
 ( 4, 4 ),
 ( 2.376698214958262694E-07, 0.007646667280170311651 ),
 .UNSPECIFIED. ) ;
#2648=ORIENTED_EDGE ( 'NONE', *, *, #1385, .F. ) ;
#2650=CARTESIAN_POINT ( 'NONE',  ( 0.000000000000000000, 5.918584287042170544, 0.000000000000000000 ) ) ;
#2653=VECTOR ( 'NONE', #3372, 1000.000000000000000 ) ;
#2654=ORIENTED_EDGE ( 'NONE', *, *, #8764, .F. ) ;
#2655=CARTESIAN_POINT ( 'NONE',  ( -4.171729424061787483, 22.33000000000001606, -12.83926296998457417 ) ) ;
#2658=CARTESIAN_POINT ( 'NONE',  ( -8.343458848123582072, 9.379999999999999005, 11.48378591275254124 ) ) ;
#2674=VERTEX_POINT ( 'NONE', #16046 ) ;
#2681=CIRCLE ( 'NONE', #4967, 26.00000000000000355 ) ;
#2682=B_SPLINE_CURVE_WITH_KNOTS ( 'NONE', 3,
 ( #14801, #8214, #12001, #2693, #13660, #1554, #3953, #9366, #14716, #13402, #16127, #4038, #13490, #14890, #1378, #9452, #6793, #12173, #8304, #16217, #13576, #64, #5467, #11031, #9630, #12259, #154, #5560 ),
 .UNSPECIFIED., .F., .F.,
 ( 4, 2, 2, 2, 2, 2, 2, 2, 2, 2, 2, 2, 2, 4 ),
 ( 0.003365197809828101606, 0.004806483441736369121, 0.006247769073644636635, 0.007689054705552904150, 0.009130340337461170797, 0.01201291160127770236, 0.01489548286509423738, 0.01633676849700250316, 0.01777805412891076894, 0.01921933976081903125, 0.02066062539272729703, 0.02354319665654382859, 0.02498448228845209437, 0.02642576792036036015 ),
 .UNSPECIFIED. ) ;
#2687=CARTESIAN_POINT ( 'NONE',  ( -9.520470885617715595, 15.63000000000000433, -6.917026985038136289 ) ) ;
#2691=CARTESIAN_POINT ( 'NONE',  ( 8.343458848123578520, 21.98000000000001108, 11.48378591275254124 ) ) ;
#2693=CARTESIAN_POINT ( 'NONE',  ( -0.7905400041755126228, 1.593905776373958320E-15, -12.11837741667673285 ) ) ;
#2697=CARTESIAN_POINT ( 'NONE',  ( 3.636496289402154414, -13.17000000000000171, 11.19198476289190758 ) ) ;
#2698=CARTESIAN_POINT ( 'NONE',  ( 23.28534784291398552, 6.548267719634617734, 4.206197538246546408 ) ) ;
#2699=CARTESIAN_POINT ( 'NONE',  ( -13.49999999999999822, -14.92000000000000171, 4.386415899144235908 ) ) ;
#2712=CARTESIAN_POINT ( 'NONE',  ( 2.279995255611139653E-15, 12.17999999999999972, -12.37355403259654985 ) ) ;
#2715=CARTESIAN_POINT ( 'NONE',  ( 3.636496289402154414, -1.170000000000004370, 11.19198476289190758 ) ) ;
#2719=CARTESIAN_POINT ( 'NONE',  ( -4.171729424061791036, -12.46999999999999531, 12.83926296998457239 ) ) ;
#2721=DIRECTION ( 'NONE',  ( 0.000000000000000000, 0.000000000000000000, 1.000000000000000000 ) ) ;
#2728=CARTESIAN_POINT ( 'NONE',  ( -9.708203932499369415, 9.496025403784438268, -7.053423027509682086 ) ) ;
#2736=ORIENTED_EDGE ( 'NONE', *, *, #9055, .T. ) ;
#2739=CARTESIAN_POINT ( 'NONE',  ( 13.50000000000000355, 15.57999999999999119, -4.386415899144233244 ) ) ;
#2744=CARTESIAN_POINT ( 'NONE',  ( -10.92172942406178926, 11.63000000000000078, -7.935100905948389460 ) ) ;
#2751=CARTESIAN_POINT ( 'NONE',  ( -17.42428528562830436, 0.000000000000000000, -19.29752010712870813 ) ) ;
#2752=ADVANCED_FACE ( 'NONE', ( #6814 ), #12021, .F. ) ;
#2754=CARTESIAN_POINT ( 'NONE',  ( -11.88920123096388792, 9.999999999999994671, -1.626927807140451154 ) ) ;
#2756=CARTESIAN_POINT ( 'NONE',  ( 0.000000000000000000, 0.000000000000000000, 0.000000000000000000 ) ) ;
#2759=CARTESIAN_POINT ( 'NONE',  ( -8.000000000000145661, 0.000000000000000000, 17.32050807568870709 ) ) ;
#2762=ORIENTED_EDGE ( 'NONE', *, *, #8980, .T. ) ;
#2765=CARTESIAN_POINT ( 'NONE',  ( 10.99999999999990941, 7.773118517290098062, 15.58845726811995824 ) ) ;
#2766=AXIS2_PLACEMENT_3D ( 'NONE', #14543, #8930, #10426 ) ;
#2770=EDGE_CURVE ( 'NONE', #860, #14305, #14259, .T. ) ;
#2771=AXIS2_PLACEMENT_3D ( 'NONE', #589, #12876, #5999 ) ;
#2776=CIRCLE ( 'NONE', #17458, 26.00000000000000355 ) ;
#2787=CARTESIAN_POINT ( 'NONE',  ( 7.272992578804308828, -10.02000000000000490, 10.01041549318726709 ) ) ;
#2789=CARTESIAN_POINT ( 'NONE',  ( -13.49999999999999822, -12.22000000000000774, -4.386415899144240349 ) ) ;
#2802=CARTESIAN_POINT ( 'NONE',  ( -7.779800476318354832E-16, 7.813974596215564006, 12.00000000000000355 ) ) ;
#2804=CARTESIAN_POINT ( 'NONE',  ( -3.636496289402156190, -1.469999999999999085, 11.19198476289190758 ) ) ;
#2807=( BOUNDED_CURVE ( )  B_SPLINE_CURVE ( 2, ( #15726, #10285, #9140, #7631, #980, #3634, #14488 ),
 .UNSPECIFIED., .F., .F. ) 
 B_SPLINE_CURVE_WITH_KNOTS ( ( 3, 2, 2, 3 ),
 ( 2.168404344971008868E-19, 0.005875474857718830310, 0.01338919962976012172, 0.01714606201576732852 ),
 .UNSPECIFIED. ) 
 CURVE ( )  GEOMETRIC_REPRESENTATION_ITEM ( )  RATIONAL_B_SPLINE_CURVE ( ( 0.9833107263962475031, 0.9617278757631589903, 1.000000000000000000, 0.9510565162951535312, 1.000000000000000000, 0.9755282581476645287, 0.9755282581475768211 ) ) 
 REPRESENTATION_ITEM ( '' )  );
#2808=CARTESIAN_POINT ( 'NONE',  ( -8.549982208541774191E-16, -12.32000000000000384, 14.19474002721660355 ) ) ;
#2811=EDGE_CURVE ( 'NONE', #6836, #1275, #6454, .T. ) ;
#2815=VECTOR ( 'NONE', #4710, 1000.000000000000000 ) ;
#2818=CARTESIAN_POINT ( 'NONE',  ( 0.000000000000000000, 9.999999999999998224, -14.50000000000000000 ) ) ;
#2826=CARTESIAN_POINT ( 'NONE',  ( -9.708203932499369415, 3.496025403784432051, -7.053423027509682086 ) ) ;
#2827=CARTESIAN_POINT ( 'NONE',  ( -19.29752010712864418, 0.000000000000000000, 17.42428528562836831 ) ) ;
#2828=CARTESIAN_POINT ( 'NONE',  ( -13.49999999999999822, 11.08000000000000540, 4.386415899144235908 ) ) ;
#2829=ORIENTED_EDGE ( 'NONE', *, *, #12929, .T. ) ;
#2833=CARTESIAN_POINT ( 'NONE',  ( 4.171729424061789260, 12.83000000000000895, 12.83926296998457239 ) ) ;
#2847=DIRECTION ( 'NONE',  ( -0.000000000000000000, 1.000000000000000000, -0.000000000000000000 ) ) ;
#2848=CARTESIAN_POINT ( 'NONE',  ( 19.00000000000000711, 0.000000000000000000, -1.732050807568807027 ) ) ;
#2849=ORIENTED_EDGE ( 'NONE', *, *, #11426, .F. ) ;
#2857=CARTESIAN_POINT ( 'NONE',  ( 10.92172942406178926, 0.1300000000000051115, 7.935100905948385908 ) ) ;
#2864=AXIS2_PLACEMENT_3D ( 'NONE', #3359, #14215, #11238 ) ;
#2872=DIRECTION ( 'NONE',  ( -0.000000000000000000, 1.000000000000000000, -0.000000000000000000 ) ) ;
#2876=CARTESIAN_POINT ( 'NONE',  ( -4.171729424061787483, -18.66999999999999815, -12.83926296998457417 ) ) ;
#2879=AXIS2_PLACEMENT_3D ( 'NONE', #15450, #6121, #2017 ) ;
#2882=PLANE ( 'NONE',  #15753 ) ;
#2884=CARTESIAN_POINT ( 'NONE',  ( 3.708203932499379185, 3.163974596215581414, -11.41267819554186858 ) ) ;
#2890=CARTESIAN_POINT ( 'NONE',  ( -4.171729424061791036, 0.5300000000000026912, 12.83926296998457239 ) ) ;
#2891=CARTESIAN_POINT ( 'NONE',  ( -9.708203932499371192, 1.096025403784446350, 7.053423027509678533 ) ) ;
#2892=DIRECTION ( 'NONE',  ( 0.000000000000000000, 0.000000000000000000, -1.000000000000000000 ) ) ;
#2893=CARTESIAN_POINT ( 'NONE',  ( 9.520470885617717371, -3.269999999999995133, -6.917026985038131848 ) ) ;
#2895=CARTESIAN_POINT ( 'NONE',  ( 0.2252273365623476686, -18.34015606061350567, 15.45843899586301973 ) ) ;
#2898=DIRECTION ( 'NONE',  ( 0.000000000000000000, 0.000000000000000000, -1.000000000000000000 ) ) ;
#2905=CARTESIAN_POINT ( 'NONE',  ( -24.73863375370588003, 5.918584287042170544, -8.000000000000282441 ) ) ;
#2914=CARTESIAN_POINT ( 'NONE',  ( -1.732050807568877859, 0.000000000000000000, -18.99999999999999645 ) ) ;
#2916=CARTESIAN_POINT ( 'NONE',  ( 8.343458848123578520, 8.980000000000011084, 11.48378591275254124 ) ) ;
#2921=CARTESIAN_POINT ( 'NONE',  ( -13.49999999999999822, 11.77999999999999758, -4.386415899144240349 ) ) ;
#2928=DIRECTION ( 'NONE',  ( 0.000000000000000000, 0.000000000000000000, 1.000000000000000000 ) ) ;
#2929=DIRECTION ( 'NONE',  ( 0.000000000000000000, 1.000000000000000000, 0.000000000000000000 ) ) ;
#2935=AXIS2_PLACEMENT_3D ( 'NONE', #2156, #7580, #12959 ) ;
#2937=DIRECTION ( 'NONE',  ( -0.000000000000000000, 1.000000000000000000, -0.000000000000000000 ) ) ;
#2939=CARTESIAN_POINT ( 'NONE',  ( -7.272992578804310604, 22.38000000000000966, 10.01041549318726709 ) ) ;
#2940=EDGE_LOOP ( 'NONE', ( #4125, #7707, #14866, #16925 ) ) ;
#2942=ORIENTED_EDGE ( 'NONE', *, *, #13823, .T. ) ;
#2944=CARTESIAN_POINT ( 'NONE',  ( 7.272992578804308828, -13.02000000000000313, 10.01041549318726709 ) ) ;
#2957=VERTEX_POINT ( 'NONE', #5930 ) ;
#2961=CARTESIAN_POINT ( 'NONE',  ( -10.99999999999979394, 7.773118517290098950, -15.58845726812003996 ) ) ;
#2965=CARTESIAN_POINT ( 'NONE',  ( 4.171729424061791924, -15.96999999999999886, -12.83926296998457239 ) ) ;
#2971=CARTESIAN_POINT ( 'NONE',  ( -15.43494339453330255, 7.854708401161940579, -10.68872673103606807 ) ) ;
#2973=CARTESIAN_POINT ( 'NONE',  ( 1.900613283894441619, 3.237093173895313480, -12.00000000000002665 ) ) ;
#2979=CARTESIAN_POINT ( 'NONE',  ( 2.894739590358088936E-06, 0.6800804143413337055, 13.49999999999938360 ) ) ;
#2980=PLANE ( 'NONE',  #162 ) ;
#2982=CARTESIAN_POINT ( 'NONE',  ( -11.76794919243112325, -4.919999999999999041, 3.823638476888994386 ) ) ;
#2984=CARTESIAN_POINT ( 'NONE',  ( 4.171729424061791924, -16.96999999999999886, -12.83926296998457239 ) ) ;
#2998=CARTESIAN_POINT ( 'NONE',  ( -18.02297152527630786, 8.055324227812098670, -0.3502263562677673248 ) ) ;
#2999=CARTESIAN_POINT ( 'NONE',  ( -11.76794919243112325, 22.08000000000000540, 3.823638476888994386 ) ) ;
#3002=DIRECTION ( 'NONE',  ( -0.000000000000000000, 1.000000000000000000, -0.000000000000000000 ) ) ;
#3004=CARTESIAN_POINT ( 'NONE',  ( 13.49999999999999822, 6.279999999999996696, 4.386415899144237684 ) ) ;
#3005=ORIENTED_EDGE ( 'NONE', *, *, #14767, .F. ) ;
#3009=CARTESIAN_POINT ( 'NONE',  ( 10.92172942406178926, 4.129999999999994564, 7.935100905948385908 ) ) ;
#3021=CARTESIAN_POINT ( 'NONE',  ( -11.85687157084362120, 9.999999999999998224, -2.107649565213920440 ) ) ;
#3025=FACE_OUTER_BOUND ( 'NONE', #5026, .T. ) ;
#3027=CARTESIAN_POINT ( 'NONE',  ( -9.520470885617717371, 22.23000000000000043, 6.917026985038133624 ) ) ;
#3028=ORIENTED_EDGE ( 'NONE', *, *, #1488, .F. ) ;
#3031=CARTESIAN_POINT ( 'NONE',  ( -11.76794919243112325, -16.92000000000000526, 3.823638476888994386 ) ) ;
#3034=DIRECTION ( 'NONE',  ( 0.5000000000000066613, 0.000000000000000000, -0.8660254037844347108 ) ) ;
#3035=EDGE_CURVE ( 'NONE', #309, #5991, #2681, .T. ) ;
#3045=CARTESIAN_POINT ( 'NONE',  ( 16.03410433562979520, 8.027996319639559175, -8.458421099448731439 ) ) ;
#3049=ORIENTED_EDGE ( 'NONE', *, *, #17329, .F. ) ;
#3055=ADVANCED_FACE ( 'NONE', ( #347 ), #7486, .F. ) ;
#3056=CARTESIAN_POINT ( 'NONE',  ( -8.343458848123582072, -17.62000000000000099, 11.48378591275254124 ) ) ;
#3060=CARTESIAN_POINT ( 'NONE',  ( 2.279995255611139653E-15, -17.82000000000000028, -12.37355403259654985 ) ) ;
#3063=CARTESIAN_POINT ( 'NONE',  ( -7.272992578804310604, -4.620000000000000995, 10.01041549318726709 ) ) ;
#3065=CARTESIAN_POINT ( 'NONE',  ( 1.509281292405760415E-13, 1.813974596215571777, 12.00000000000000000 ) ) ;
#3071=CARTESIAN_POINT ( 'NONE',  ( -1.541208229742845548, 7.854057316169015479, -18.71369360505681811 ) ) ;
#3072=FACE_OUTER_BOUND ( 'NONE', #6583, .T. ) ;
#3074=CARTESIAN_POINT ( 'NONE',  ( -4.171729424061791036, 30.53000000000000114, 12.83926296998457239 ) ) ;
#3075=CARTESIAN_POINT ( 'NONE',  ( 11.76794919243112680, -6.420000000000001705, -3.823638476888993942 ) ) ;
#3077=CARTESIAN_POINT ( 'NONE',  ( 1.900613283903584083, 6.237093173894926679, -11.99999999999702993 ) ) ;
#3086=DIRECTION ( 'NONE',  ( -0.000000000000000000, 1.000000000000000000, -0.000000000000000000 ) ) ;
#3087=LINE ( 'NONE', #9926, #9516 ) ;
#3088=CARTESIAN_POINT ( 'NONE',  ( -25.42428528562849266, 0.000000000000000000, -5.441113646577748320 ) ) ;
#3092=CARTESIAN_POINT ( 'NONE',  ( -18.18516759496687740, 8.007293617507080796, 0.8582236110266343587 ) ) ;
#3093=CARTESIAN_POINT ( 'NONE',  ( 3.636496289402157078, 24.02999999999999403, -11.19198476289190936 ) ) ;
#3094=ORIENTED_EDGE ( 'NONE', *, *, #13412, .F. ) ;
#3096=CARTESIAN_POINT ( 'NONE',  ( -3.708203932499367195, 3.196025403784437113, -11.41267819554184548 ) ) ;
#3098=CARTESIAN_POINT ( 'NONE',  ( -13.50000000000000000, 4.930000000000004157, -3.469446951953614189E-15 ) ) ;
#3099=VERTEX_POINT ( 'NONE', #15203 ) ;
#3101=LINE ( 'NONE', #15201, #5721 ) ;
#3102=CARTESIAN_POINT ( 'NONE',  ( -13.49999999999999822, 0.07999999999999600486, 4.386415899144235908 ) ) ;
#3103=EDGE_CURVE ( 'NONE', #2050, #9433, #3959, .T. ) ;
#3115=CARTESIAN_POINT ( 'NONE',  ( -13.49999999999999822, -9.919999999999999929, 4.386415899144235908 ) ) ;
#3117=DIRECTION ( 'NONE',  ( 1.000000000000000000, 0.000000000000000000, 9.821670480311996085E-15 ) ) ;
#3119=CARTESIAN_POINT ( 'NONE',  ( -11.76794919243112325, 24.78000000000000824, -3.823638476888998827 ) ) ;
#3122=ORIENTED_EDGE ( 'NONE', *, *, #2631, .F. ) ;
#3123=CARTESIAN_POINT ( 'NONE',  ( -9.520470885617715595, -17.36999999999999744, -6.917026985038136289 ) ) ;
#3126=CARTESIAN_POINT ( 'NONE',  ( -15.58845726811999910, 0.000000000000000000, 10.99999999999985256 ) ) ;
#3129=CARTESIAN_POINT ( 'NONE',  ( 2.207926304393408011E-15, 8.062177826491096155, 17.99999999999999645 ) ) ;
#3134=VERTEX_POINT ( 'NONE', #3735 ) ;
#3136=ORIENTED_EDGE ( 'NONE', *, *, #2187, .T. ) ;
#3141=CARTESIAN_POINT ( 'NONE',  ( -16.17460542229569498, 8.007813505529846054, 8.351563113033579455 ) ) ;
#3144=CARTESIAN_POINT ( 'NONE',  ( -3.636496289402152637, 27.32999999999999474, -11.19198476289190936 ) ) ;
#3150=FACE_OUTER_BOUND ( 'NONE', #6063, .T. ) ;
#3151=CARTESIAN_POINT ( 'NONE',  ( 11.76794919243112325, -3.569999999999996732, 1.734723475976807094E-15 ) ) ;
#3157=CARTESIAN_POINT ( 'NONE',  ( -13.35138662365028317, 1.798999282680476490E-09, 1.996909364337476678 ) ) ;
#3158=CARTESIAN_POINT ( 'NONE',  ( 0.000000000000000000, 9.999999999999998224, 0.000000000000000000 ) ) ;
#3160=CARTESIAN_POINT ( 'NONE',  ( 8.343458848123583849, 28.88000000000001322, -11.48378591275253768 ) ) ;
#3161=CARTESIAN_POINT ( 'NONE',  ( 3.636496289402157078, -8.969999999999998863, -11.19198476289190936 ) ) ;
#3163=CARTESIAN_POINT ( 'NONE',  ( -4.171729424061787483, -13.66999999999999460, -12.83926296998457417 ) ) ;
#3168=PRODUCT_DEFINITION ( 'UNKNOWN', '', #8215, #7745 ) ;
#3175=EDGE_CURVE ( 'NONE', #6231, #11897, #12829, .T. ) ;
#3177=ADVANCED_FACE ( 'NONE', ( #716 ), #14221, .F. ) ;
#3178=CARTESIAN_POINT ( 'NONE',  ( -9.999999999999776179, 0.000000000000000000, -17.32050807568890605 ) ) ;
#3182=CARTESIAN_POINT ( 'NONE',  ( 11.76794919243112680, 23.58000000000001961, -3.823638476888993942 ) ) ;
#3187=CARTESIAN_POINT ( 'NONE',  ( -8.343458848123576743, 10.48000000000000753, -11.48378591275254301 ) ) ;
#3188=ORIENTED_EDGE ( 'NONE', *, *, #7234, .F. ) ;
#3191=CARTESIAN_POINT ( 'NONE',  ( 8.343458848123583849, 1.879999999999997451, -11.48378591275253768 ) ) ;
#3206=EDGE_CURVE ( 'NONE', #9217, #1172, #11808, .T. ) ;
#3209=CARTESIAN_POINT ( 'NONE',  ( 1.133320036021603139, 9.999999999999996447, 13.00525967219381762 ) ) ;
#3213=ORIENTED_EDGE ( 'NONE', *, *, #13130, .F. ) ;
#3214=CARTESIAN_POINT ( 'NONE',  ( 13.50000000000000355, 33.58000000000000540, -4.386415899144233244 ) ) ;
#3224=CARTESIAN_POINT ( 'NONE',  ( 3.636496289402157078, 15.03000000000001535, -11.19198476289190936 ) ) ;
#3228=CARTESIAN_POINT ( 'NONE',  ( -8.891200544363830713E-16, 8.679999999999999716, 13.49999999999999822 ) ) ;
#3234=CARTESIAN_POINT ( 'NONE',  ( -11.00000000000012612, 0.000000000000000000, 15.58845726811980725 ) ) ;
#3236=CARTESIAN_POINT ( 'NONE',  ( 7.272992578804311492, 32.88000000000000256, -10.01041549318726709 ) ) ;
#3240=FACE_OUTER_BOUND ( 'NONE', #5359, .T. ) ;
#3241=CARTESIAN_POINT ( 'NONE',  ( -11.76794919243112325, -2.069999999999995399, -2.602085213965210642E-15 ) ) ;
#3247=DIRECTION ( 'NONE',  ( 0.000000000000000000, 0.000000000000000000, 1.000000000000000000 ) ) ;
#3249=CARTESIAN_POINT ( 'NONE',  ( -17.42428528562871293, 0.000000000000000000, 19.29752010712834220 ) ) ;
#3250=CARTESIAN_POINT ( 'NONE',  ( 13.50000000000000000, 31.43000000000001393, 1.734723475976807094E-15 ) ) ;
#3251=CARTESIAN_POINT ( 'NONE',  ( 9.520470885617717371, -6.269999999999997797, -6.917026985038131848 ) ) ;
#3255=CARTESIAN_POINT ( 'NONE',  ( -4.171729424061791036, -15.46999999999999709, 12.83926296998457239 ) ) ;
#3256=APPLICATION_CONTEXT ( 'automotive_design' ) ;
#3259=CARTESIAN_POINT ( 'NONE',  ( 8.343458848123580296, 2.979999999999998650, 11.48378591275253768 ) ) ;
#3260=MANIFOLD_SOLID_BREP ( 'Combine1', #4371 ) ;
#3261=EDGE_CURVE ( 'NONE', #8284, #11444, #7607, .T. ) ;
#3265=( GEOMETRIC_REPRESENTATION_CONTEXT ( 3 ) GLOBAL_UNCERTAINTY_ASSIGNED_CONTEXT ( ( #15266 ) ) GLOBAL_UNIT_ASSIGNED_CONTEXT ( ( #8539, #13889, #14068 ) ) REPRESENTATION_CONTEXT ( 'NONE', 'WORKASPACE' ) );
#3271=CARTESIAN_POINT ( 'NONE',  ( 8.000000000000023093, 0.000000000000000000, -17.32050807568876394 ) ) ;
#3273=CARTESIAN_POINT ( 'NONE',  ( 9.520470885617717371, 17.72999999999999687, -6.917026985038131848 ) ) ;
#3274=VERTEX_POINT ( 'NONE', #474 ) ;
#3278=CARTESIAN_POINT ( 'NONE',  ( -13.49999999999999822, 4.780000000000001137, -4.386415899144240349 ) ) ;
#3279=CARTESIAN_POINT ( 'NONE',  ( 7.272992578804311492, 32.88000000000000256, -10.01041549318726709 ) ) ;
#3280=CARTESIAN_POINT ( 'NONE',  ( -9.999999999999776179, 0.000000000000000000, -15.32050807568890605 ) ) ;
#3281=AXIS2_PLACEMENT_3D ( 'NONE', #1187, #1269, #10400 ) ;
#3282=CARTESIAN_POINT ( 'NONE',  ( 4.171729424061789260, 6.830000000000002736, 12.83926296998457239 ) ) ;
#3285=LINE ( 'NONE', #14231, #303 ) ;
#3286=EDGE_CURVE ( 'NONE', #14568, #15151, #11437, .T. ) ;
#3287=( BOUNDED_CURVE ( )  B_SPLINE_CURVE ( 2, ( #4423, #3077, #1837, #8504, #13853, #1756, #7252, #16691, #4598, #2006, #12812, #11745, #3603 ),
 .UNSPECIFIED., .F., .F. ) 
 B_SPLINE_CURVE_WITH_KNOTS ( ( 3, 2, 2, 2, 2, 2, 3 ),
 ( 0.09225345574959326056, 0.09600779387844439461, 0.1035164701361835637, 0.1110251463939227468, 0.1185338226516619159, 0.1260424989094010850, 0.1297968370382597270 ),
 .UNSPECIFIED. ) 
 CURVE ( )  GEOMETRIC_REPRESENTATION_ITEM ( )  RATIONAL_B_SPLINE_CURVE ( ( 0.9755282581475768211, 0.9755282581476976134, 1.000000000000000000, 0.9510565162951535312, 1.000000000000000000, 0.9510565162951535312, 1.000000000000000000, 0.9510565162951535312, 1.000000000000000000, 0.9510565162951535312, 1.000000000000000000, 0.9755282581476480974, 0.9755282581475767101 ) ) 
 REPRESENTATION_ITEM ( '' )  );
#3293=B_SPLINE_CURVE_WITH_KNOTS ( 'NONE', 3,
 ( #305, #8455, #129, #4283 ),
 .UNSPECIFIED., .F., .F.,
 ( 4, 4 ),
 ( 2.383248697827832346E-07, 0.007646667935218598965 ),
 .UNSPECIFIED. ) ;
#3298=CARTESIAN_POINT ( 'NONE',  ( -11.00000000000012612, 0.000000000000000000, 15.58845726811980725 ) ) ;
#3304=ORIENTED_EDGE ( 'NONE', *, *, #12057, .F. ) ;
#3305=CARTESIAN_POINT ( 'NONE',  ( 11.76794919243112325, -18.72000000000000952, 3.823638476888996163 ) ) ;
#3311=CARTESIAN_POINT ( 'NONE',  ( 11.33202052101486146, -2.258074356960819520E-15, 6.793706961618169338 ) ) ;
#3312=EDGE_CURVE ( 'NONE', #15652, #7559, #10626, .T. ) ;
#3319=EDGE_LOOP ( 'NONE', ( #3477, #8212, #14391, #16991 ) ) ;
#3322=B_SPLINE_CURVE_WITH_KNOTS ( 'NONE', 3,
 ( #6401, #4892, #9149, #13018 ),
 .UNSPECIFIED., .F., .F.,
 ( 4, 4 ),
 ( 2.383248697861188768E-07, 0.007646667935218605036 ),
 .UNSPECIFIED. ) ;
#3326=CARTESIAN_POINT ( 'NONE',  ( 17.32050807568873552, 7.773118517290098062, 8.000000000000083489 ) ) ;
#3327=CARTESIAN_POINT ( 'NONE',  ( -13.49999999999999822, 6.080000000000002736, 4.386415899144235020 ) ) ;
#3330=CARTESIAN_POINT ( 'NONE',  ( -3.636496289402152637, 33.32999999999999829, -11.19198476289190936 ) ) ;
#3333=ADVANCED_FACE ( 'NONE', ( #811 ), #1161, .T. ) ;
#3335=CARTESIAN_POINT ( 'NONE',  ( -7.272992578804307939, -14.51999999999999957, -10.01041549318726886 ) ) ;
#3337=LINE ( 'NONE', #11478, #7034 ) ;
#3338=CARTESIAN_POINT ( 'NONE',  ( 7.272992578804311492, -0.1199999999999976641, -10.01041549318726709 ) ) ;
#3341=CARTESIAN_POINT ( 'NONE',  ( -4.206197538246631673, 6.548267719634617734, 23.28534784291397131 ) ) ;
#3345=CARTESIAN_POINT ( 'NONE',  ( 5.441113646577480978, 5.918584287042170544, -25.42428528562854595 ) ) ;
#3346=CARTESIAN_POINT ( 'NONE',  ( -11.00000000000012612, 7.773118517290097174, 15.58845726811980725 ) ) ;
#3353=AXIS2_PLACEMENT_3D ( 'NONE', #9165, #13035, #11538 ) ;
#3359=CARTESIAN_POINT ( 'NONE',  ( 1.732050807568740858, 0.000000000000000000, 19.00000000000000355 ) ) ;
#3364=AXIS2_PLACEMENT_3D ( 'NONE', #15668, #2404, #3576 ) ;
#3365=CARTESIAN_POINT ( 'NONE',  ( 2.279995255611139653E-15, 18.18000000000001393, -12.37355403259654985 ) ) ;
#3367=ORIENTED_EDGE ( 'NONE', *, *, #4951, .T. ) ;
#3371=CARTESIAN_POINT ( 'NONE',  ( -10.92172942406179104, -0.7699999999999929123, 7.935100905948385908 ) ) ;
#3372=DIRECTION ( 'NONE',  ( -0.000000000000000000, -1.000000000000000000, -0.000000000000000000 ) ) ;
#3376=CARTESIAN_POINT ( 'NONE',  ( -4.206197538246465584, 6.548267719634618622, -23.28534784291399973 ) ) ;
#3383=CARTESIAN_POINT ( 'NONE',  ( -1.900613283894436512, 7.737093173895296161, 12.00000000000000178 ) ) ;
#3390=ORIENTED_EDGE ( 'NONE', *, *, #4854, .T. ) ;
#3393=ORIENTED_EDGE ( 'NONE', *, *, #13130, .T. ) ;
#3394=CARTESIAN_POINT ( 'NONE',  ( -8.549982208541774191E-16, 29.67999999999999972, 14.19474002721660355 ) ) ;
#3401=CARTESIAN_POINT ( 'NONE',  ( 12.39312577248542624, 2.367644581053835256E-15, 4.108133863307598332 ) ) ;
#3403=LINE ( 'NONE', #8903, #5728 ) ;
#3406=ORIENTED_EDGE ( 'NONE', *, *, #3832, .F. ) ;
#3407=DIRECTION ( 'NONE',  ( -0.000000000000000000, -1.000000000000000000, -0.000000000000000000 ) ) ;
#3409=ORIENTED_EDGE ( 'NONE', *, *, #17329, .T. ) ;
#3413=CARTESIAN_POINT ( 'NONE',  ( 8.000000000000023093, 0.000000000000000000, -17.32050807568876394 ) ) ;
#3415=CARTESIAN_POINT ( 'NONE',  ( 16.17792858571907644, 8.007293667506182544, 8.349340579021683695 ) ) ;
#3416=CARTESIAN_POINT ( 'NONE',  ( 11.00000000000001599, 0.000000000000000000, -15.58845726811988364 ) ) ;
#3419=CARTESIAN_POINT ( 'NONE',  ( 2.279995255611139653E-15, 33.17999999999999972, -12.37355403259654985 ) ) ;
#3424=CARTESIAN_POINT ( 'NONE',  ( 7.272992578804311492, -3.120000000000004992, -10.01041549318726709 ) ) ;
#3430=CARTESIAN_POINT ( 'NONE',  ( 17.42428528562858148, 5.918584287042170544, -19.29752010712846300 ) ) ;
#3431=LINE ( 'NONE', #3249, #2321 ) ;
#3432=VERTEX_POINT ( 'NONE', #11952 ) ;
#3434=DIRECTION ( 'NONE',  ( 0.000000000000000000, 0.000000000000000000, -1.000000000000000000 ) ) ;
#3449=EDGE_CURVE ( 'NONE', #6427, #15651, #14492, .T. ) ;
#3450=LINE ( 'NONE', #793, #8473 ) ;
#3453=CARTESIAN_POINT ( 'NONE',  ( 11.76794919243112680, 14.57999999999999474, -3.823638476888993942 ) ) ;
#3458=CARTESIAN_POINT ( 'NONE',  ( -13.49999999999999822, 2.079999999999997851, 4.386415899144235908 ) ) ;
#3459=CARTESIAN_POINT ( 'NONE',  ( 7.272992578804311492, 29.88000000000000966, -10.01041549318726709 ) ) ;
#3477=ORIENTED_EDGE ( 'NONE', *, *, #9399, .T. ) ;
#3479=CARTESIAN_POINT ( 'NONE',  ( -13.49999999999999822, 28.78000000000001535, -4.386415899144240349 ) ) ;
#3485=CARTESIAN_POINT ( 'NONE',  ( 5.441113646577305119, 5.918584287042172321, 25.42428528562857792 ) ) ;
#3490=CARTESIAN_POINT ( 'NONE',  ( 12.00000000000000178, 5.146025403784437735, 3.899036354794877202 ) ) ;
#3495=CARTESIAN_POINT ( 'NONE',  ( 17.32050807568878170, 7.773118517290099838, -7.999999999999961808 ) ) ;
#3497=CARTESIAN_POINT ( 'NONE',  ( 19.29752010712851984, 0.000000000000000000, -17.42428528562851042 ) ) ;
#3499=DIRECTION ( 'NONE',  ( -1.000000000000000000, 0.000000000000000000, 4.676985943005715098E-16 ) ) ;
#3504=EDGE_CURVE ( 'NONE', #3760, #15564, #8965, .T. ) ;
#3513=AXIS2_PLACEMENT_3D ( 'NONE', #16928, #11726, #10235 ) ;
#3514=CARTESIAN_POINT ( 'NONE',  ( -1.005545769327274827E-13, 2.180000000000013927, -13.50000000000000000 ) ) ;
#3515=ORIENTED_EDGE ( 'NONE', *, *, #53, .F. ) ;
#3519=CARTESIAN_POINT ( 'NONE',  ( -22.26874168100106033, 6.548282979925672542, -8.000000000000257572 ) ) ;
#3523=ADVANCED_FACE ( 'NONE', ( #6397 ), #15641, .F. ) ;
#3528=CARTESIAN_POINT ( 'NONE',  ( 8.378360550312208943, 10.00007452681958497, 10.58551248116806498 ) ) ;
#3533=CARTESIAN_POINT ( 'NONE',  ( -3.636496289402156190, 10.53000000000001180, 11.19198476289190758 ) ) ;
#3538=CARTESIAN_POINT ( 'NONE',  ( -8.343458848123576743, 1.479999999999995541, -11.48378591275254301 ) ) ;
#3539=B_SPLINE_CURVE_WITH_KNOTS ( 'NONE', 3,
 ( #14571, #11682, #13088, #9041 ),
 .UNSPECIFIED., .F., .F.,
 ( 4, 4 ),
 ( 0.008786844460939030252, 0.01643317035798799036 ),
 .UNSPECIFIED. ) ;
#3540=CARTESIAN_POINT ( 'NONE',  ( 3.636496289402154414, 31.82999999999999829, 11.19198476289190758 ) ) ;
#3556=CARTESIAN_POINT ( 'NONE',  ( 1.137810555388867773, -1.046521029022079216E-15, -11.94593600937347055 ) ) ;
#3558=ORIENTED_EDGE ( 'NONE', *, *, #11641, .F. ) ;
#3560=CARTESIAN_POINT ( 'NONE',  ( -9.520470885617715595, 6.629999999999997229, -6.917026985038136289 ) ) ;
#3561=ORIENTED_EDGE ( 'NONE', *, *, #2631, .T. ) ;
#3562=ORIENTED_EDGE ( 'NONE', *, *, #7310, .F. ) ;
#3563=CARTESIAN_POINT ( 'NONE',  ( 8.343458848123583849, 27.88000000000001322, -11.48378591275253768 ) ) ;
#3570=CARTESIAN_POINT ( 'NONE',  ( 0.000000000000000000, 30.93000000000001393, 0.000000000000000000 ) ) ;
#3573=DIRECTION ( 'NONE',  ( -0.000000000000000000, 1.000000000000000000, -0.000000000000000000 ) ) ;
#3576=DIRECTION ( 'NONE',  ( 0.000000000000000000, 0.000000000000000000, -1.000000000000000000 ) ) ;
#3577=ORIENTED_EDGE ( 'NONE', *, *, #11185, .T. ) ;
#3581=EDGE_CURVE ( 'NONE', #8520, #860, #15587, .T. ) ;
#3597=DIRECTION ( 'NONE',  ( 0.8660254037844362651, 0.000000000000000000, 0.5000000000000041078 ) ) ;
#3599=CARTESIAN_POINT ( 'NONE',  ( 13.50000000000000355, 25.58000000000000185, -4.386415899144233244 ) ) ;
#3601=ORIENTED_EDGE ( 'NONE', *, *, #14970, .T. ) ;
#3602=DIRECTION ( 'NONE',  ( 0.5000000000000066613, -0.000000000000000000, -0.8660254037844347108 ) ) ;
#3603=CARTESIAN_POINT ( 'NONE',  ( 1.108954987895778950E-11, 4.813974596216015200, 12.00000000000000178 ) ) ;
#3606=CARTESIAN_POINT ( 'NONE',  ( -3.556480217745532916E-14, 9.046025403784437202, -12.00000000000000000 ) ) ;
#3608=CARTESIAN_POINT ( 'NONE',  ( -8.549982208541774191E-16, 6.679999999999998828, 14.19474002721660355 ) ) ;
#3615=CARTESIAN_POINT ( 'NONE',  ( 12.00000000000000178, 2.146025403784442620, 3.899036354794877202 ) ) ;
#3619=ORIENTED_EDGE ( 'NONE', *, *, #13412, .T. ) ;
#3620=CARTESIAN_POINT ( 'NONE',  ( -11.76794919243112325, 9.929999999999994387, -2.602085213965210642E-15 ) ) ;
#3621=ORIENTED_EDGE ( 'NONE', *, *, #10800, .T. ) ;
#3625=CARTESIAN_POINT ( 'NONE',  ( 8.343458848123583849, 0.8799999999999997824, -11.48378591275253768 ) ) ;
#3626=EDGE_CURVE ( 'NONE', #4018, #4394, #13707, .T. ) ;
#3634=CARTESIAN_POINT ( 'NONE',  ( -1.900613283901089634, 9.390856018536133831, -11.99999999999790390 ) ) ;
#3638=DIRECTION ( 'NONE',  ( 0.8660254037844430375, -0.000000000000000000, -0.4999999999999925060 ) ) ;
#3644=FACE_OUTER_BOUND ( 'NONE', #7385, .T. ) ;
#3646=EDGE_LOOP ( 'NONE', ( #9521, #7185, #17362, #8949 ) ) ;
#3650=CARTESIAN_POINT ( 'NONE',  ( 11.76794919243112325, 8.280000000000006466, 3.823638476888996163 ) ) ;
#3651=ORIENTED_EDGE ( 'NONE', *, *, #5434, .T. ) ;
#3655=CARTESIAN_POINT ( 'NONE',  ( -4.171729424061787483, 25.33000000000001961, -12.83926296998457417 ) ) ;
#3667=CARTESIAN_POINT ( 'NONE',  ( 19.29752010712840615, 0.000000000000000000, 17.42428528562864898 ) ) ;
#3670=ORIENTED_EDGE ( 'NONE', *, *, #16344, .T. ) ;
#3688=CARTESIAN_POINT ( 'NONE',  ( 9.520470885617717371, 20.72999999999999687, -6.917026985038131848 ) ) ;
#3691=DIRECTION ( 'NONE',  ( 0.000000000000000000, 0.000000000000000000, -1.000000000000000000 ) ) ;
#3693=CARTESIAN_POINT ( 'NONE',  ( 10.92172942406179104, 22.73000000000000043, -7.935100905948385908 ) ) ;
#3694=ORIENTED_EDGE ( 'NONE', *, *, #15310, .F. ) ;
#3699=CARTESIAN_POINT ( 'NONE',  ( -13.49999999999999822, -6.220000000000002416, -4.386415899144240349 ) ) ;
#3711=CARTESIAN_POINT ( 'NONE',  ( 3.636496289402157078, 9.030000000000010019, -11.19198476289190936 ) ) ;
#3715=DIRECTION ( 'NONE',  ( 0.000000000000000000, 1.000000000000000000, 0.000000000000000000 ) ) ;
#3716=CARTESIAN_POINT ( 'NONE',  ( 10.92172942406179104, 0.7300000000000084199, -7.935100905948385908 ) ) ;
#3727=CARTESIAN_POINT ( 'NONE',  ( 1.876532330890708260E-11, 6.313974596214807278, -12.00000000000000355 ) ) ;
#3735=CARTESIAN_POINT ( 'NONE',  ( 1.509281292405760415E-13, 1.813974596215571777, 12.00000000000000178 ) ) ;
#3738=CARTESIAN_POINT ( 'NONE',  ( -3.636496289402152637, 3.329999999999999627, -11.19198476289190936 ) ) ;
#3739=ORIENTED_EDGE ( 'NONE', *, *, #15969, .T. ) ;
#3741=ORIENTED_EDGE ( 'NONE', *, *, #1418, .T. ) ;
#3742=CARTESIAN_POINT ( 'NONE',  ( 13.50000000000000355, 24.58000000000001606, -4.386415899144233244 ) ) ;
#3750=CARTESIAN_POINT ( 'NONE',  ( 10.92172942406179104, 1.730000000000009308, -7.935100905948385908 ) ) ;
#3751=EDGE_CURVE ( 'NONE', #14160, #1419, #6919, .T. ) ;
#3753=CARTESIAN_POINT ( 'NONE',  ( 25.42428528562856727, 0.000000000000000000, -5.441113646577394825 ) ) ;
#3760=VERTEX_POINT ( 'NONE', #6739 ) ;
#3761=VERTEX_POINT ( 'NONE', #6827 ) ;
#3763=ORIENTED_EDGE ( 'NONE', *, *, #15079, .F. ) ;
#3764=CARTESIAN_POINT ( 'NONE',  ( -4.171729424061791036, 17.53000000000001890, 12.83926296998457239 ) ) ;
#3771=EDGE_CURVE ( 'NONE', #5443, #4554, #9793, .T. ) ;
#3776=CARTESIAN_POINT ( 'NONE',  ( 3.636496289402157078, 21.02999999999999403, -11.19198476289190936 ) ) ;
#3778=DIRECTION ( 'NONE',  ( 0.8660254037844400399, 0.000000000000000000, -0.4999999999999976685 ) ) ;
#3784=B_SPLINE_CURVE_WITH_KNOTS ( 'NONE', 3,
 ( #10054, #12863, #15404, #2060, #6240, #3311, #10306, #8725, #3401, #14339, #2315, #6072, #15575, #2228, #16829, #9074, #15751, #7743, #14083, #14254, #8813, #1970, #12775, #663, #7568, #917, #15490, #7482 ),
 .UNSPECIFIED., .F., .F.,
 ( 4, 2, 2, 2, 2, 2, 2, 2, 2, 2, 2, 2, 2, 4 ),
 ( 1.666147490140627990E-16, 0.002883762942657031644, 0.004325644413985462247, 0.005767525885313893284, 0.008651288827970756226, 0.01009317029929918813, 0.01153505177062761830, 0.01297693324195605021, 0.01441881471328448211, 0.01730257765594134592, 0.01874445912726978303, 0.02018634059859821667, 0.02162822206992665031, 0.02307010354125508395 ),
 .UNSPECIFIED. ) ;
#3787=CARTESIAN_POINT ( 'NONE',  ( -13.50000000000000000, -3.069999999999996287, -3.469446951953614189E-15 ) ) ;
#3793=AXIS2_PLACEMENT_3D ( 'NONE', #13494, #5473, #14805 ) ;
#3797=PRODUCT_DEFINITION_SHAPE ( 'NONE', 'NONE',  #3168 ) ;
#3802=CARTESIAN_POINT ( 'NONE',  ( 0.000000000000000000, 9.000000000000000000, 0.000000000000000000 ) ) ;
#3803=CARTESIAN_POINT ( 'NONE',  ( 3.636496289402157078, 15.03000000000001535, -11.19198476289190936 ) ) ;
#3804=ORIENTED_EDGE ( 'NONE', *, *, #7234, .T. ) ;
#3808=CARTESIAN_POINT ( 'NONE',  ( -4.171729424061787483, -7.669999999999996376, -12.83926296998457417 ) ) ;
#3810=DIRECTION ( 'NONE',  ( 0.000000000000000000, 0.000000000000000000, -1.000000000000000000 ) ) ;
#3813=DIRECTION ( 'NONE',  ( 2.806191565803427284E-15, 0.000000000000000000, -1.000000000000000000 ) ) ;
#3818=CARTESIAN_POINT ( 'NONE',  ( -9.708203932499367639, 3.763974596215556190, -7.053423027509681198 ) ) ;
#3827=CARTESIAN_POINT ( 'NONE',  ( 9.520470885617717371, 8.730000000000014637, -6.917026985038131848 ) ) ;
#3828=VERTEX_POINT ( 'NONE', #9316 ) ;
#3829=ORIENTED_EDGE ( 'NONE', *, *, #8420, .F. ) ;
#3830=CARTESIAN_POINT ( 'NONE',  ( 8.343458848123578520, 23.98000000000000753, 11.48378591275254124 ) ) ;
#3832=EDGE_CURVE ( 'NONE', #7801, #17099, #5504, .T. ) ;
#3834=VECTOR ( 'NONE', #14029, 1000.000000000000000 ) ;
#3841=PLANE ( 'NONE',  #10916 ) ;
#3842=CYLINDRICAL_SURFACE ( 'NONE', #3364, 13.50000000000000000 ) ;
#3847=ORIENTED_EDGE ( 'NONE', *, *, #7267, .T. ) ;
#3850=EDGE_CURVE ( 'NONE', #9365, #9933, #4414, .T. ) ;
#3853=AXIS2_PLACEMENT_3D ( 'NONE', #11306, #15346, #3247 ) ;
#3860=CARTESIAN_POINT ( 'NONE',  ( -11.76794919243112325, 18.78000000000001180, -3.823638476888998827 ) ) ;
#3864=ORIENTED_EDGE ( 'NONE', *, *, #10758, .T. ) ;
#3865=CARTESIAN_POINT ( 'NONE',  ( 9.335235950531815854E-15, 8.180000000000005045, -13.50000000000000178 ) ) ;
#3867=CARTESIAN_POINT ( 'NONE',  ( 2.279995255611139653E-15, 27.18000000000000682, -12.37355403259654985 ) ) ;
#3882=CARTESIAN_POINT ( 'NONE',  ( 9.520470885617715595, 11.13000000000000078, 6.917026985038135400 ) ) ;
#3885=CARTESIAN_POINT ( 'NONE',  ( 7.272992578804308828, 4.980000000000008420, 10.01041549318726709 ) ) ;
#3889=CARTESIAN_POINT ( 'NONE',  ( -13.50000000000000000, -10.06999999999999496, -3.469446951953614189E-15 ) ) ;
#3890=PLANE ( 'NONE',  #4324 ) ;
#3909=DIRECTION ( 'NONE',  ( -0.000000000000000000, 1.000000000000000000, -0.000000000000000000 ) ) ;
#3910=CARTESIAN_POINT ( 'NONE',  ( 9.520470885617717371, 2.730000000000010196, -6.917026985038131848 ) ) ;
#3912=EDGE_LOOP ( 'NONE', ( #10047, #1056, #6154, #6746 ) ) ;
#3913=CARTESIAN_POINT ( 'NONE',  ( -13.50000000000000000, 19.93000000000000327, -3.469446951953614189E-15 ) ) ;
#3916=CARTESIAN_POINT ( 'NONE',  ( 13.50000000000000355, 10.57999999999999119, -4.386415899144233244 ) ) ;
#3923=LINE ( 'NONE', #6941, #16031 ) ;
#3924=DIRECTION ( 'NONE',  ( -0.000000000000000000, 1.000000000000000000, -0.000000000000000000 ) ) ;
#3925=CARTESIAN_POINT ( 'NONE',  ( -3.998255974501887078, 10.00000000000000888, -12.30404106125027575 ) ) ;
#3931=ORIENTED_EDGE ( 'NONE', *, *, #12689, .F. ) ;
#3933=VERTEX_POINT ( 'NONE', #9841 ) ;
#3936=VECTOR ( 'NONE', #12887, 1000.000000000000000 ) ;
#3945=EDGE_CURVE ( 'NONE', #8869, #3432, #3087, .T. ) ;
#3947=CARTESIAN_POINT ( 'NONE',  ( -3.636496289402152637, 21.33000000000001606, -11.19198476289190936 ) ) ;
#3952=ORIENTED_EDGE ( 'NONE', *, *, #13794, .T. ) ;
#3953=CARTESIAN_POINT ( 'NONE',  ( -2.707340708274796892, 3.720968205702271315E-15, -11.97265601701247384 ) ) ;
#3956=CARTESIAN_POINT ( 'NONE',  ( 11.76794919243112325, -12.56999999999999851, 1.734723475976807094E-15 ) ) ;
#3958=CARTESIAN_POINT ( 'NONE',  ( -10.92172942406178926, -3.369999999999997886, -7.935100905948389460 ) ) ;
#3959=( BOUNDED_CURVE ( )  B_SPLINE_CURVE ( 2, ( #5783, #377, #11168, #11616, #6151 ),
 .UNSPECIFIED., .F., .F. ) 
 B_SPLINE_CURVE_WITH_KNOTS ( ( 3, 2, 3 ),
 ( 0.2424487531369445559, 0.2462071549303284645, 0.2503072064569185073 ),
 .UNSPECIFIED. ) 
 CURVE ( )  GEOMETRIC_REPRESENTATION_ITEM ( )  RATIONAL_B_SPLINE_CURVE ( ( 0.9755282581475768211, 0.9755282581474007397, 1.000000000000000000, 0.9733037051233607295, 0.9757304765342935671 ) ) 
 REPRESENTATION_ITEM ( '' )  );
#3973=DIRECTION ( 'NONE',  ( 0.000000000000000000, 0.000000000000000000, -1.000000000000000000 ) ) ;
#3974=CARTESIAN_POINT ( 'NONE',  ( -9.520470885617717371, 7.230000000000014637, 6.917026985038133624 ) ) ;
#3978=CARTESIAN_POINT ( 'NONE',  ( 8.343458848123578520, -9.020000000000008455, 11.48378591275254124 ) ) ;
#3999=CARTESIAN_POINT ( 'NONE',  ( -8.343458848123582072, 20.38000000000000256, 11.48378591275254124 ) ) ;
#4002=CARTESIAN_POINT ( 'NONE',  ( 10.92172942406178926, 10.13000000000000078, 7.935100905948385908 ) ) ;
#4008=VECTOR ( 'NONE', #9943, 1000.000000000000000 ) ;
#4011=CARTESIAN_POINT ( 'NONE',  ( -5.441113646577662166, 5.918584287042170544, 25.42428528562851042 ) ) ;
#4012=CARTESIAN_POINT ( 'NONE',  ( -1.403940416332137451E-13, 0.000000000000000000, 19.99999999999999289 ) ) ;
#4015=CARTESIAN_POINT ( 'NONE',  ( 17.42428528562844292, 5.918584287042172321, 19.29752010712858024 ) ) ;
#4018=VERTEX_POINT ( 'NONE', #16786 ) ;
#4019=VERTEX_POINT ( 'NONE', #11237 ) ;
#4025=CARTESIAN_POINT ( 'NONE',  ( 8.178053476330042315, 7.956441929884681130, 16.47733079524786248 ) ) ;
#4033=CARTESIAN_POINT ( 'NONE',  ( -9.520470885617717371, 16.22999999999999332, 6.917026985038133624 ) ) ;
#4038=CARTESIAN_POINT ( 'NONE',  ( -8.048508853266335805, 2.177477983142712198E-15, -9.806701840662514158 ) ) ;
#4041=CARTESIAN_POINT ( 'NONE',  ( -11.76794919243112325, -11.22000000000000242, -3.823638476888998827 ) ) ;
#4042=FACE_OUTER_BOUND ( 'NONE', #5955, .T. ) ;
#4044=CARTESIAN_POINT ( 'NONE',  ( 4.171729424061791924, -3.970000000000001528, -12.83926296998457239 ) ) ;
#4057=CARTESIAN_POINT ( 'NONE',  ( -8.343458848123582072, 8.380000000000002558, 11.48378591275253768 ) ) ;
#4058=CARTESIAN_POINT ( 'NONE',  ( 9.520470885617717371, 2.730000000000010196, -6.917026985038131848 ) ) ;
#4062=( BOUNDED_CURVE ( )  B_SPLINE_CURVE ( 2, ( #4146, #262, #7163, #12632, #2891, #16599, #8323, #1575, #6993, #4506, #15260, #12368, #16237 ),
 .UNSPECIFIED., .F., .F. ) 
 B_SPLINE_CURVE_WITH_KNOTS ( ( 3, 2, 2, 2, 2, 2, 3 ),
 ( 0.5972222222222222099, 0.5999999999999999778, 0.6055555555555555136, 0.6111111111111111605, 0.6166666666666666963, 0.6222222222222222321, 0.6250000000000000000 ),
 .UNSPECIFIED. ) 
 CURVE ( )  GEOMETRIC_REPRESENTATION_ITEM ( )  RATIONAL_B_SPLINE_CURVE ( ( 0.9755282581475768211, 0.9755282581475768211, 1.000000000000000000, 0.9510565162951535312, 1.000000000000000000, 0.9510565162951535312, 1.000000000000000000, 0.9510565162951535312, 1.000000000000000000, 0.9510565162951535312, 1.000000000000000000, 0.9755282581475768211, 0.9755282581475768211 ) ) 
 REPRESENTATION_ITEM ( '' )  );
#4063=CARTESIAN_POINT ( 'NONE',  ( -10.92172942406178926, -7.369999999999994778, -7.935100905948389460 ) ) ;
#4068=FACE_OUTER_BOUND ( 'NONE', #6557, .T. ) ;
#4072=CARTESIAN_POINT ( 'NONE',  ( -3.708203932499367195, 9.196025403784441110, -11.41267819554184548 ) ) ;
#4073=DIRECTION ( 'NONE',  ( 0.000000000000000000, 1.000000000000000000, 0.000000000000000000 ) ) ;
#4074=CARTESIAN_POINT ( 'NONE',  ( -7.416407864998739718, 4.513974596215559743, 10.20780970022447853 ) ) ;
#4083=CARTESIAN_POINT ( 'NONE',  ( 10.92172942406178926, 12.13000000000000256, 7.935100905948385908 ) ) ;
#4084=ORIENTED_EDGE ( 'NONE', *, *, #14767, .T. ) ;
#4089=CARTESIAN_POINT ( 'NONE',  ( -10.92172942406178926, 14.63000000000000433, -7.935100905948389460 ) ) ;
#4090=ADVANCED_FACE ( 'NONE', ( #11063 ), #4339, .F. ) ;
#4097=CARTESIAN_POINT ( 'NONE',  ( 0.3512640400060710877, 8.055266896996085890, -18.02316420754752713 ) ) ;
#4101=CARTESIAN_POINT ( 'NONE',  ( 10.92172942406178926, 6.129999999999996341, 7.935100905948385908 ) ) ;
#4104=DIRECTION ( 'NONE',  ( -0.000000000000000000, -1.000000000000000000, -0.000000000000000000 ) ) ;
#4105=ORIENTED_EDGE ( 'NONE', *, *, #9055, .F. ) ;
#4106=CARTESIAN_POINT ( 'NONE',  ( 11.76794919243112325, 23.28000000000000114, 3.823638476888996163 ) ) ;
#4108=AXIS2_PLACEMENT_3D ( 'NONE', #14580, #3813, #2550 ) ;
#4122=CARTESIAN_POINT ( 'NONE',  ( 0.000000000000000000, 9.000000000000000000, 0.000000000000000000 ) ) ;
#4125=ORIENTED_EDGE ( 'NONE', *, *, #1840, .T. ) ;
#4127=CARTESIAN_POINT ( 'NONE',  ( 2.621994543952811015E-15, 20.17999999999999261, -14.19474002721660355 ) ) ;
#4132=CARTESIAN_POINT ( 'NONE',  ( 7.272992578804311492, -9.120000000000004547, -10.01041549318726709 ) ) ;
#4134=CARTESIAN_POINT ( 'NONE',  ( 13.49999999999999822, -13.72000000000000419, 4.386415899144237684 ) ) ;
#4145=CARTESIAN_POINT ( 'NONE',  ( -7.272992578804310604, 13.37999999999999012, 10.01041549318726709 ) ) ;
#4146=CARTESIAN_POINT ( 'NONE',  ( -8.891200544363830713E-16, 1.546025403784439423, 12.00000000000000000 ) ) ;
#4149=CARTESIAN_POINT ( 'NONE',  ( -11.76794919243112325, 0.7799999999999955858, -3.823638476888998827 ) ) ;
#4152=CARTESIAN_POINT ( 'NONE',  ( 4.171729424061791924, -10.96999999999999353, -12.83926296998457239 ) ) ;
#4160=CARTESIAN_POINT ( 'NONE',  ( 0.000000000000000000, 9.000000000000000000, 0.000000000000000000 ) ) ;
#4161=APPLICATION_CONTEXT ( 'automotive_design' ) ;
#4162=CARTESIAN_POINT ( 'NONE',  ( -22.26879735319533893, 6.548268786306344680, 7.999999999999786837 ) ) ;
#4163=DIRECTION ( 'NONE',  ( -0.8660254037844393737, -0.000000000000000000, 0.4999999999999986122 ) ) ;
#4165=EDGE_CURVE ( 'NONE', #16001, #14960, #14783, .T. ) ;
#4171=CARTESIAN_POINT ( 'NONE',  ( -12.00000000000000178, 3.946025403784445551, 3.899036354794875869 ) ) ;
#4173=CARTESIAN_POINT ( 'NONE',  ( -10.92172942406179104, 11.23000000000000398, 7.935100905948385908 ) ) ;
#4174=ORIENTED_EDGE ( 'NONE', *, *, #16694, .F. ) ;
#4179=CARTESIAN_POINT ( 'NONE',  ( -8.343458848123576743, 11.48000000000000398, -11.48378591275254301 ) ) ;
#4189=CIRCLE ( 'NONE', #9569, 26.00000000000000355 ) ;
#4190=CARTESIAN_POINT ( 'NONE',  ( -5.733944026526732074, 10.00000000000000000, -11.46105073991378376 ) ) ;
#4195=CARTESIAN_POINT ( 'NONE',  ( 1.775737858763662015E-15, 9.000000000000000000, 14.50000000000000000 ) ) ;
#4196=CARTESIAN_POINT ( 'NONE',  ( -9.999999999999776179, 7.983052681820796970, -15.32050807568890427 ) ) ;
#4199=VERTEX_POINT ( 'NONE', #7072 ) ;
#4201=CARTESIAN_POINT ( 'NONE',  ( -7.272992578804307939, -14.51999999999999957, -10.01041549318726886 ) ) ;
#4211=VECTOR ( 'NONE', #11830, 1000.000000000000114 ) ;
#4217=CARTESIAN_POINT ( 'NONE',  ( -1.732050807569007977, 0.000000000000000000, 18.99999999999998224 ) ) ;
#4220=DIRECTION ( 'NONE',  ( -0.8660254037844434816, 0.000000000000000000, 0.4999999999999918399 ) ) ;
#4221=CARTESIAN_POINT ( 'NONE',  ( 4.171729424061791924, -12.96999999999999531, -12.83926296998457239 ) ) ;
#4225=ADVANCED_FACE ( 'NONE', ( #340 ), #5749, .F. ) ;
#4228=DIRECTION ( 'NONE',  ( -0.000000000000000000, -1.000000000000000000, -0.000000000000000000 ) ) ;
#4231=CONICAL_SURFACE ( 'NONE', #16932, 14.50000000000000000, 1.308996938995753867 ) ;
#4238=DIRECTION ( 'NONE',  ( 0.000000000000000000, 1.000000000000000000, 0.000000000000000000 ) ) ;
#4239=CARTESIAN_POINT ( 'NONE',  ( 10.92172942406179104, 4.730000000000011973, -7.935100905948385908 ) ) ;
#4241=CARTESIAN_POINT ( 'NONE',  ( -9.520470885617715595, 6.629999999999997229, -6.917026985038136289 ) ) ;
#4243=CARTESIAN_POINT ( 'NONE',  ( 10.92172942406179104, -17.26999999999999957, -7.935100905948385908 ) ) ;
#4247=EDGE_CURVE ( 'NONE', #17099, #2562, #5839, .T. ) ;
#4263=CARTESIAN_POINT ( 'NONE',  ( 10.92172942406178926, 9.129999999999999005, 7.935100905948385908 ) ) ;
#4268=CARTESIAN_POINT ( 'NONE',  ( 13.49999999999999822, 7.279999999999994031, 4.386415899144237684 ) ) ;
#4277=CARTESIAN_POINT ( 'NONE',  ( -19.29752010712827826, 5.918584287042170544, -17.42428528562878398 ) ) ;
#4281=CARTESIAN_POINT ( 'NONE',  ( 4.171729424061791924, 7.030000000000008242, -12.83926296998457239 ) ) ;
#4283=CARTESIAN_POINT ( 'NONE',  ( -10.99999999999979394, 7.773118517290098950, -15.58845726812003996 ) ) ;
#4284=CARTESIAN_POINT ( 'NONE',  ( 0.000000000000000000, 9.999999999999998224, 0.000000000000000000 ) ) ;
#4285=CARTESIAN_POINT ( 'NONE',  ( 7.272992578804308828, 22.98000000000001108, 10.01041549318726709 ) ) ;
#4286=ORIENTED_EDGE ( 'NONE', *, *, #13269, .F. ) ;
#4288=EDGE_LOOP ( 'NONE', ( #10045, #3409, #1423, #7450 ) ) ;
#4289=CARTESIAN_POINT ( 'NONE',  ( 3.636496289402157078, -14.96999999999999709, -11.19198476289190936 ) ) ;
#4292=CARTESIAN_POINT ( 'NONE',  ( 2.445080149700053643E-15, 1.180000000000002602, -13.50000000000000000 ) ) ;
#4309=CARTESIAN_POINT ( 'NONE',  ( 13.49999999999999822, -19.72000000000000597, 4.386415899144237684 ) ) ;
#4313=ADVANCED_FACE ( 'NONE', ( #2492 ), #7749, .F. ) ;
#4319=CARTESIAN_POINT ( 'NONE',  ( 9.708203932499369415, 4.996025403784432939, 7.053423027509680310 ) ) ;
#4324=AXIS2_PLACEMENT_3D ( 'NONE', #13601, #5321, #1496 ) ;
#4325=CARTESIAN_POINT ( 'NONE',  ( -12.86241927028127385, 0.1170935115772343549, 5.263970488369911216 ) ) ;
#4326=DIRECTION ( 'NONE',  ( 0.000000000000000000, 0.000000000000000000, -1.000000000000000000 ) ) ;
#4328=CARTESIAN_POINT ( 'NONE',  ( 13.49999999999999822, 31.28000000000000824, 4.386415899144237684 ) ) ;
#4329=CARTESIAN_POINT ( 'NONE',  ( 11.76794919243112325, -6.720000000000000639, 3.823638476888996163 ) ) ;
#4331=CARTESIAN_POINT ( 'NONE',  ( -13.50000000000000000, 1.930000000000015037, -3.469446951953614189E-15 ) ) ;
#4332=CARTESIAN_POINT ( 'NONE',  ( 7.999999999999850786, 5.918584287042170544, 24.73863375370601858 ) ) ;
#4335=DIRECTION ( 'NONE',  ( 0.000000000000000000, 0.000000000000000000, 1.000000000000000000 ) ) ;
#4339=CYLINDRICAL_SURFACE ( 'NONE', #10353, 1.999999999999998224 ) ;
#4340=CARTESIAN_POINT ( 'NONE',  ( -13.49999999999999822, 5.080000000000005400, 4.386415899144235020 ) ) ;
#4341=CARTESIAN_POINT ( 'NONE',  ( -12.00000000000002842, 0.9139745962155733094, -3.899036354794888304 ) ) ;
#4345=CARTESIAN_POINT ( 'NONE',  ( -18.85009555739750198, 7.815224737767797691, 1.645503437279392855 ) ) ;
#4347=ORIENTED_EDGE ( 'NONE', *, *, #773, .T. ) ;
#4351=CARTESIAN_POINT ( 'NONE',  ( 2.621994543952811015E-15, 7.179999999999997939, -14.19474002721660355 ) ) ;
#4352=VERTEX_POINT ( 'NONE', #15667 ) ;
#4356=CARTESIAN_POINT ( 'NONE',  ( 4.171729424061791924, 2.030000000000003801, -12.83926296998457239 ) ) ;
#4363=B_SPLINE_CURVE_WITH_KNOTS ( 'NONE', 3,
 ( #685, #6260, #6098, #16854, #10162, #15511, #14359, #8839, #11647, #4928, #14196, #7327, #2078, #10329, #11732, #16016, #15683, #7503 ),
 .UNSPECIFIED., .F., .F.,
 ( 4, 2, 2, 2, 2, 2, 2, 2, 4 ),
 ( 2.344023999658286050E-07, 0.0005273255500080976975, 0.001054416697616229618, 0.001581507845224361646, 0.002108598992832493458, 0.002635690140440625270, 0.003162781288048757081, 0.003689872435656888026, 0.004216963583265019404 ),
 .UNSPECIFIED. ) ;
#4366=B_SPLINE_CURVE_WITH_KNOTS ( 'NONE', 3,
 ( #2401, #14691, #1096, #13377, #17267, #5179, #1185, #6595, #11975, #3925, #2578, #1266, #4190, #15123, #14859, #8362, #11003, #16374, #9514, #5622, #9689, #12504, #8186, #13719, #476, #9603, #3021, #2754 ),
 .UNSPECIFIED., .F., .F.,
 ( 4, 2, 2, 2, 2, 2, 2, 2, 2, 2, 2, 2, 2, 4 ),
 ( 8.328931132934574426E-17, 0.002882167905697472030, 0.004323251858546166629, 0.005764335811394859926, 0.008646503717092248256, 0.01008758766994094329, 0.01152867162278963659, 0.01296975557563833509, 0.01441083952848702665, 0.01729300743418441325, 0.01873409138703310481, 0.02017517533988179290, 0.02161625929273048100, 0.02305734324557916909 ),
 .UNSPECIFIED. ) ;
#4371=CLOSED_SHELL ( 'NONE', ( #8446, #12472, #17195, #9573, #3177, #5585, #9260, #7781, #16869, #15779, #7854, #1997, #8526, #17373, #2752, #15722, #10424, #12008, #6918, #11838, #8321, #6145, #6164, #98, #404, #5607, #14720, #8358, #3333, #12597, #1565, #6899, #951, #5287, #1688, #4313, #12985, #9740, #16893, #16293, #3523, #6753, #14861, #1613, #5134, #14745, #4225, #15658, #13386, #14527, #13034, #1207, #1883, #7395, #9, #5266, #7953, #2446, #4389, #4090, #15287, #1298, #8860, #14428, #12556, #5159, #17152, #6876, #7192, #11660, #355, #1341, #14050, #810, #3055 ) ) ;
#4373=DIRECTION ( 'NONE',  ( 1.182917971378672060E-16, -0.2588190451025143002, 0.9659258262890700886 ) ) ;
#4378=ORIENTED_EDGE ( 'NONE', *, *, #7024, .F. ) ;
#4379=CARTESIAN_POINT ( 'NONE',  ( -9.520470885617717371, -16.76999999999999957, 6.917026985038133624 ) ) ;
#4382=FACE_OUTER_BOUND ( 'NONE', #9066, .T. ) ;
#4389=ADVANCED_FACE ( 'NONE', ( #6598 ), #3841, .F. ) ;
#4390=ORIENTED_EDGE ( 'NONE', *, *, #2530, .F. ) ;
#4391=CARTESIAN_POINT ( 'NONE',  ( 15.31970530204987035, 8.007293614239921808, -9.835827272001340660 ) ) ;
#4394=VERTEX_POINT ( 'NONE', #7838 ) ;
#4396=CARTESIAN_POINT ( 'NONE',  ( -10.99999999999979394, 0.000000000000000000, -15.58845726812003996 ) ) ;
#4400=CARTESIAN_POINT ( 'NONE',  ( -8.343458848123582072, -14.62000000000000277, 11.48378591275254124 ) ) ;
#4401=AXIS2_PLACEMENT_3D ( 'NONE', #3802, #7968, #12103 ) ;
#4405=CARTESIAN_POINT ( 'NONE',  ( 5.883989548015875926, -19.07073847365937169, 10.19133431864935879 ) ) ;
#4408=CARTESIAN_POINT ( 'NONE',  ( 11.76794919243112325, -3.720000000000000195, 3.823638476888996163 ) ) ;
#4411=DIRECTION ( 'NONE',  ( -0.000000000000000000, -1.000000000000000000, -0.000000000000000000 ) ) ;
#4414=CIRCLE ( 'NONE', #13430, 26.00000000000000355 ) ;
#4418=DIRECTION ( 'NONE',  ( 0.000000000000000000, 1.000000000000000000, 0.000000000000000000 ) ) ;
#4420=CARTESIAN_POINT ( 'NONE',  ( 10.92172942406179104, 31.73000000000000753, -7.935100905948385908 ) ) ;
#4421=CARTESIAN_POINT ( 'NONE',  ( -9.520470885617717371, -10.76999999999999424, 6.917026985038133624 ) ) ;
#4423=CARTESIAN_POINT ( 'NONE',  ( 1.876532330890708260E-11, 6.313974596214807278, -12.00000000000000355 ) ) ;
#4432=LINE ( 'NONE', #12382, #11826 ) ;
#4439=CARTESIAN_POINT ( 'NONE',  ( -9.520470885617717371, 22.23000000000000043, 6.917026985038133624 ) ) ;
#4440=ORIENTED_EDGE ( 'NONE', *, *, #15340, .F. ) ;
#4442=CARTESIAN_POINT ( 'NONE',  ( -1.900613283894436512, 4.469143981464173798, 12.00000000000000000 ) ) ;
#4444=CARTESIAN_POINT ( 'NONE',  ( 10.92172942406179104, 6.730000000000013749, -7.935100905948385908 ) ) ;
#4445=ORIENTED_EDGE ( 'NONE', *, *, #16392, .T. ) ;
#4449=CARTESIAN_POINT ( 'NONE',  ( 13.50000000000000355, 1.579999999999999405, -4.386415899144233244 ) ) ;
#4456=EDGE_CURVE ( 'NONE', #9433, #4352, #9807, .T. ) ;
#4458=CARTESIAN_POINT ( 'NONE',  ( 3.708203932499387179, 7.963974596215601665, 11.41267819554190055 ) ) ;
#4459=CARTESIAN_POINT ( 'NONE',  ( 24.73863375370598305, 0.000000000000000000, -7.999999999999934275 ) ) ;
#4465=LINE ( 'NONE', #13810, #11372 ) ;
#4467=CARTESIAN_POINT ( 'NONE',  ( -3.636496289402156190, 25.52999999999999758, 11.19198476289190758 ) ) ;
#4470=EDGE_LOOP ( 'NONE', ( #10849, #2495, #13382, #8806, #17363 ) ) ;
#4471=CARTESIAN_POINT ( 'NONE',  ( 11.76794919243112325, -15.57000000000000028, 1.734723475976807094E-15 ) ) ;
#4474=CARTESIAN_POINT ( 'NONE',  ( 13.49999999999999822, 0.2799999999999969180, 4.386415899144236796 ) ) ;
#4486=CARTESIAN_POINT ( 'NONE',  ( 0.000000000000000000, 5.918584287042170544, 0.000000000000000000 ) ) ;
#4489=CARTESIAN_POINT ( 'NONE',  ( 10.92172942406178926, -16.86999999999999744, 7.935100905948385908 ) ) ;
#4498=CARTESIAN_POINT ( 'NONE',  ( 11.76794919243112680, -3.420000000000002593, -3.823638476888993942 ) ) ;
#4500=CARTESIAN_POINT ( 'NONE',  ( 12.00000000000002665, 2.563974596215591983, 1.734723475976807094E-15 ) ) ;
#4505=CARTESIAN_POINT ( 'NONE',  ( -2.138187132794193701, 0.6031186787740299149, 13.50000091354000809 ) ) ;
#4506=CARTESIAN_POINT ( 'NONE',  ( -7.416407864998736166, 0.3460254037844350261, -10.20780970022448031 ) ) ;
#4507=CARTESIAN_POINT ( 'NONE',  ( -1.003751346110120011E-07, 3.679997203684337137, 13.49999999999999822 ) ) ;
#4508=CARTESIAN_POINT ( 'NONE',  ( -4.171729424061787483, 29.32999999999999474, -12.83926296998457417 ) ) ;
#4509=CARTESIAN_POINT ( 'NONE',  ( 11.76794919243112325, -9.569999999999994955, 1.734723475976807094E-15 ) ) ;
#4511=CARTESIAN_POINT ( 'NONE',  ( 7.999999999999868550, 6.548268786306342903, 22.26879735319531761 ) ) ;
#4520=CARTESIAN_POINT ( 'NONE',  ( -17.32050807568867512, 0.000000000000000000, -8.000000000000207834 ) ) ;
#4525=CARTESIAN_POINT ( 'NONE',  ( -11.76794919243112325, 18.78000000000001180, -3.823638476888998827 ) ) ;
#4526=VERTEX_POINT ( 'NONE', #9344 ) ;
#4530=CARTESIAN_POINT ( 'NONE',  ( -4.171729424061787483, 10.33000000000000540, -12.83926296998457417 ) ) ;
#4531=ORIENTED_EDGE ( 'NONE', *, *, #11260, .T. ) ;
#4533=CARTESIAN_POINT ( 'NONE',  ( -25.42428528562849266, 5.918584287042170544, -5.441113646577749208 ) ) ;
#4534=CARTESIAN_POINT ( 'NONE',  ( -8.549982208541774191E-16, 3.680000000000005933, 14.19474002721660355 ) ) ;
#4537=AXIS2_PLACEMENT_3D ( 'NONE', #888, #14146, #11432 ) ;
#4545=CARTESIAN_POINT ( 'NONE',  ( -7.999999999999670486, 0.000000000000000000, -24.73863375370606477 ) ) ;
#4546=CARTESIAN_POINT ( 'NONE',  ( 1.732050807568739970, 7.773118517290100726, 19.00000000000000355 ) ) ;
#4551=CARTESIAN_POINT ( 'NONE',  ( -10.56248930388449558, 10.00000000000000000, 5.855161195429291254 ) ) ;
#4553=CARTESIAN_POINT ( 'NONE',  ( -7.409984580736203970E-16, 25.67999999999999616, 12.37355403259654985 ) ) ;
#4554=VERTEX_POINT ( 'NONE', #3667 ) ;
#4569=AXIS2_PLACEMENT_3D ( 'NONE', #9017, #6365, #1128 ) ;
#4570=CARTESIAN_POINT ( 'NONE',  ( -8.000000000000145661, 0.000000000000000000, 17.32050807568870709 ) ) ;
#4574=CARTESIAN_POINT ( 'NONE',  ( -15.43600950528680116, 7.854010657973331533, 10.69176227072916951 ) ) ;
#4575=PLANE ( 'NONE',  #6498 ) ;
#4578=CARTESIAN_POINT ( 'NONE',  ( -7.272992578804307939, 27.48000000000001108, -10.01041549318726886 ) ) ;
#4583=AXIS2_PLACEMENT_3D ( 'NONE', #6540, #6274, #17213 ) ;
#4585=CARTESIAN_POINT ( 'NONE',  ( -11.76794919243112325, -5.069999999999998508, -2.602085213965210642E-15 ) ) ;
#4588=B_SPLINE_CURVE_WITH_KNOTS ( 'NONE', 3,
 ( #9693, #9781, #4551, #8278, #1533, #9870, #15220, #6949, #11096, #1793, #15128, #12327, #7039, #7204, #9956, #12590, #479, #5626, #11007, #3209, #1876, #16378, #12417, #12237, #5714, #8887 ),
 .UNSPECIFIED., .F., .F.,
 ( 4, 2, 2, 2, 2, 2, 2, 2, 2, 2, 2, 2, 4 ),
 ( 0.003287795359550850938, 0.004729367074732778939, 0.006170938789914706506, 0.007612510505096635807, 0.009054082220278565976, 0.01193722565064242458, 0.01337879736582435475, 0.01482036908100628665, 0.01626194079618821509, 0.01770351251137014525, 0.02058665594173400559, 0.02346979937209786593, 0.02635294280246172627 ),
 .UNSPECIFIED. ) ;
#4592=CARTESIAN_POINT ( 'NONE',  ( -10.92172942406179104, 0.2300000000000079758, 7.935100905948385908 ) ) ;
#4593=CARTESIAN_POINT ( 'NONE',  ( 8.061801495184115041, 7.889711263303322397, -16.81068189100985322 ) ) ;
#4594=CARTESIAN_POINT ( 'NONE',  ( 13.50000000000000355, 31.57999999999999474, -4.386415899144233244 ) ) ;
#4595=CARTESIAN_POINT ( 'NONE',  ( 2.279995255611139653E-15, -5.820000000000007390, -12.37355403259654985 ) ) ;
#4598=CARTESIAN_POINT ( 'NONE',  ( 9.708203932499369415, 5.263974596215557966, 7.053423027509680310 ) ) ;
#4612=CARTESIAN_POINT ( 'NONE',  ( -3.636496289402152637, 21.33000000000001606, -11.19198476289190936 ) ) ;
#4613=ORIENTED_EDGE ( 'NONE', *, *, #7633, .T. ) ;
#4617=CARTESIAN_POINT ( 'NONE',  ( -13.49999999999999822, 5.080000000000005400, 4.386415899144235908 ) ) ;
#4621=CARTESIAN_POINT ( 'NONE',  ( -13.49999999999999822, 5.779999999999998472, -4.386415899144240349 ) ) ;
#4631=CARTESIAN_POINT ( 'NONE',  ( -12.00000000000000178, 6.913974596215557433, -3.899036354794879866 ) ) ;
#4638=VERTEX_POINT ( 'NONE', #15934 ) ;
#4642=CARTESIAN_POINT ( 'NONE',  ( 13.50000000000000355, 30.57999999999999829, -4.386415899144233244 ) ) ;
#4648=VECTOR ( 'NONE', #15524, 1000.000000000000000 ) ;
#4655=EDGE_LOOP ( 'NONE', ( #12526, #13284, #11422, #2347 ) ) ;
#4658=CARTESIAN_POINT ( 'NONE',  ( -10.92172942406178926, 17.63000000000000611, -7.935100905948389460 ) ) ;
#4662=LINE ( 'NONE', #15420, #7352 ) ;
#4665=CARTESIAN_POINT ( 'NONE',  ( -9.520470885617717371, 28.23000000000000398, 6.917026985038133624 ) ) ;
#4669=CARTESIAN_POINT ( 'NONE',  ( -11.76794919243112325, -14.06999999999999851, -2.602085213965210642E-15 ) ) ;
#4671=DIRECTION ( 'NONE',  ( -0.4999999999999953371, -0.000000000000000000, -0.8660254037844413721 ) ) ;
#4672=EDGE_CURVE ( 'NONE', #6684, #4811, #4707, .T. ) ;
#4673=CARTESIAN_POINT ( 'NONE',  ( 9.520470885617717371, -0.2699999999999924682, -6.917026985038131848 ) ) ;
#4676=CARTESIAN_POINT ( 'NONE',  ( -13.49999999999999822, 4.780000000000000249, -4.386415899144240349 ) ) ;
#4680=LINE ( 'NONE', #8760, #9318 ) ;
#4681=CARTESIAN_POINT ( 'NONE',  ( 0.000000000000000000, 0.000000000000000000, 0.000000000000000000 ) ) ;
#4682=CARTESIAN_POINT ( 'NONE',  ( 4.171729424061791924, 26.02999999999999758, -12.83926296998457239 ) ) ;
#4683=CARTESIAN_POINT ( 'NONE',  ( 7.272992578804311492, -6.120000000000004547, -10.01041549318726709 ) ) ;
#4686=CARTESIAN_POINT ( 'NONE',  ( 1.469576158976824144E-15, 9.000000000000000000, 12.00000000000000178 ) ) ;
#4692=CARTESIAN_POINT ( 'NONE',  ( -1.732050807568877859, 0.000000000000000000, -18.99999999999999645 ) ) ;
#4695=DIRECTION ( 'NONE',  ( 0.000000000000000000, -0.000000000000000000, 1.000000000000000000 ) ) ;
#4699=CARTESIAN_POINT ( 'NONE',  ( 11.76794919243112680, 20.58000000000001251, -3.823638476888993942 ) ) ;
#4704=CARTESIAN_POINT ( 'NONE',  ( -8.549982208541774191E-16, -0.3199999999999986189, 14.19474002721660355 ) ) ;
#4707=CIRCLE ( 'NONE', #8111, 13.50000000000000000 ) ;
#4710=DIRECTION ( 'NONE',  ( -0.000000000000000000, 1.000000000000000000, -0.000000000000000000 ) ) ;
#4712=CARTESIAN_POINT ( 'NONE',  ( 4.171729424061791924, 8.030000000000010019, -12.83926296998457239 ) ) ;
#4716=EDGE_CURVE ( 'NONE', #1168, #201, #14556, .T. ) ;
#4717=CARTESIAN_POINT ( 'NONE',  ( 0.8575635061788081659, 8.007388461842865013, 18.18484536092594439 ) ) ;
#4720=VECTOR ( 'NONE', #759, 1000.000000000000000 ) ;
#4723=CARTESIAN_POINT ( 'NONE',  ( 0.5701897248585299227, 0.02296074491301186918, -12.00000000000000178 ) ) ;
#4725=ORIENTED_EDGE ( 'NONE', *, *, #1110, .T. ) ;
#4728=ORIENTED_EDGE ( 'NONE', *, *, #10160, .F. ) ;
#4729=CARTESIAN_POINT ( 'NONE',  ( 13.49999999999999822, 30.28000000000000824, 4.386415899144237684 ) ) ;
#4732=CARTESIAN_POINT ( 'NONE',  ( 8.000000000000019540, 0.000000000000000000, -24.73863375370596174 ) ) ;
#4740=EDGE_LOOP ( 'NONE', ( #7905, #5628, #11657, #7729 ) ) ;
#4741=FACE_OUTER_BOUND ( 'NONE', #11113, .T. ) ;
#4743=DIRECTION ( 'NONE',  ( 0.000000000000000000, 0.000000000000000000, -1.000000000000000000 ) ) ;
#4748=PLANE ( 'NONE',  #10698 ) ;
#4751=CARTESIAN_POINT ( 'NONE',  ( 3.636496289402157078, 33.03000000000000114, -11.19198476289190936 ) ) ;
#4754=CARTESIAN_POINT ( 'NONE',  ( -11.76794919243112325, -14.22000000000000242, -3.823638476888998827 ) ) ;
#4757=DIRECTION ( 'NONE',  ( 0.000000000000000000, 0.000000000000000000, -1.000000000000000000 ) ) ;
#4758=CARTESIAN_POINT ( 'NONE',  ( 2.279995255611139653E-15, -2.819999999999999840, -12.37355403259654985 ) ) ;
#4761=CARTESIAN_POINT ( 'NONE',  ( 0.000000000000000000, 30.93000000000001393, 0.000000000000000000 ) ) ;
#4762=AXIS2_PLACEMENT_3D ( 'NONE', #7420, #10077, #4757 ) ;
#4764=CARTESIAN_POINT ( 'NONE',  ( 11.00000000000001599, 0.000000000000000000, -15.58845726811988364 ) ) ;
#4766=CARTESIAN_POINT ( 'NONE',  ( -5.441113646577473872, 5.918584287042170544, -25.42428528562855305 ) ) ;
#4767=CARTESIAN_POINT ( 'NONE',  ( 4.171729424061789260, 27.82999999999999474, 12.83926296998457239 ) ) ;
#4773=EDGE_CURVE ( 'NONE', #6360, #1191, #12506, .T. ) ;
#4775=AXIS2_PLACEMENT_3D ( 'NONE', #6762, #9511, #2928 ) ;
#4782=CARTESIAN_POINT ( 'NONE',  ( 18.99999999999999289, 0.000000000000000000, 1.732050807568941586 ) ) ;
#4784=DIRECTION ( 'NONE',  ( -0.000000000000000000, 1.000000000000000000, -0.000000000000000000 ) ) ;
#4787=CARTESIAN_POINT ( 'NONE',  ( 7.272992578804308828, 16.98000000000000753, 10.01041549318726709 ) ) ;
#4792=CARTESIAN_POINT ( 'NONE',  ( -4.171729424061787483, 1.329999999999997851, -12.83926296998457417 ) ) ;
#4793=CARTESIAN_POINT ( 'NONE',  ( -7.272992578804310604, 31.38000000000002032, 10.01041549318726709 ) ) ;
#4811=VERTEX_POINT ( 'NONE', #13549 ) ;
#4813=CARTESIAN_POINT ( 'NONE',  ( -13.49999999999999822, 29.08000000000000185, 4.386415899144235908 ) ) ;
#4826=VERTEX_POINT ( 'NONE', #4015 ) ;
#4828=ORIENTED_EDGE ( 'NONE', *, *, #14194, .F. ) ;
#4837=CARTESIAN_POINT ( 'NONE',  ( 11.76794919243112680, 32.58000000000001251, -3.823638476888993942 ) ) ;
#4840=LINE ( 'NONE', #17024, #14619 ) ;
#4844=CARTESIAN_POINT ( 'NONE',  ( -8.343458848123582072, 5.379999999999995453, 11.48378591275253768 ) ) ;
#4847=CARTESIAN_POINT ( 'NONE',  ( -24.73863375370587292, 0.000000000000000000, -8.000000000000280664 ) ) ;
#4848=CARTESIAN_POINT ( 'NONE',  ( 8.000000000000023093, 7.773118517290098062, -17.32050807568876394 ) ) ;
#4849=CARTESIAN_POINT ( 'NONE',  ( -13.50000000000000000, 23.93000000000000682, -3.469446951953614189E-15 ) ) ;
#4852=CARTESIAN_POINT ( 'NONE',  ( -15.28534784291415249, 6.548267719634618622, 18.06260399879734990 ) ) ;
#4854=EDGE_CURVE ( 'NONE', #1275, #15564, #11760, .T. ) ;
#4859=VECTOR ( 'NONE', #16544, 1000.000000000000000 ) ;
#4867=VECTOR ( 'NONE', #8986, 1000.000000000000000 ) ;
#4871=CARTESIAN_POINT ( 'NONE',  ( -7.272992578804310604, 16.37999999999999901, 10.01041549318726709 ) ) ;
#4876=CARTESIAN_POINT ( 'NONE',  ( 8.343458848123583849, -2.120000000000000107, -11.48378591275253768 ) ) ;
#4877=CARTESIAN_POINT ( 'NONE',  ( 7.272992578804308828, 28.98000000000000398, 10.01041549318726709 ) ) ;
#4878=LINE ( 'NONE', #3280, #1451 ) ;
#4880=FACE_OUTER_BOUND ( 'NONE', #18, .T. ) ;
#4886=CARTESIAN_POINT ( 'NONE',  ( -18.99999999999998224, 0.000000000000000000, -1.732050807569074369 ) ) ;
#4892=CARTESIAN_POINT ( 'NONE',  ( 18.06260399879750267, 6.548267719634618622, -15.28534784291396420 ) ) ;
#4895=ORIENTED_EDGE ( 'NONE', *, *, #1840, .F. ) ;
#4898=( BOUNDED_CURVE ( )  B_SPLINE_CURVE ( 2, ( #9671, #4442, #13530, #5512, #12394, #4171, #14934, #15196, #2826, #8257, #3096, #12304, #13618 ),
 .UNSPECIFIED., .F., .F. ) 
 B_SPLINE_CURVE_WITH_KNOTS ( ( 3, 2, 2, 2, 2, 2, 3 ),
 ( 0.5416666666666666297, 0.5444444444444443976, 0.5500000000000000444, 0.5555555555555555802, 0.5611111111111111160, 0.5666666666666666519, 0.5694444444444444198 ),
 .UNSPECIFIED. ) 
 CURVE ( )  GEOMETRIC_REPRESENTATION_ITEM ( )  RATIONAL_B_SPLINE_CURVE ( ( 0.9755282581475768211, 0.9755282581475768211, 1.000000000000000000, 0.9510565162951535312, 1.000000000000000000, 0.9510565162951535312, 1.000000000000000000, 0.9510565162951535312, 1.000000000000000000, 0.9510565162951535312, 1.000000000000000000, 0.9755282581475768211, 0.9755282581475768211 ) ) 
 REPRESENTATION_ITEM ( '' )  );
#4901=CARTESIAN_POINT ( 'NONE',  ( 4.171729424061791924, 34.03000000000000114, -12.83926296998457239 ) ) ;
#4911=EDGE_CURVE ( 'NONE', #16538, #9933, #5971, .T. ) ;
#4912=LINE ( 'NONE', #15579, #9402 ) ;
#4917=DIRECTION ( 'NONE',  ( 0.000000000000000000, 0.000000000000000000, 1.000000000000000000 ) ) ;
#4918=ORIENTED_EDGE ( 'NONE', *, *, #3850, .T. ) ;
#4923=CARTESIAN_POINT ( 'NONE',  ( 15.34492079894891603, 7.924935932049796072, 10.35602470258067953 ) ) ;
#4925=FACE_OUTER_BOUND ( 'NONE', #5648, .T. ) ;
#4928=CARTESIAN_POINT ( 'NONE',  ( 17.99988701463195184, 8.062211464643718628, 0.1761320247422976937 ) ) ;
#4932=EDGE_CURVE ( 'NONE', #5443, #4826, #7551, .T. ) ;
#4936=CARTESIAN_POINT ( 'NONE',  ( 10.00000000000135891, 7.983052681821872554, -15.32050807568352191 ) ) ;
#4937=CIRCLE ( 'NONE', #12839, 26.00000000000000355 ) ;
#4940=CARTESIAN_POINT ( 'NONE',  ( 9.335235950531815854E-15, 8.180000000000005045, -13.50000000000000178 ) ) ;
#4943=CARTESIAN_POINT ( 'NONE',  ( 8.000000000000023093, 7.773118517290098062, -17.32050807568876394 ) ) ;
#4945=CARTESIAN_POINT ( 'NONE',  ( -4.171729424061791036, -2.469999999999999751, 12.83926296998457239 ) ) ;
#4951=EDGE_CURVE ( 'NONE', #15482, #8209, #13161, .T. ) ;
#4959=CARTESIAN_POINT ( 'NONE',  ( -3.636496289402156190, 13.53000000000001357, 11.19198476289190758 ) ) ;
#4967=AXIS2_PLACEMENT_3D ( 'NONE', #10001, #8674, #16687 ) ;
#4969=CARTESIAN_POINT ( 'NONE',  ( 7.999999999999904965, 0.000000000000000000, 17.32050807568881368 ) ) ;
#4984=CARTESIAN_POINT ( 'NONE',  ( 11.76794919243112680, 2.579999999999996962, -3.823638476888993942 ) ) ;
#4985=ORIENTED_EDGE ( 'NONE', *, *, #6292, .T. ) ;
#4987=ORIENTED_EDGE ( 'NONE', *, *, #6378, .F. ) ;
#4988=CARTESIAN_POINT ( 'NONE',  ( -10.92172942406179104, 29.23000000000000753, 7.935100905948385908 ) ) ;
#4996=CARTESIAN_POINT ( 'NONE',  ( 1.732050807568739970, 7.773118517290100726, 19.00000000000000355 ) ) ;
#4997=AXIS2_PLACEMENT_3D ( 'NONE', #16789, #11152, #4695 ) ;
#4999=CARTESIAN_POINT ( 'NONE',  ( 1.469576158976824144E-15, 9.000000000000000000, 12.00000000000000178 ) ) ;
#5012=CARTESIAN_POINT ( 'NONE',  ( -4.171729424061787483, 5.330000000000001847, -12.83926296998457417 ) ) ;
#5015=B_SPLINE_CURVE_WITH_KNOTS ( 'NONE', 3,
 ( #7345, #15268, #4511, #4332 ),
 .UNSPECIFIED., .F., .F.,
 ( 4, 4 ),
 ( 0.008723199174958473981, 0.01636875612029861649 ),
 .UNSPECIFIED. ) ;
#5020=CARTESIAN_POINT ( 'NONE',  ( -11.76794919243112325, 15.78000000000001535, -3.823638476888998827 ) ) ;
#5025=CARTESIAN_POINT ( 'NONE',  ( -4.171729424061791036, 27.52999999999999758, 12.83926296998457239 ) ) ;
#5026=EDGE_LOOP ( 'NONE', ( #6083, #2238, #3028, #2476 ) ) ;
#5027=CARTESIAN_POINT ( 'NONE',  ( -13.50000000000000000, 8.929999999999992610, -3.469446951953614189E-15 ) ) ;
#5034=CARTESIAN_POINT ( 'NONE',  ( 10.92172942406178926, -10.86999999999999744, 7.935100905948385908 ) ) ;
#5050=CARTESIAN_POINT ( 'NONE',  ( -3.636496289402152637, 9.330000000000005400, -11.19198476289190936 ) ) ;
#5054=CARTESIAN_POINT ( 'NONE',  ( 0.000000000000000000, 9.000000000000000000, -12.00000000000000178 ) ) ;
#5055=CARTESIAN_POINT ( 'NONE',  ( -10.92172942406179104, 2.230000000000009752, 7.935100905948385908 ) ) ;
#5057=CIRCLE ( 'NONE', #9582, 26.00000000000000355 ) ;
#5063=CARTESIAN_POINT ( 'NONE',  ( 2.785879211291982797E-06, 6.680077384874748780, 13.49999999999942979 ) ) ;
#5075=ORIENTED_EDGE ( 'NONE', *, *, #7977, .F. ) ;
#5078=CARTESIAN_POINT ( 'NONE',  ( -3.636496289402156190, 7.530000000000009130, 11.19198476289190758 ) ) ;
#5079=ORIENTED_EDGE ( 'NONE', *, *, #13650, .T. ) ;
#5082=CARTESIAN_POINT ( 'NONE',  ( -8.549982208541774191E-16, 23.68000000000000327, 14.19474002721660355 ) ) ;
#5088=AXIS2_PLACEMENT_3D ( 'NONE', #14325, #11873, #13102 ) ;
#5091=CYLINDRICAL_SURFACE ( 'NONE', #9309, 13.50000000000000000 ) ;
#5098=VERTEX_POINT ( 'NONE', #11239 ) ;
#5105=FACE_OUTER_BOUND ( 'NONE', #131, .T. ) ;
#5114=CARTESIAN_POINT ( 'NONE',  ( 2.279995255611139653E-15, 18.18000000000001393, -12.37355403259654985 ) ) ;
#5120=CARTESIAN_POINT ( 'NONE',  ( 13.50000000000000000, 19.43000000000000327, 1.734723475976807094E-15 ) ) ;
#5121=ORIENTED_EDGE ( 'NONE', *, *, #2507, .T. ) ;
#5126=CARTESIAN_POINT ( 'NONE',  ( -8.343458848123582072, -5.620000000000006324, 11.48378591275254124 ) ) ;
#5134=ADVANCED_FACE ( 'NONE', ( #7176 ), #450, .F. ) ;
#5140=CARTESIAN_POINT ( 'NONE',  ( 11.76794919243112680, 8.579999999999994742, -3.823638476888993942 ) ) ;
#5145=CARTESIAN_POINT ( 'NONE',  ( -8.343458848123582072, -6.619999999999994778, 11.48378591275254124 ) ) ;
#5156=CARTESIAN_POINT ( 'NONE',  ( -3.708203932499366751, 6.463974596215563473, -11.41267819554184193 ) ) ;
#5157=CARTESIAN_POINT ( 'NONE',  ( -3.708203932499369859, 4.663974596215568091, 11.41267819554184193 ) ) ;
#5159=ADVANCED_FACE ( 'NONE', ( #16617 ), #15188, .F. ) ;
#5164=ORIENTED_EDGE ( 'NONE', *, *, #9821, .F. ) ;
#5167=CARTESIAN_POINT ( 'NONE',  ( 7.272992578804308828, 1.980000000000001315, 10.01041549318726709 ) ) ;
#5170=CARTESIAN_POINT ( 'NONE',  ( 8.343458848123578520, 26.98000000000001108, 11.48378591275254124 ) ) ;
#5177=CARTESIAN_POINT ( 'NONE',  ( 4.171729424061791924, 2.030000000000003801, -12.83926296998457239 ) ) ;
#5179=CARTESIAN_POINT ( 'NONE',  ( 0.2312350160357779238, 9.999999999999994671, -13.20992764163158917 ) ) ;
#5190=CARTESIAN_POINT ( 'NONE',  ( -13.50000000000000000, 16.92999999999999972, -3.469446951953614189E-15 ) ) ;
#5202=CARTESIAN_POINT ( 'NONE',  ( -11.76794919243112325, 19.08000000000001606, 3.823638476888994386 ) ) ;
#5206=CARTESIAN_POINT ( 'NONE',  ( -8.549982208541774191E-16, 18.68000000000001393, 14.19474002721660355 ) ) ;
#5208=CARTESIAN_POINT ( 'NONE',  ( -2.138189944381216012, 8.256881422320265784, -13.50000000000000533 ) ) ;
#5209=CARTESIAN_POINT ( 'NONE',  ( -3.636496289402156190, 28.53000000000000114, 11.19198476289190758 ) ) ;
#5213=CARTESIAN_POINT ( 'NONE',  ( -13.49999999999999822, -3.220000000000009077, -4.386415899144240349 ) ) ;
#5214=( BOUNDED_CURVE ( )  B_SPLINE_CURVE ( 2, ( #8327, #13682, #16427, #11230, #6998, #267, #4331, #13941, #5933, #9739, #15085, #8415, #16516 ),
 .UNSPECIFIED., .F., .F. ) 
 B_SPLINE_CURVE_WITH_KNOTS ( ( 3, 2, 2, 2, 2, 2, 3 ),
 ( 0.5972222222222222099, 0.5999999999999999778, 0.6055555555555555136, 0.6111111111111111605, 0.6166666666666666963, 0.6222222222222222321, 0.6250000000000000000 ),
 .UNSPECIFIED. ) 
 CURVE ( )  GEOMETRIC_REPRESENTATION_ITEM ( )  RATIONAL_B_SPLINE_CURVE ( ( 0.9755282581475768211, 0.9755282581475768211, 1.000000000000000000, 0.9510565162951535312, 1.000000000000000000, 0.9510565162951535312, 1.000000000000000000, 0.9510565162951535312, 1.000000000000000000, 0.9510565162951535312, 1.000000000000000000, 0.9755282581475768211, 0.9755282581475768211 ) ) 
 REPRESENTATION_ITEM ( '' )  );
#5227=CARTESIAN_POINT ( 'NONE',  ( -11.76794919243112325, 12.78000000000000824, -3.823638476888998827 ) ) ;
#5230=CARTESIAN_POINT ( 'NONE',  ( 7.272992578804311492, 5.879999999999995453, -10.01041549318726709 ) ) ;
#5234=CARTESIAN_POINT ( 'NONE',  ( -4.171729424061791036, -9.469999999999998863, 12.83926296998457239 ) ) ;
#5239=CARTESIAN_POINT ( 'NONE',  ( 0.000000000000000000, 5.918584287042170544, 0.000000000000000000 ) ) ;
#5250=ORIENTED_EDGE ( 'NONE', *, *, #17010, .F. ) ;
#5253=CARTESIAN_POINT ( 'NONE',  ( -7.409984580736203970E-16, 4.680000000000003268, 12.37355403259654985 ) ) ;
#5254=EDGE_LOOP ( 'NONE', ( #12307, #9674, #10533, #3406 ) ) ;
#5256=ORIENTED_EDGE ( 'NONE', *, *, #9356, .T. ) ;
#5257=CARTESIAN_POINT ( 'NONE',  ( 2.621994543952811015E-15, 19.18000000000001037, -14.19474002721660355 ) ) ;
#5260=AXIS2_PLACEMENT_3D ( 'NONE', #5581, #5842, #8410 ) ;
#5261=CARTESIAN_POINT ( 'NONE',  ( 10.92172942406179104, 10.73000000000000398, -7.935100905948385908 ) ) ;
#5266=ADVANCED_FACE ( 'NONE', ( #11417 ), #16528, .F. ) ;
#5268=DIRECTION ( 'NONE',  ( 0.000000000000000000, 0.000000000000000000, 1.000000000000000000 ) ) ;
#5276=EDGE_LOOP ( 'NONE', ( #15741, #1016, #5537, #4987, #1777 ) ) ;
#5287=ADVANCED_FACE ( 'NONE', ( #16877, #363 ), #8686, .T. ) ;
#5292=CARTESIAN_POINT ( 'NONE',  ( 11.76794919243112680, 20.58000000000001251, -3.823638476888993942 ) ) ;
#5296=CARTESIAN_POINT ( 'NONE',  ( -10.92172942406179104, 21.23000000000000043, 7.935100905948385908 ) ) ;
#5297=ORIENTED_EDGE ( 'NONE', *, *, #9656, .F. ) ;
#5298=LINE ( 'NONE', #1211, #11540 ) ;
#5301=CARTESIAN_POINT ( 'NONE',  ( 3.636496289402157078, -11.96999999999999531, -11.19198476289190936 ) ) ;
#5303=CARTESIAN_POINT ( 'NONE',  ( -8.343458848123576743, -3.519999999999999130, -11.48378591275254301 ) ) ;
#5305=EDGE_CURVE ( 'NONE', #1193, #860, #10100, .T. ) ;
#5315=CARTESIAN_POINT ( 'NONE',  ( 4.171729424061791924, 5.030000000000006466, -12.83926296998457239 ) ) ;
#5316=CARTESIAN_POINT ( 'NONE',  ( -3.636496289402156190, 1.530000000000003579, 11.19198476289190758 ) ) ;
#5320=CARTESIAN_POINT ( 'NONE',  ( 10.92172942406178926, -5.869999999999993001, 7.935100905948385908 ) ) ;
#5321=DIRECTION ( 'NONE',  ( 0.4999999999999925060, 0.000000000000000000, 0.8660254037844430375 ) ) ;
#5329=DIRECTION ( 'NONE',  ( 0.000000000000000000, 0.000000000000000000, 1.000000000000000000 ) ) ;
#5330=CARTESIAN_POINT ( 'NONE',  ( -1.900613283889030392, 4.737093173895517317, 12.00000000000175859 ) ) ;
#5339=VERTEX_POINT ( 'NONE', #11501 ) ;
#5340=ORIENTED_EDGE ( 'NONE', *, *, #3261, .T. ) ;
#5341=CARTESIAN_POINT ( 'NONE',  ( 8.343458848123583849, 24.88000000000000966, -11.48378591275253768 ) ) ;
#5343=CARTESIAN_POINT ( 'NONE',  ( -4.171729424061787483, 11.33000000000000718, -12.83926296998457417 ) ) ;
#5354=CARTESIAN_POINT ( 'NONE',  ( 24.73863375370592976, 0.000000000000000000, 8.000000000000104805 ) ) ;
#5359=EDGE_LOOP ( 'NONE', ( #1253, #4347, #15133, #2217 ) ) ;
#5363=AXIS2_PLACEMENT_3D ( 'NONE', #6573, #7986, #11953 ) ;
#5372=CARTESIAN_POINT ( 'NONE',  ( -7.272992578804310604, 16.37999999999999901, 10.01041549318726709 ) ) ;
#5376=VECTOR ( 'NONE', #10089, 1000.000000000000000 ) ;
#5379=CARTESIAN_POINT ( 'NONE',  ( 21.14483242576215716, 7.170662809914417402, -2.970370385949218317 ) ) ;
#5382=CARTESIAN_POINT ( 'NONE',  ( 9.520470885617717371, -9.269999999999999574, -6.917026985038131848 ) ) ;
#5384=CARTESIAN_POINT ( 'NONE',  ( 13.49999999999999822, -4.719999999999997975, 4.386415899144237684 ) ) ;
#5396=EDGE_CURVE ( 'NONE', #5891, #2674, #8583, .T. ) ;
#5398=CARTESIAN_POINT ( 'NONE',  ( -7.272992578804307939, 12.48000000000000576, -10.01041549318726886 ) ) ;
#5400=CARTESIAN_POINT ( 'NONE',  ( 11.76794919243112325, -0.5699999999999871836, 1.734723475976807094E-15 ) ) ;
#5404=CARTESIAN_POINT ( 'NONE',  ( -10.92172942406179104, -3.769999999999995577, 7.935100905948385908 ) ) ;
#5406=DIRECTION ( 'NONE',  ( -1.000000000000000000, 0.000000000000000000, -1.075706766891313812E-14 ) ) ;
#5414=CARTESIAN_POINT ( 'NONE',  ( -1.900613283907767848, 0.3908560185363838535, -11.99999999999569766 ) ) ;
#5422=ORIENTED_EDGE ( 'NONE', *, *, #3035, .F. ) ;
#5426=CARTESIAN_POINT ( 'NONE',  ( 4.171729424061791924, 11.03000000000001180, -12.83926296998457239 ) ) ;
#5431=VECTOR ( 'NONE', #5697, 1000.000000000000000 ) ;
#5434=EDGE_CURVE ( 'NONE', #14697, #10231, #7256, .T. ) ;
#5443=VERTEX_POINT ( 'NONE', #12719 ) ;
#5445=CARTESIAN_POINT ( 'NONE',  ( -9.520470885617715595, 24.63000000000001322, -6.917026985038136289 ) ) ;
#5447=ORIENTED_EDGE ( 'NONE', *, *, #14402, .T. ) ;
#5448=VECTOR ( 'NONE', #13295, 1000.000000000000000 ) ;
#5456=AXIS2_PLACEMENT_3D ( 'NONE', #710, #8863, #11500 ) ;
#5461=DIRECTION ( 'NONE',  ( 0.000000000000000000, 0.000000000000000000, -1.000000000000000000 ) ) ;
#5464=DIRECTION ( 'NONE',  ( 0.8660254037844399289, 0.000000000000000000, -0.4999999999999977240 ) ) ;
#5466=VERTEX_POINT ( 'NONE', #3345 ) ;
#5467=CARTESIAN_POINT ( 'NONE',  ( -13.16837719205942570, 1.171226224988977633E-15, -1.863363871322652354 ) ) ;
#5472=CARTESIAN_POINT ( 'NONE',  ( -7.409984580736203970E-16, -10.32000000000000384, 12.37355403259654985 ) ) ;
#5473=DIRECTION ( 'NONE',  ( -0.000000000000000000, -1.000000000000000000, -0.000000000000000000 ) ) ;
#5474=CARTESIAN_POINT ( 'NONE',  ( 8.343458848123583849, -16.12000000000000810, -11.48378591275253768 ) ) ;
#5478=EDGE_CURVE ( 'NONE', #16817, #12239, #8759, .T. ) ;
#5486=CARTESIAN_POINT ( 'NONE',  ( 11.76794919243112325, 14.28000000000000647, 3.823638476888996163 ) ) ;
#5487=LINE ( 'NONE', #10868, #3834 ) ;
#5488=CARTESIAN_POINT ( 'NONE',  ( 8.343458848123583849, 4.879999999999997229, -11.48378591275253768 ) ) ;
#5490=CARTESIAN_POINT ( 'NONE',  ( 9.520470885617715595, 5.129999999999995453, 6.917026985038135400 ) ) ;
#5493=LINE ( 'NONE', #9305, #2293 ) ;
#5494=CARTESIAN_POINT ( 'NONE',  ( -13.49999999999999822, -12.92000000000000171, 4.386415899144235908 ) ) ;
#5504=LINE ( 'NONE', #2818, #2131 ) ;
#5506=CARTESIAN_POINT ( 'NONE',  ( -25.42428528562860990, 5.918584287042170544, 5.441113646577212748 ) ) ;
#5510=CARTESIAN_POINT ( 'NONE',  ( -18.99999999999998224, 7.773118517290098062, -1.732050807569074147 ) ) ;
#5511=EDGE_LOOP ( 'NONE', ( #11856, #16023, #1463, #16354, #3049, #10493, #15830, #3515, #11506, #12696, #3188, #14413, #4378, #14436, #6685, #10747, #17345, #1858, #13448, #10744, #6971, #15762, #13829, #15321, #15919, #17055, #1895, #2408, #2654 ) ) ;
#5512=CARTESIAN_POINT ( 'NONE',  ( -7.416407864998737942, 4.246025403784436492, 10.20780970022447853 ) ) ;
#5514=CARTESIAN_POINT ( 'NONE',  ( 8.343458848123583849, 12.88000000000000611, -11.48378591275253768 ) ) ;
#5520=CARTESIAN_POINT ( 'NONE',  ( 8.343458848123583849, 7.880000000000003446, -11.48378591275253768 ) ) ;
#5534=CARTESIAN_POINT ( 'NONE',  ( -7.999999999999741540, 7.170708369609773314, -19.79695994079638055 ) ) ;
#5536=CARTESIAN_POINT ( 'NONE',  ( 7.272992578804311492, 23.88000000000000966, -10.01041549318726709 ) ) ;
#5537=ORIENTED_EDGE ( 'NONE', *, *, #8764, .T. ) ;
#5541=CARTESIAN_POINT ( 'NONE',  ( -7.409984580736203970E-16, -13.32000000000000028, 12.37355403259654985 ) ) ;
#5556=CARTESIAN_POINT ( 'NONE',  ( 15.50190989971479816, 7.815224736851132725, -10.85009556066090930 ) ) ;
#5560=CARTESIAN_POINT ( 'NONE',  ( -13.35138662365028317, 1.798999282680476490E-09, 1.996909364337476678 ) ) ;
#5564=CARTESIAN_POINT ( 'NONE',  ( 11.76794919243112680, -9.419999999999999929, -3.823638476888993942 ) ) ;
#5565=FACE_OUTER_BOUND ( 'NONE', #12257, .T. ) ;
#5566=CARTESIAN_POINT ( 'NONE',  ( 13.50000000000000355, -16.42000000000000171, -4.386415899144233244 ) ) ;
#5571=CARTESIAN_POINT ( 'NONE',  ( -15.67790026899612954, 8.062143948122718839, -8.845307762532401696 ) ) ;
#5573=VECTOR ( 'NONE', #11634, 1000.000000000000000 ) ;
#5581=CARTESIAN_POINT ( 'NONE',  ( -15.58845726811976817, 0.000000000000000000, -11.00000000000018296 ) ) ;
#5584=CARTESIAN_POINT ( 'NONE',  ( -9.520470885617717371, -1.769999999999993801, 6.917026985038133624 ) ) ;
#5585=ADVANCED_FACE ( 'NONE', ( #2237 ), #16837, .F. ) ;
#5587=CARTESIAN_POINT ( 'NONE',  ( -10.92172942406178926, -16.36999999999999744, -7.935100905948389460 ) ) ;
#5589=LINE ( 'NONE', #10968, #15029 ) ;
#5595=CYLINDRICAL_SURFACE ( 'NONE', #15765, 2.000000000000001776 ) ;
#5602=ORIENTED_EDGE ( 'NONE', *, *, #16490, .F. ) ;
#5605=CARTESIAN_POINT ( 'NONE',  ( -8.549982208541774191E-16, 17.68000000000001748, 14.19474002721660355 ) ) ;
#5606=ORIENTED_EDGE ( 'NONE', *, *, #3449, .F. ) ;
#5607=ADVANCED_FACE ( 'NONE', ( #4741 ), #10145, .T. ) ;
#5611=CARTESIAN_POINT ( 'NONE',  ( 8.343458848123583849, 13.87999999999999012, -11.48378591275253768 ) ) ;
#5612=CARTESIAN_POINT ( 'NONE',  ( -12.00000000000000178, 6.796025403784443419, -2.718289652585035561E-15 ) ) ;
#5622=CARTESIAN_POINT ( 'NONE',  ( -10.40911334466800575, 10.00000000000000178, -6.687738405650081930 ) ) ;
#5624=CARTESIAN_POINT ( 'NONE',  ( -8.891200544363830713E-16, 5.680000000000002380, 13.49999999999999822 ) ) ;
#5626=CARTESIAN_POINT ( 'NONE',  ( -0.7873830781139755652, 9.999999999999998224, 12.87957660135147542 ) ) ;
#5628=ORIENTED_EDGE ( 'NONE', *, *, #11125, .T. ) ;
#5630=ORIENTED_EDGE ( 'NONE', *, *, #7310, .T. ) ;
#5631=EDGE_CURVE ( 'NONE', #16216, #14697, #10548, .T. ) ;
#5634=CARTESIAN_POINT ( 'NONE',  ( -10.35602470258073105, 7.924935932049796072, 15.34492079894888050 ) ) ;
#5635=VECTOR ( 'NONE', #5663, 1000.000000000000000 ) ;
#5643=CIRCLE ( 'NONE', #17473, 14.50000000000000000 ) ;
#5648=EDGE_LOOP ( 'NONE', ( #17251, #927, #13574, #4084 ) ) ;
#5651=DIRECTION ( 'NONE',  ( -0.000000000000000000, 1.000000000000000000, -0.000000000000000000 ) ) ;
#5654=CARTESIAN_POINT ( 'NONE',  ( 2.621994543952811015E-15, -18.81999999999999673, -14.19474002721660355 ) ) ;
#5659=DIRECTION ( 'NONE',  ( 0.000000000000000000, 0.000000000000000000, -1.000000000000000000 ) ) ;
#5661=EDGE_CURVE ( 'NONE', #3933, #4554, #2065, .T. ) ;
#5663=DIRECTION ( 'NONE',  ( 0.000000000000000000, -1.000000000000000000, 0.000000000000000000 ) ) ;
#5665=CARTESIAN_POINT ( 'NONE',  ( 9.708203932499371192, 5.596025403784450347, -7.053423027509677645 ) ) ;
#5669=CARTESIAN_POINT ( 'NONE',  ( 24.73863375370592976, 5.918584287042170544, 8.000000000000106581 ) ) ;
#5671=DIRECTION ( 'NONE',  ( 0.000000000000000000, 0.000000000000000000, 1.000000000000000000 ) ) ;
#5673=CARTESIAN_POINT ( 'NONE',  ( 7.272992578804311492, -9.120000000000004547, -10.01041549318726709 ) ) ;
#5675=CARTESIAN_POINT ( 'NONE',  ( 13.50000000000000000, -14.57000000000000028, 1.734723475976807094E-15 ) ) ;
#5686=DIRECTION ( 'NONE',  ( 0.000000000000000000, -1.000000000000000000, 0.000000000000000000 ) ) ;
#5691=ORIENTED_EDGE ( 'NONE', *, *, #10327, .T. ) ;
#5693=CARTESIAN_POINT ( 'NONE',  ( 10.00000000000002132, 0.000000000000000000, -17.32050807568876394 ) ) ;
#5697=DIRECTION ( 'NONE',  ( -0.000000000000000000, 1.000000000000000000, -0.000000000000000000 ) ) ;
#5699=CARTESIAN_POINT ( 'NONE',  ( -8.343458848123582072, 0.3799999999999937317, 11.48378591275254124 ) ) ;
#5706=CARTESIAN_POINT ( 'NONE',  ( 0.000000000000000000, 0.000000000000000000, 0.000000000000000000 ) ) ;
#5714=CARTESIAN_POINT ( 'NONE',  ( 7.575483063523256178, 10.00000000000000000, 11.14317524721867692 ) ) ;
#5718=ORIENTED_EDGE ( 'NONE', *, *, #11157, .T. ) ;
#5721=VECTOR ( 'NONE', #13877, 1000.000000000000000 ) ;
#5722=CARTESIAN_POINT ( 'NONE',  ( -8.000000000000140332, 7.815224843475954586, 17.14741290055376410 ) ) ;
#5724=EDGE_CURVE ( 'NONE', #106, #13215, #12870, .T. ) ;
#5728=VECTOR ( 'NONE', #17092, 1000.000000000000000 ) ;
#5732=CARTESIAN_POINT ( 'NONE',  ( 15.34211313687880285, 8.027799056124985455, -9.658320279281790377 ) ) ;
#5740=CARTESIAN_POINT ( 'NONE',  ( 13.50000000000000000, -13.56999999999999851, 1.734723475976807094E-15 ) ) ;
#5744=CARTESIAN_POINT ( 'NONE',  ( 9.520470885617717371, -18.27000000000000313, -6.917026985038131848 ) ) ;
#5748=DIRECTION ( 'NONE',  ( 0.000000000000000000, 1.000000000000000000, 0.000000000000000000 ) ) ;
#5749=PLANE ( 'NONE',  #11755 ) ;
#5753=CARTESIAN_POINT ( 'NONE',  ( 10.92172942406178926, 4.129999999999994564, 7.935100905948385908 ) ) ;
#5755=CARTESIAN_POINT ( 'NONE',  ( -7.272992578804310604, -10.62000000000000099, 10.01041549318726709 ) ) ;
#5757=CARTESIAN_POINT ( 'NONE',  ( -24.73863375370603634, 5.918584287042171432, 7.999999999999761080 ) ) ;
#5767=CARTESIAN_POINT ( 'NONE',  ( -3.708203932499374744, 0.4639745962155741310, -11.41267819554187035 ) ) ;
#5772=CARTESIAN_POINT ( 'NONE',  ( 7.272992578804311492, 23.88000000000000966, -10.01041549318726709 ) ) ;
#5777=CARTESIAN_POINT ( 'NONE',  ( 13.50000000000000000, 9.429999999999994387, 1.734723475976807094E-15 ) ) ;
#5778=EDGE_LOOP ( 'NONE', ( #7124, #13784, #3562, #15834 ) ) ;
#5782=CARTESIAN_POINT ( 'NONE',  ( -8.343458848123576743, 5.480000000000007532, -11.48378591275254301 ) ) ;
#5783=CARTESIAN_POINT ( 'NONE',  ( -2.734444271416374749E-11, 0.3139745962166686777, -12.00000000000000000 ) ) ;
#5792=CARTESIAN_POINT ( 'NONE',  ( 0.1772876194880554368, 8.062177826491097932, -18.00000000000000355 ) ) ;
#5800=DIRECTION ( 'NONE',  ( -9.821670480311996085E-15, 0.000000000000000000, 1.000000000000000000 ) ) ;
#5802=VERTEX_POINT ( 'NONE', #16924 ) ;
#5804=ORIENTED_EDGE ( 'NONE', *, *, #10758, .F. ) ;
#5809=FACE_OUTER_BOUND ( 'NONE', #6064, .T. ) ;
#5815=B_SPLINE_CURVE_WITH_KNOTS ( 'NONE', 3,
 ( #9558, #11225, #14908, #10962 ),
 .UNSPECIFIED., .F., .F.,
 ( 4, 4 ),
 ( 2.383248697825728792E-07, 0.007646667935218603301 ),
 .UNSPECIFIED. ) ;
#5818=ORIENTED_EDGE ( 'NONE', *, *, #2057, .T. ) ;
#5822=CARTESIAN_POINT ( 'NONE',  ( -15.32135601632717403, 7.956016702382084915, 10.18318151426807816 ) ) ;
#5826=CARTESIAN_POINT ( 'NONE',  ( -4.171729424061787483, -12.66999999999999993, -12.83926296998457417 ) ) ;
#5833=CARTESIAN_POINT ( 'NONE',  ( 11.76794919243112680, -6.420000000000001705, -3.823638476888993942 ) ) ;
#5839=CIRCLE ( 'NONE', #752, 14.50000000000000000 ) ;
#5842=DIRECTION ( 'NONE',  ( 0.8660254037844454800, 0.000000000000000000, -0.4999999999999881761 ) ) ;
#5844=CARTESIAN_POINT ( 'NONE',  ( -13.49999999999999822, 29.78000000000001180, -4.386415899144240349 ) ) ;
#5845=CARTESIAN_POINT ( 'NONE',  ( -9.520470885617715595, -2.369999999999996998, -6.917026985038136289 ) ) ;
#5847=CARTESIAN_POINT ( 'NONE',  ( 13.49999999999999822, -14.72000000000000242, 4.386415899144237684 ) ) ;
#5848=EDGE_CURVE ( 'NONE', #11548, #6684, #10929, .T. ) ;
#5852=B_SPLINE_CURVE_WITH_KNOTS ( 'NONE', 3,
 ( #1622, #5534, #16288, #8544 ),
 .UNSPECIFIED., .F., .F.,
 ( 4, 4 ),
 ( 0.008723199174958463573, 0.01636875612029859914 ),
 .UNSPECIFIED. ) ;
#5853=VECTOR ( 'NONE', #1530, 1000.000000000000000 ) ;
#5859=PLANE ( 'NONE',  #15581 ) ;
#5860=DIRECTION ( 'NONE',  ( -0.000000000000000000, 1.000000000000000000, -0.000000000000000000 ) ) ;
#5864=CARTESIAN_POINT ( 'NONE',  ( -7.272992578804307939, 24.48000000000000398, -10.01041549318726886 ) ) ;
#5865=ORIENTED_EDGE ( 'NONE', *, *, #9920, .T. ) ;
#5869=CARTESIAN_POINT ( 'NONE',  ( 10.92172942406179104, 3.730000000000011084, -7.935100905948385908 ) ) ;
#5872=DIRECTION ( 'NONE',  ( -0.000000000000000000, -1.000000000000000000, -0.000000000000000000 ) ) ;
#5873=CARTESIAN_POINT ( 'NONE',  ( 10.92172942406178926, 1.129999999999992122, 7.935100905948385908 ) ) ;
#5883=DIRECTION ( 'NONE',  ( -0.000000000000000000, 1.000000000000000000, -0.000000000000000000 ) ) ;
#5888=B_SPLINE_CURVE_WITH_KNOTS ( 'NONE', 3,
 ( #10431, #1213, #14718, #10682 ),
 .UNSPECIFIED., .F., .F.,
 ( 4, 4 ),
 ( 2.383248697861188768E-07, 0.007646667935218598965 ),
 .UNSPECIFIED. ) ;
#5891=VERTEX_POINT ( 'NONE', #12954 ) ;
#5899=EDGE_CURVE ( 'NONE', #1880, #6127, #8733, .T. ) ;
#5906=CARTESIAN_POINT ( 'NONE',  ( 8.622924440245734345, 9.863741101803070066, -11.09913452436183867 ) ) ;
#5914=CARTESIAN_POINT ( 'NONE',  ( -9.520470885617715595, 33.62999999999999545, -6.917026985038136289 ) ) ;
#5919=CARTESIAN_POINT ( 'NONE',  ( -15.34225977864763379, 8.027996330223285071, -9.656730951920845740 ) ) ;
#5920=CARTESIAN_POINT ( 'NONE',  ( -3.636496289402152637, -2.669999999999998597, -11.19198476289190936 ) ) ;
#5924=DIRECTION ( 'NONE',  ( 1.000000000000000000, 0.000000000000000000, 1.426480712616743416E-14 ) ) ;
#5930=CARTESIAN_POINT ( 'NONE',  ( 1.775737858763662015E-15, 9.999999999999998224, 14.50000000000000000 ) ) ;
#5931=CARTESIAN_POINT ( 'NONE',  ( -9.520470885617715595, -5.370000000000000107, -6.917026985038136289 ) ) ;
#5933=CARTESIAN_POINT ( 'NONE',  ( -10.92172942406178926, 1.629999999999992566, -7.935100905948389460 ) ) ;
#5937=CARTESIAN_POINT ( 'NONE',  ( 4.171729424061791924, 4.030000000000005578, -12.83926296998457239 ) ) ;
#5944=DIRECTION ( 'NONE',  ( 1.000000000000000000, -0.000000000000000000, 9.821670480311996085E-15 ) ) ;
#5949=CARTESIAN_POINT ( 'NONE',  ( -3.636496289402152637, 24.33000000000001961, -11.19198476289190936 ) ) ;
#5954=CARTESIAN_POINT ( 'NONE',  ( -4.171729424061787483, 7.330000000000003624, -12.83926296998457417 ) ) ;
#5955=EDGE_LOOP ( 'NONE', ( #8475, #1447, #12934, #12766 ) ) ;
#5956=CARTESIAN_POINT ( 'NONE',  ( -9.520470885617715595, 33.62999999999999545, -6.917026985038136289 ) ) ;
#5958=CARTESIAN_POINT ( 'NONE',  ( -10.92172942406178926, -0.3700000000000092104, -7.935100905948389460 ) ) ;
#5968=CARTESIAN_POINT ( 'NONE',  ( -7.416407864998739718, 7.513974596215567736, 10.20780970022447853 ) ) ;
#5971=LINE ( 'NONE', #3298, #9241 ) ;
#5979=CARTESIAN_POINT ( 'NONE',  ( -8.343458848123576743, 34.48000000000000398, -11.48378591275254301 ) ) ;
#5988=DIRECTION ( 'NONE',  ( -0.5000000000000006661, -0.000000000000000000, 0.8660254037844383745 ) ) ;
#5991=VERTEX_POINT ( 'NONE', #17211 ) ;
#5998=CARTESIAN_POINT ( 'NONE',  ( -17.14738331136000227, 7.815232041205461222, 7.999999999999841904 ) ) ;
#5999=DIRECTION ( 'NONE',  ( 0.000000000000000000, 0.000000000000000000, 1.000000000000000000 ) ) ;
#6003=CARTESIAN_POINT ( 'NONE',  ( 3.636496289402154414, 28.82999999999999474, 11.19198476289190758 ) ) ;
#6007=CARTESIAN_POINT ( 'NONE',  ( 11.76794919243112325, -15.71999999999999709, 3.823638476888996163 ) ) ;
#6009=VECTOR ( 'NONE', #16103, 1000.000000000000000 ) ;
#6011=CARTESIAN_POINT ( 'NONE',  ( -11.76794919243112325, -2.220000000000004192, -3.823638476888998827 ) ) ;
#6019=CARTESIAN_POINT ( 'NONE',  ( -3.636496289402152637, -5.669999999999994600, -11.19198476289190936 ) ) ;
#6025=EDGE_CURVE ( 'NONE', #9365, #9130, #10254, .T. ) ;
#6026=DIRECTION ( 'NONE',  ( -0.000000000000000000, -1.000000000000000000, -0.000000000000000000 ) ) ;
#6031=AXIS2_PLACEMENT_3D ( 'NONE', #10238, #7410, #16931 ) ;
#6038=CARTESIAN_POINT ( 'NONE',  ( -7.272992578804310604, 19.38000000000000256, 10.01041549318726709 ) ) ;
#6043=CARTESIAN_POINT ( 'NONE',  ( 11.76794919243112325, 32.43000000000001393, 1.734723475976807094E-15 ) ) ;
#6045=( BOUNDED_CURVE ( )  B_SPLINE_CURVE ( 2, ( #9092, #934, #6343, #14187, #17020, #3327, #2244, #6255, #7497, #11729, #5012, #766, #16846 ),
 .UNSPECIFIED., .F., .F. ) 
 B_SPLINE_CURVE_WITH_KNOTS ( ( 3, 2, 2, 2, 2, 2, 3 ),
 ( 0.4952864492504068794, 0.4981166612263263072, 0.5037770778311709829, 0.5094374944360154922, 0.5150979110408601125, 0.5207583276457047328, 0.5235885359481271539 ),
 .UNSPECIFIED. ) 
 CURVE ( )  GEOMETRIC_REPRESENTATION_ITEM ( )  RATIONAL_B_SPLINE_CURVE ( ( 0.9755282581476180104, 0.9755282263842351975, 1.000000000000000000, 0.9510565162951535312, 1.000000000000000000, 0.9510565162951535312, 1.000000000000000000, 0.9510565162951535312, 1.000000000000000000, 0.9510565162951535312, 1.000000000000000000, 0.9755282581475762660, 0.9755282581475768211 ) ) 
 REPRESENTATION_ITEM ( '' )  );
#6051=CARTESIAN_POINT ( 'NONE',  ( 9.335235950531815854E-15, 8.180000000000005045, -13.50000000000000178 ) ) ;
#6057=DIRECTION ( 'NONE',  ( 0.000000000000000000, 1.000000000000000000, 0.000000000000000000 ) ) ;
#6061=ORIENTED_EDGE ( 'NONE', *, *, #1742, .T. ) ;
#6063=EDGE_LOOP ( 'NONE', ( #16401, #14674, #8822, #7557 ) ) ;
#6064=EDGE_LOOP ( 'NONE', ( #17190, #12254, #15940, #7705 ) ) ;
#6065=CARTESIAN_POINT ( 'NONE',  ( 0.1963306558083189324, -19.34015606061350923, 13.47512034797125580 ) ) ;
#6072=CARTESIAN_POINT ( 'NONE',  ( 12.78300487269503805, -4.622062490413154417E-15, 1.228102481046923433 ) ) ;
#6080=B_SPLINE_CURVE_WITH_KNOTS ( 'NONE', 3,
 ( #2002, #779, #10251, #3430 ),
 .UNSPECIFIED., .F., .F.,
 ( 4, 4 ),
 ( 2.376698214958262694E-07, 0.007646667280170314253 ),
 .UNSPECIFIED. ) ;
#6081=ORIENTED_EDGE ( 'NONE', *, *, #15210, .F. ) ;
#6083=ORIENTED_EDGE ( 'NONE', *, *, #17408, .T. ) ;
#6084=CARTESIAN_POINT ( 'NONE',  ( 13.49999999999999822, 9.280000000000002913, 4.386415899144236796 ) ) ;
#6088=CARTESIAN_POINT ( 'NONE',  ( 1.653273178848926472E-15, 0.000000000000000000, 13.50000000000000000 ) ) ;
#6089=CARTESIAN_POINT ( 'NONE',  ( 15.78643792884164299, 8.055054264001460851, 8.704847339800551254 ) ) ;
#6092=CARTESIAN_POINT ( 'NONE',  ( -11.76794919243112325, 31.07999999999999829, 3.823638476888994386 ) ) ;
#6096=CARTESIAN_POINT ( 'NONE',  ( 7.272992578804308828, -16.02000000000000313, 10.01041549318726709 ) ) ;
#6098=CARTESIAN_POINT ( 'NONE',  ( 18.71385749420391420, 7.854010659623985369, -1.541332980592505120 ) ) ;
#6099=CARTESIAN_POINT ( 'NONE',  ( -9.520470885617715595, 0.6299999999999916778, -6.917026985038136289 ) ) ;
#6102=CARTESIAN_POINT ( 'NONE',  ( -19.29752010712864418, 0.000000000000000000, 17.42428528562836831 ) ) ;
#6105=CARTESIAN_POINT ( 'NONE',  ( 0.000000000000000000, 9.000000000000000000, 0.000000000000000000 ) ) ;
#6106=CARTESIAN_POINT ( 'NONE',  ( -13.50000000000000000, 2.930000000000001936, -3.469446951953614189E-15 ) ) ;
#6109=AXIS2_PLACEMENT_3D ( 'NONE', #3158, #12548, #4326 ) ;
#6116=AXIS2_PLACEMENT_3D ( 'NONE', #1241, #8071, #14834 ) ;
#6120=EDGE_CURVE ( 'NONE', #16109, #6426, #6916, .T. ) ;
#6121=DIRECTION ( 'NONE',  ( -0.000000000000000000, -1.000000000000000000, -0.000000000000000000 ) ) ;
#6126=CARTESIAN_POINT ( 'NONE',  ( 7.272992578804311492, 14.88000000000000078, -10.01041549318726709 ) ) ;
#6127=VERTEX_POINT ( 'NONE', #14289 ) ;
#6131=CARTESIAN_POINT ( 'NONE',  ( -11.76794919243112325, 31.07999999999999829, 3.823638476888994386 ) ) ;
#6138=CARTESIAN_POINT ( 'NONE',  ( 13.50000000000000355, 7.580000000000000071, -4.386415899144233244 ) ) ;
#6145=ADVANCED_FACE ( 'NONE', ( #2087 ), #9195, .T. ) ;
#6147=PLANE ( 'NONE',  #5088 ) ;
#6151=CARTESIAN_POINT ( 'NONE',  ( 7.329991333342587900, -1.736202706843529944E-17, -9.501117147637041072 ) ) ;
#6154=ORIENTED_EDGE ( 'NONE', *, *, #1901, .F. ) ;
#6155=CARTESIAN_POINT ( 'NONE',  ( 4.171729424061791924, 31.03000000000000114, -12.83926296998457239 ) ) ;
#6164=ADVANCED_FACE ( 'NONE', ( #6537 ), #9013, .T. ) ;
#6166=ORIENTED_EDGE ( 'NONE', *, *, #11694, .T. ) ;
#6168=VERTEX_POINT ( 'NONE', #14460 ) ;
#6171=LINE ( 'NONE', #3497, #8627 ) ;
#6174=DIRECTION ( 'NONE',  ( 0.000000000000000000, 0.000000000000000000, 1.000000000000000000 ) ) ;
#6176=CARTESIAN_POINT ( 'NONE',  ( 11.76794919243112680, 29.58000000000000540, -3.823638476888993942 ) ) ;
#6188=EDGE_LOOP ( 'NONE', ( #12241, #322, #3577, #10512, #6468, #14051, #15323, #3739, #15224, #2406, #9060, #3694, #8715, #3005, #11916, #10446, #3304, #9350 ) ) ;
#6201=CARTESIAN_POINT ( 'NONE',  ( 24.73863375370598305, 0.000000000000000000, -7.999999999999934275 ) ) ;
#6206=CARTESIAN_POINT ( 'NONE',  ( -11.76794919243112325, 15.92999999999999972, -2.602085213965210642E-15 ) ) ;
#6207=ORIENTED_EDGE ( 'NONE', *, *, #14312, .F. ) ;
#6211=CARTESIAN_POINT ( 'NONE',  ( 2.621994543952811015E-15, -1.820000000000002283, -14.19474002721660355 ) ) ;
#6212=CARTESIAN_POINT ( 'NONE',  ( 11.76794919243112325, 29.43000000000001037, 1.734723475976807094E-15 ) ) ;
#6218=DIRECTION ( 'NONE',  ( -0.000000000000000000, -1.000000000000000000, -0.000000000000000000 ) ) ;
#6227=DIRECTION ( 'NONE',  ( -0.8660254037844365982, 0.000000000000000000, -0.5000000000000035527 ) ) ;
#6231=VERTEX_POINT ( 'NONE', #8035 ) ;
#6233=CARTESIAN_POINT ( 'NONE',  ( -4.171729424061791036, 32.53000000000000114, 12.83926296998457239 ) ) ;
#6240=CARTESIAN_POINT ( 'NONE',  ( 10.85239523646640336, -2.258074356960818337E-15, 7.640122180002231644 ) ) ;
#6242=CARTESIAN_POINT ( 'NONE',  ( 1.732050807568877415, 7.773118517290098950, -19.00000000000000000 ) ) ;
#6247=ORIENTED_EDGE ( 'NONE', *, *, #1763, .T. ) ;
#6248=CARTESIAN_POINT ( 'NONE',  ( 8.377273874081270222, 10.00009955288323127, 10.58637257760431361 ) ) ;
#6254=FACE_OUTER_BOUND ( 'NONE', #4740, .T. ) ;
#6255=CARTESIAN_POINT ( 'NONE',  ( -13.49999999999999822, 5.779999999999997584, -4.386415899144240349 ) ) ;
#6260=CARTESIAN_POINT ( 'NONE',  ( 18.85009555739749487, 7.815224737767794139, -1.645503437279525416 ) ) ;
#6267=CARTESIAN_POINT ( 'NONE',  ( 3.708203932499368527, 7.696025403784440222, 11.41267819554184371 ) ) ;
#6269=CARTESIAN_POINT ( 'NONE',  ( -10.92172942406179104, 27.23000000000000398, 7.935100905948385908 ) ) ;
#6274=DIRECTION ( 'NONE',  ( 0.000000000000000000, 1.000000000000000000, 0.000000000000000000 ) ) ;
#6276=CARTESIAN_POINT ( 'NONE',  ( 8.343458848123583849, -1.120000000000002327, -11.48378591275253768 ) ) ;
#6277=CARTESIAN_POINT ( 'NONE',  ( 4.171729424061789260, 2.829999999999999183, 12.83926296998457239 ) ) ;
#6290=ORIENTED_EDGE ( 'NONE', *, *, #14194, .T. ) ;
#6291=CARTESIAN_POINT ( 'NONE',  ( 2.279995255611139653E-15, 15.18000000000000504, -12.37355403259654985 ) ) ;
#6292=EDGE_CURVE ( 'NONE', #9130, #13814, #5298, .T. ) ;
#6297=CARTESIAN_POINT ( 'NONE',  ( -8.549982208541774191E-16, -3.319999999999998064, 14.19474002721660355 ) ) ;
#6300=DIRECTION ( 'NONE',  ( -0.000000000000000000, 1.000000000000000000, -0.000000000000000000 ) ) ;
#6303=AXIS2_PLACEMENT_3D ( 'NONE', #12932, #2127, #8970 ) ;
#6307=DIRECTION ( 'NONE',  ( -0.8660254037844326014, 0.000000000000000000, -0.5000000000000104361 ) ) ;
#6316=CARTESIAN_POINT ( 'NONE',  ( 11.76794919243112325, 5.279999999999999361, 3.823638476888996163 ) ) ;
#6317=ORIENTED_EDGE ( 'NONE', *, *, #11024, .F. ) ;
#6320=CARTESIAN_POINT ( 'NONE',  ( 11.76794919243112325, -18.56999999999999673, 1.734723475976807094E-15 ) ) ;
#6327=CYLINDRICAL_SURFACE ( 'NONE', #10151, 12.00000000000000178 ) ;
#6328=LINE ( 'NONE', #7397, #15570 ) ;
#6334=EDGE_LOOP ( 'NONE', ( #10128, #12609 ) ) ;
#6336=EDGE_CURVE ( 'NONE', #14477, #14459, #14705, .T. ) ;
#6338=CARTESIAN_POINT ( 'NONE',  ( 8.343458848123583849, 15.87999999999999901, -11.48378591275253768 ) ) ;
#6340=DIRECTION ( 'NONE',  ( -0.000000000000000000, 1.000000000000000000, -0.000000000000000000 ) ) ;
#6343=CARTESIAN_POINT ( 'NONE',  ( -4.171729424061791036, 6.530000000000008242, 12.83926296998457239 ) ) ;
#6348=CARTESIAN_POINT ( 'NONE',  ( 20.00000000000000000, 0.000000000000000000, 7.056441485635107799E-14 ) ) ;
#6352=CARTESIAN_POINT ( 'NONE',  ( 15.58845726811984811, 7.773118517290097174, 11.00000000000007283 ) ) ;
#6355=EDGE_CURVE ( 'NONE', #4352, #11548, #2682, .T. ) ;
#6359=CARTESIAN_POINT ( 'NONE',  ( 2.621994543952811015E-15, 23.17999999999999616, -14.19474002721660355 ) ) ;
#6360=VERTEX_POINT ( 'NONE', #10944 ) ;
#6362=DIRECTION ( 'NONE',  ( -0.000000000000000000, -1.000000000000000000, -0.000000000000000000 ) ) ;
#6365=DIRECTION ( 'NONE',  ( -0.000000000000000000, -1.000000000000000000, -0.000000000000000000 ) ) ;
#6367=CARTESIAN_POINT ( 'NONE',  ( 13.50000000000000000, -4.569999999999997620, 1.734723475976807094E-15 ) ) ;
#6376=VECTOR ( 'NONE', #7404, 1000.000000000000000 ) ;
#6378=EDGE_CURVE ( 'NONE', #5891, #2325, #16310, .T. ) ;
#6382=CARTESIAN_POINT ( 'NONE',  ( -9.520470885617715595, 9.629999999999999005, -6.917026985038136289 ) ) ;
#6389=DIRECTION ( 'NONE',  ( 0.000000000000000000, -1.000000000000000000, 0.000000000000000000 ) ) ;
#6397=FACE_OUTER_BOUND ( 'NONE', #14504, .T. ) ;
#6401=CARTESIAN_POINT ( 'NONE',  ( 19.29752010712851984, 5.918584287042171432, -17.42428528562851042 ) ) ;
#6408=CARTESIAN_POINT ( 'NONE',  ( 3.636496289402154414, 1.829999999999998295, 11.19198476289190758 ) ) ;
#6412=CARTESIAN_POINT ( 'NONE',  ( 10.92172942406179104, 24.73000000000000043, -7.935100905948385908 ) ) ;
#6419=AXIS2_PLACEMENT_3D ( 'NONE', #17359, #10657, #14432 ) ;
#6426=VERTEX_POINT ( 'NONE', #3865 ) ;
#6427=VERTEX_POINT ( 'NONE', #12441 ) ;
#6429=ORIENTED_EDGE ( 'NONE', *, *, #1152, .T. ) ;
#6430=CARTESIAN_POINT ( 'NONE',  ( -4.171729424061787483, 13.33000000000000895, -12.83926296998457417 ) ) ;
#6431=CARTESIAN_POINT ( 'NONE',  ( 3.636496289402157078, -11.96999999999999531, -11.19198476289190936 ) ) ;
#6434=FACE_OUTER_BOUND ( 'NONE', #7056, .T. ) ;
#6447=CARTESIAN_POINT ( 'NONE',  ( -10.92172942406178926, 20.63000000000000966, -7.935100905948389460 ) ) ;
#6453=CARTESIAN_POINT ( 'NONE',  ( -10.92172942406179104, -2.769999999999994689, 7.935100905948385908 ) ) ;
#6454=( BOUNDED_CURVE ( )  B_SPLINE_CURVE ( 2, ( #9472, #16149, #2624, #4057, #10614, #9385, #14566, #8057, #14820, #8235, #13421, #6906, #12191 ),
 .UNSPECIFIED., .F., .T. ) 
 B_SPLINE_CURVE_WITH_KNOTS ( ( 3, 2, 2, 2, 2, 2, 3 ),
 ( 0.4861111111111111049, 0.4888888888888888729, 0.4944444444444444642, 0.5000000000000000000, 0.5055555555555555358, 0.5111111111111110716, 0.5138888888888888395 ),
 .UNSPECIFIED. ) 
 CURVE ( )  GEOMETRIC_REPRESENTATION_ITEM ( )  RATIONAL_B_SPLINE_CURVE ( ( 0.9755282581475768211, 0.9755282581475768211, 1.000000000000000000, 0.9510565162951535312, 1.000000000000000000, 0.9510565162951535312, 1.000000000000000000, 0.9510565162951535312, 1.000000000000000000, 0.9510565162951535312, 1.000000000000000000, 0.9755282581475772652, 0.9755282581475768211 ) ) 
 REPRESENTATION_ITEM ( '' )  );
#6458=EDGE_CURVE ( 'NONE', #1168, #12765, #12701, .T. ) ;
#6468=ORIENTED_EDGE ( 'NONE', *, *, #2212, .T. ) ;
#6469=CARTESIAN_POINT ( 'NONE',  ( -9.520470885617717371, 16.22999999999999332, 6.917026985038133624 ) ) ;
#6474=CARTESIAN_POINT ( 'NONE',  ( -8.343458848123582072, -3.620000000000003215, 11.48378591275254124 ) ) ;
#6481=EDGE_CURVE ( 'NONE', #15151, #14477, #4189, .T. ) ;
#6485=CARTESIAN_POINT ( 'NONE',  ( -18.99999999999998224, 0.000000000000000000, -1.732050807569074369 ) ) ;
#6487=VECTOR ( 'NONE', #4163, 1000.000000000000227 ) ;
#6496=CARTESIAN_POINT ( 'NONE',  ( 7.272992578804311492, 2.880000000000001670, -10.01041549318726709 ) ) ;
#6497=ORIENTED_EDGE ( 'NONE', *, *, #1224, .F. ) ;
#6498=AXIS2_PLACEMENT_3D ( 'NONE', #15329, #765, #11640 ) ;
#6500=CARTESIAN_POINT ( 'NONE',  ( 13.50000000000000355, 21.58000000000000895, -4.386415899144233244 ) ) ;
#6505=VECTOR ( 'NONE', #13445, 1000.000000000000000 ) ;
#6519=EDGE_LOOP ( 'NONE', ( #10846, #1190, #11722, #1123 ) ) ;
#6520=CARTESIAN_POINT ( 'NONE',  ( -8.343458848123576743, 13.48000000000001641, -11.48378591275254301 ) ) ;
#6522=EDGE_CURVE ( 'NONE', #12765, #3761, #10730, .T. ) ;
#6537=FACE_OUTER_BOUND ( 'NONE', #16577, .T. ) ;
#6538=CARTESIAN_POINT ( 'NONE',  ( 7.272992578804311492, 26.88000000000001677, -10.01041549318726709 ) ) ;
#6540=CARTESIAN_POINT ( 'NONE',  ( 0.000000000000000000, 9.999999999999998224, 0.000000000000000000 ) ) ;
#6542=CARTESIAN_POINT ( 'NONE',  ( 13.49999999999999822, -7.720000000000004192, 4.386415899144237684 ) ) ;
#6550=CARTESIAN_POINT ( 'NONE',  ( 1.900613283894434735, 1.622906826104706601, 12.00000000000000000 ) ) ;
#6553=CARTESIAN_POINT ( 'NONE',  ( -11.76794919243112325, 13.07999999999999829, 3.823638476888994386 ) ) ;
#6555=ORIENTED_EDGE ( 'NONE', *, *, #16241, .T. ) ;
#6556=CARTESIAN_POINT ( 'NONE',  ( 11.76794919243112325, 2.280000000000006466, 3.823638476888996163 ) ) ;
#6557=EDGE_LOOP ( 'NONE', ( #12937, #6882, #16005, #2648 ) ) ;
#6560=CARTESIAN_POINT ( 'NONE',  ( 6.475374228414382927, 9.912830568698879574, 12.09076339992581417 ) ) ;
#6561=CARTESIAN_POINT ( 'NONE',  ( 13.49999999999999822, -5.720000000000003304, 4.386415899144237684 ) ) ;
#6573=CARTESIAN_POINT ( 'NONE',  ( 9.999999999999902300, 0.000000000000000000, 17.32050807568882789 ) ) ;
#6582=CARTESIAN_POINT ( 'NONE',  ( 7.272992578804308828, 4.980000000000008420, 10.01041549318726709 ) ) ;
#6583=EDGE_LOOP ( 'NONE', ( #2849, #10939, #11633, #6771 ) ) ;
#6585=CARTESIAN_POINT ( 'NONE',  ( -10.92172942406178926, 19.63000000000000966, -7.935100905948389460 ) ) ;
#6594=LINE ( 'NONE', #9513, #14081 ) ;
#6595=CARTESIAN_POINT ( 'NONE',  ( -1.688033560168326508, 9.999999999999996447, -13.00620140183451490 ) ) ;
#6598=FACE_OUTER_BOUND ( 'NONE', #2940, .T. ) ;
#6602=ORIENTED_EDGE ( 'NONE', *, *, #3449, .T. ) ;
#6609=CARTESIAN_POINT ( 'NONE',  ( 9.835827272001290922, 8.007293614239925361, 15.31970530204991121 ) ) ;
#6616=CARTESIAN_POINT ( 'NONE',  ( -18.99999999999998224, 7.773118517290098062, -1.732050807569074147 ) ) ;
#6619=CARTESIAN_POINT ( 'NONE',  ( 10.92172942406178926, 22.13000000000000966, 7.935100905948385908 ) ) ;
#6625=CARTESIAN_POINT ( 'NONE',  ( 2.279995255611139653E-15, -11.81999999999999851, -12.37355403259654985 ) ) ;
#6627=CARTESIAN_POINT ( 'NONE',  ( -4.171729424061791036, -5.469999999999995310, 12.83926296998457239 ) ) ;
#6630=PRODUCT_CONTEXT ( 'NONE', #3256, 'mechanical' ) ;
#6634=AXIS2_PLACEMENT_3D ( 'NONE', #9871, #4104, #13553 ) ;
#6637=CARTESIAN_POINT ( 'NONE',  ( 3.708203932499371192, 2.896025403784442620, -11.41267819554184548 ) ) ;
#6641=CARTESIAN_POINT ( 'NONE',  ( -7.409984580736203970E-16, 1.680000000000003491, 12.37355403259654985 ) ) ;
#6645=CARTESIAN_POINT ( 'NONE',  ( 2.621994543952811015E-15, -4.820000000000002949, -14.19474002721660355 ) ) ;
#6654=DIRECTION ( 'NONE',  ( -0.000000000000000000, 1.000000000000000000, -0.000000000000000000 ) ) ;
#6661=VERTEX_POINT ( 'NONE', #16489 ) ;
#6665=CARTESIAN_POINT ( 'NONE',  ( -13.50000000000000000, 22.93000000000000682, -3.469446951953614189E-15 ) ) ;
#6669=CARTESIAN_POINT ( 'NONE',  ( -8.549982208541774191E-16, 12.67999999999999794, 14.19474002721660355 ) ) ;
#6676=EDGE_CURVE ( 'NONE', #13814, #8520, #16368, .T. ) ;
#6681=DIRECTION ( 'NONE',  ( 0.4999999999999945599, 0.000000000000000000, 0.8660254037844418162 ) ) ;
#6684=VERTEX_POINT ( 'NONE', #6088 ) ;
#6685=ORIENTED_EDGE ( 'NONE', *, *, #7934, .F. ) ;
#6703=CARTESIAN_POINT ( 'NONE',  ( -8.343458848123582072, 21.37999999999999901, 11.48378591275254124 ) ) ;
#6704=ORIENTED_EDGE ( 'NONE', *, *, #2113, .T. ) ;
#6709=CARTESIAN_POINT ( 'NONE',  ( 18.99999999999999289, 0.000000000000000000, 1.732050807568941586 ) ) ;
#6710=CARTESIAN_POINT ( 'NONE',  ( -13.50000000000000000, -6.069999999999999396, -3.469446951953614189E-15 ) ) ;
#6711=B_SPLINE_CURVE_WITH_KNOTS ( 'NONE', 3,
 ( #2332, #13051, #15677, #12962 ),
 .UNSPECIFIED., .F., .F.,
 ( 4, 4 ),
 ( 2.383248697750600941E-07, 0.007646667935218598965 ),
 .UNSPECIFIED. ) ;
#6723=CARTESIAN_POINT ( 'NONE',  ( -9.520470885617717371, 13.23000000000001997, 6.917026985038133624 ) ) ;
#6726=CARTESIAN_POINT ( 'NONE',  ( 3.636496289402157078, 0.03000000000000224709, -11.19198476289190936 ) ) ;
#6730=CARTESIAN_POINT ( 'NONE',  ( -8.549982208541774191E-16, -6.320000000000004725, 14.19474002721660355 ) ) ;
#6731=CARTESIAN_POINT ( 'NONE',  ( 8.375056734751542109, 9.999950376471138824, 10.58801762894534271 ) ) ;
#6738=CARTESIAN_POINT ( 'NONE',  ( -12.00000000000000178, 9.796025403784433649, -2.718289652585035561E-15 ) ) ;
#6739=CARTESIAN_POINT ( 'NONE',  ( 2.785879211291982797E-06, 6.680077384874748780, 13.49999999999942979 ) ) ;
#6746=ORIENTED_EDGE ( 'NONE', *, *, #17277, .F. ) ;
#6751=CARTESIAN_POINT ( 'NONE',  ( 13.49999999999999822, 18.28000000000001180, 4.386415899144237684 ) ) ;
#6753=ADVANCED_FACE ( 'NONE', ( #2070 ), #7581, .F. ) ;
#6755=CARTESIAN_POINT ( 'NONE',  ( -8.549982208541774191E-16, 9.680000000000003268, 14.19474002721660355 ) ) ;
#6761=AXIS2_PLACEMENT_3D ( 'NONE', #4122, #11996, #9536 ) ;
#6762=CARTESIAN_POINT ( 'NONE',  ( 0.000000000000000000, 0.000000000000000000, 0.000000000000000000 ) ) ;
#6763=CARTESIAN_POINT ( 'NONE',  ( -8.000000000000143885, 7.773118517290097174, 17.32050807568870709 ) ) ;
#6767=CARTESIAN_POINT ( 'NONE',  ( 8.343458848123583849, 6.880000000000006999, -11.48378591275253768 ) ) ;
#6771=ORIENTED_EDGE ( 'NONE', *, *, #9474, .F. ) ;
#6777=CARTESIAN_POINT ( 'NONE',  ( 10.92172942406179104, 16.72999999999999332, -7.935100905948385908 ) ) ;
#6787=CARTESIAN_POINT ( 'NONE',  ( 0.000000000000000000, 9.000000000000000000, 0.000000000000000000 ) ) ;
#6789=FACE_OUTER_BOUND ( 'NONE', #8103, .T. ) ;
#6791=CARTESIAN_POINT ( 'NONE',  ( 4.171729424061789260, 21.83000000000001606, 12.83926296998457239 ) ) ;
#6793=CARTESIAN_POINT ( 'NONE',  ( -11.06327252796750926, 9.630592963500558854E-15, -6.703345338116586838 ) ) ;
#6795=VECTOR ( 'NONE', #6300, 1000.000000000000000 ) ;
#6798=CARTESIAN_POINT ( 'NONE',  ( -9.520470885617717371, -7.769999999999999574, 6.917026985038133624 ) ) ;
#6799=DIRECTION ( 'NONE',  ( -0.4999999999999918399, 0.000000000000000000, -0.8660254037844434816 ) ) ;
#6800=CARTESIAN_POINT ( 'NONE',  ( 2.621994543952811015E-15, -15.82000000000000561, -14.19474002721660355 ) ) ;
#6812=CARTESIAN_POINT ( 'NONE',  ( -3.636496289402152637, 9.330000000000005400, -11.19198476289190936 ) ) ;
#6814=FACE_OUTER_BOUND ( 'NONE', #11965, .T. ) ;
#6815=CARTESIAN_POINT ( 'NONE',  ( -7.272992578804310604, 1.379999999999991456, 10.01041549318726709 ) ) ;
#6819=CARTESIAN_POINT ( 'NONE',  ( -8.343458848123576743, -7.520000000000004015, -11.48378591275254301 ) ) ;
#6827=CARTESIAN_POINT ( 'NONE',  ( -9.999999999999776179, 7.983052681820796970, -15.32050807568890427 ) ) ;
#6830=DIRECTION ( 'NONE',  ( -0.000000000000000000, 1.000000000000000000, -0.000000000000000000 ) ) ;
#6832=VECTOR ( 'NONE', #2197, 1000.000000000000000 ) ;
#6835=CARTESIAN_POINT ( 'NONE',  ( -18.46710335681943960, 7.924935997292880785, -1.296119813004219079 ) ) ;
#6836=VERTEX_POINT ( 'NONE', #1821 ) ;
#6837=CYLINDRICAL_SURFACE ( 'NONE', #16997, 1.999999999999998224 ) ;
#6839=CARTESIAN_POINT ( 'NONE',  ( 13.49999999999999822, 15.28000000000000469, 4.386415899144237684 ) ) ;
#6844=CARTESIAN_POINT ( 'NONE',  ( 4.171729424061791924, 14.03000000000001535, -12.83926296998457239 ) ) ;
#6850=VECTOR ( 'NONE', #11262, 1000.000000000000227 ) ;
#6853=CARTESIAN_POINT ( 'NONE',  ( 1.900613283894444283, 7.890856018535865601, 12.00000000000006040 ) ) ;
#6861=CARTESIAN_POINT ( 'NONE',  ( -11.76794919243112325, 24.93000000000000682, -2.602085213965210642E-15 ) ) ;
#6862=EDGE_LOOP ( 'NONE', ( #3561, #16485, #5075, #9852 ) ) ;
#6865=VECTOR ( 'NONE', #2010, 1000.000000000000000 ) ;
#6867=CARTESIAN_POINT ( 'NONE',  ( 9.520470885617715595, -12.86999999999999922, 6.917026985038135400 ) ) ;
#6874=AXIS2_PLACEMENT_3D ( 'NONE', #608, #11572, #13937 ) ;
#6876=ADVANCED_FACE ( 'NONE', ( #3150 ), #2882, .F. ) ;
#6882=ORIENTED_EDGE ( 'NONE', *, *, #3504, .T. ) ;
#6883=LINE ( 'NONE', #12255, #9786 ) ;
#6885=ORIENTED_EDGE ( 'NONE', *, *, #4165, .T. ) ;
#6887=CARTESIAN_POINT ( 'NONE',  ( 25.42428528562856727, 5.918584287042170544, -5.441113646577394825 ) ) ;
#6891=CARTESIAN_POINT ( 'NONE',  ( -13.49999999999999822, -18.22000000000000242, -4.386415899144240349 ) ) ;
#6896=CYLINDRICAL_SURFACE ( 'NONE', #1079, 26.00000000000000355 ) ;
#6899=ADVANCED_FACE ( 'NONE', ( #9726 ), #6896, .T. ) ;
#6906=CARTESIAN_POINT ( 'NONE',  ( -2.138189944381279073, 7.256881422320270225, -13.49999999999998579 ) ) ;
#6907=CARTESIAN_POINT ( 'NONE',  ( -7.272992578804310604, -1.620000000000001217, 10.01041549318726709 ) ) ;
#6909=CARTESIAN_POINT ( 'NONE',  ( 8.343458848123583849, -17.12000000000000099, -11.48378591275253768 ) ) ;
#6916=( BOUNDED_CURVE ( )  B_SPLINE_CURVE ( 2, ( #7862, #2174, #11833, #7600, #15608, #17035, #5027, #10513, #15875, #11658, #2431, #5208, #4940 ),
 .UNSPECIFIED., .F., .F. ) 
 B_SPLINE_CURVE_WITH_KNOTS ( ( 3, 2, 2, 2, 2, 2, 3 ),
 ( 0.4386822870511441486, 0.4415124951778801599, 0.4471729117827247801, 0.4528333283875693449, 0.4584937449924140207, 0.4641541615972585855, 0.4669843698996809511 ),
 .UNSPECIFIED. ) 
 CURVE ( )  GEOMETRIC_REPRESENTATION_ITEM ( )  RATIONAL_B_SPLINE_CURVE ( ( 0.9755282581475768211, 0.9755282596666697836, 1.000000000000000000, 0.9510565162951535312, 1.000000000000000000, 0.9510565162951535312, 1.000000000000000000, 0.9510565162951535312, 1.000000000000000000, 0.9510565162951535312, 1.000000000000000000, 0.9755282581475765991, 0.9755282581475768211 ) ) 
 REPRESENTATION_ITEM ( '' )  );
#6918=ADVANCED_FACE ( 'NONE', ( #3240 ), #16503, .F. ) ;
#6919=LINE ( 'NONE', #17332, #7244 ) ;
#6921=CARTESIAN_POINT ( 'NONE',  ( -15.58845726811976995, 7.773118517290098062, -11.00000000000018119 ) ) ;
#6928=CARTESIAN_POINT ( 'NONE',  ( -13.49999999999999822, 14.07999999999999652, 4.386415899144235908 ) ) ;
#6934=CARTESIAN_POINT ( 'NONE',  ( 8.343458848123578520, 12.98000000000000220, 11.48378591275254124 ) ) ;
#6941=CARTESIAN_POINT ( 'NONE',  ( 5.441113646577305119, 0.000000000000000000, 25.42428528562857792 ) ) ;
#6943=DIRECTION ( 'NONE',  ( 0.000000000000000000, 0.000000000000000000, 1.000000000000000000 ) ) ;
#6946=CARTESIAN_POINT ( 'NONE',  ( -9.999999999999776179, 0.000000000000000000, -17.32050807568890605 ) ) ;
#6949=CARTESIAN_POINT ( 'NONE',  ( -8.397663224344118049, 9.999999999999998224, 9.034341791799572974 ) ) ;
#6950=CARTESIAN_POINT ( 'NONE',  ( -8.673064033300265763, 8.051595442100884625, -15.81825948347707822 ) ) ;
#6951=CARTESIAN_POINT ( 'NONE',  ( -9.520470885617715595, 24.63000000000001322, -6.917026985038136289 ) ) ;
#6952=ORIENTED_EDGE ( 'NONE', *, *, #13007, .T. ) ;
#6953=CARTESIAN_POINT ( 'NONE',  ( -1.732050807568877859, 0.000000000000000000, -18.99999999999999645 ) ) ;
#6955=ORIENTED_EDGE ( 'NONE', *, *, #2057, .F. ) ;
#6958=CARTESIAN_POINT ( 'NONE',  ( -8.110285629053095136, 7.924527542031521321, 16.64312382832866888 ) ) ;
#6969=CARTESIAN_POINT ( 'NONE',  ( 11.00000000000001599, 0.000000000000000000, -15.58845726811988364 ) ) ;
#6971=ORIENTED_EDGE ( 'NONE', *, *, #6676, .F. ) ;
#6976=CARTESIAN_POINT ( 'NONE',  ( 11.00000000000001599, 0.000000000000000000, -15.58845726811988364 ) ) ;
#6978=CARTESIAN_POINT ( 'NONE',  ( 21.14483242576213584, 7.170662809914417402, 2.970370385949366199 ) ) ;
#6980=CARTESIAN_POINT ( 'NONE',  ( 4.171729424061791924, -18.97000000000000242, -12.83926296998457239 ) ) ;
#6985=DIRECTION ( 'NONE',  ( 1.075706766891313654E-14, 0.000000000000000000, -1.000000000000000000 ) ) ;
#6987=CARTESIAN_POINT ( 'NONE',  ( 12.00000000000002665, 2.413974596215582746, 3.899036354794885639 ) ) ;
#6988=CARTESIAN_POINT ( 'NONE',  ( 12.00000000000000178, 5.296025403784440755, 1.734723475976807094E-15 ) ) ;
#6993=CARTESIAN_POINT ( 'NONE',  ( -9.708203932499369415, 0.4960254037844292752, -7.053423027509682086 ) ) ;
#6994=CYLINDRICAL_SURFACE ( 'NONE', #80, 12.00000000000000178 ) ;
#6996=CARTESIAN_POINT ( 'NONE',  ( -11.76794919243112325, -2.220000000000004192, -3.823638476888998827 ) ) ;
#6998=CARTESIAN_POINT ( 'NONE',  ( -10.92172942406179104, 2.230000000000009752, 7.935100905948385908 ) ) ;
#7008=CARTESIAN_POINT ( 'NONE',  ( -4.171729424061791036, 5.530000000000007354, 12.83926296998457239 ) ) ;
#7009=CARTESIAN_POINT ( 'NONE',  ( -7.416407864998755706, 1.513974596215569957, 10.20780970022450163 ) ) ;
#7016=DIRECTION ( 'NONE',  ( -0.000000000000000000, -1.000000000000000000, -0.000000000000000000 ) ) ;
#7017=DIRECTION ( 'NONE',  ( -0.000000000000000000, 1.000000000000000000, -0.000000000000000000 ) ) ;
#7018=CARTESIAN_POINT ( 'NONE',  ( -13.49999999999999822, 7.779999999999992255, -4.386415899144240349 ) ) ;
#7023=CARTESIAN_POINT ( 'NONE',  ( 2.621994543952811015E-15, 11.18000000000000149, -14.19474002721660355 ) ) ;
#7024=EDGE_CURVE ( 'NONE', #14888, #1687, #9230, .T. ) ;
#7034=VECTOR ( 'NONE', #10653, 1000.000000000000000 ) ;
#7037=CARTESIAN_POINT ( 'NONE',  ( 10.92172942406179104, 6.730000000000013749, -7.935100905948385908 ) ) ;
#7039=CARTESIAN_POINT ( 'NONE',  ( -4.491212130746389697, 10.00000000000000000, 11.83243654515264076 ) ) ;
#7040=DIRECTION ( 'NONE',  ( 0.000000000000000000, 1.000000000000000000, 0.000000000000000000 ) ) ;
#7041=CARTESIAN_POINT ( 'NONE',  ( 9.520470885617715595, 23.13000000000001322, 6.917026985038135400 ) ) ;
#7045=CARTESIAN_POINT ( 'NONE',  ( -3.636496289402156190, -16.46999999999999886, 11.19198476289190758 ) ) ;
#7056=EDGE_LOOP ( 'NONE', ( #1357, #13789, #11098, #5602 ) ) ;
#7058=EDGE_LOOP ( 'NONE', ( #7779, #14417, #15222, #10173 ) ) ;
#7064=CARTESIAN_POINT ( 'NONE',  ( 10.92172942406179104, -16.26999999999999957, -7.935100905948385908 ) ) ;
#7072=CARTESIAN_POINT ( 'NONE',  ( 2.902084407815607718E-14, 5.180000000000006821, -13.50000000000000000 ) ) ;
#7076=CARTESIAN_POINT ( 'NONE',  ( -0.1775006636059834053, 8.062177826491096155, -17.99999999999999289 ) ) ;
#7080=CARTESIAN_POINT ( 'NONE',  ( 3.636496289402154414, -7.169999999999995488, 11.19198476289190758 ) ) ;
#7082=CARTESIAN_POINT ( 'NONE',  ( 8.343458848123578520, -15.02000000000000846, 11.48378591275254124 ) ) ;
#7089=CARTESIAN_POINT ( 'NONE',  ( 0.000000000000000000, 5.918584287042170544, 0.000000000000000000 ) ) ;
#7091=CARTESIAN_POINT ( 'NONE',  ( -16.82677684650015237, 7.170662809914417402, -13.14483242576234723 ) ) ;
#7093=DIRECTION ( 'NONE',  ( 0.000000000000000000, 0.000000000000000000, 1.000000000000000000 ) ) ;
#7097=CARTESIAN_POINT ( 'NONE',  ( -7.409984580736203970E-16, 22.68000000000000327, 12.37355403259654985 ) ) ;
#7100=DIRECTION ( 'NONE',  ( 0.000000000000000000, 0.000000000000000000, 1.000000000000000000 ) ) ;
#7102=CARTESIAN_POINT ( 'NONE',  ( -8.343458848123576743, 4.480000000000009308, -11.48378591275254301 ) ) ;
#7107=CARTESIAN_POINT ( 'NONE',  ( 4.171729424061791924, 5.030000000000006466, -12.83926296998457239 ) ) ;
#7108=CARTESIAN_POINT ( 'NONE',  ( -7.416407864998736166, 6.346025403784442354, -10.20780970022448031 ) ) ;
#7119=CARTESIAN_POINT ( 'NONE',  ( 2.138189944381200469, 7.103118577679737200, -13.50000000000001421 ) ) ;
#7123=CARTESIAN_POINT ( 'NONE',  ( -11.76794919243112325, 21.93000000000000682, -2.602085213965210642E-15 ) ) ;
#7124=ORIENTED_EDGE ( 'NONE', *, *, #5724, .T. ) ;
#7129=CIRCLE ( 'NONE', #13045, 1.999999999999998224 ) ;
#7148=CARTESIAN_POINT ( 'NONE',  ( -11.76794919243112325, 33.78000000000000824, -3.823638476888998827 ) ) ;
#7151=VECTOR ( 'NONE', #5944, 1000.000000000000000 ) ;
#7155=CARTESIAN_POINT ( 'NONE',  ( 9.520470885617717371, -6.269999999999997797, -6.917026985038131848 ) ) ;
#7158=CARTESIAN_POINT ( 'NONE',  ( 0.000000000000000000, 9.000000000000000000, 0.000000000000000000 ) ) ;
#7163=CARTESIAN_POINT ( 'NONE',  ( -3.708203932499370303, 1.396025403784441066, 11.41267819554184371 ) ) ;
#7165=CARTESIAN_POINT ( 'NONE',  ( -7.272992578804307939, -5.520000000000001350, -10.01041549318726886 ) ) ;
#7167=CARTESIAN_POINT ( 'NONE',  ( -13.49999999999999822, -13.21999999999999709, -4.386415899144240349 ) ) ;
#7176=FACE_OUTER_BOUND ( 'NONE', #7555, .T. ) ;
#7180=CARTESIAN_POINT ( 'NONE',  ( 9.520470885617715595, 20.13000000000000966, 6.917026985038135400 ) ) ;
#7181=ORIENTED_EDGE ( 'NONE', *, *, #10188, .F. ) ;
#7185=ORIENTED_EDGE ( 'NONE', *, *, #5899, .T. ) ;
#7187=LINE ( 'NONE', #12576, #9100 ) ;
#7188=CARTESIAN_POINT ( 'NONE',  ( -13.49999999999999822, 2.779999999999990923, -4.386415899144240349 ) ) ;
#7192=ADVANCED_FACE ( 'NONE', ( #11563 ), #1910, .F. ) ;
#7201=CARTESIAN_POINT ( 'NONE',  ( 17.32050807568878170, 0.000000000000000000, -7.999999999999961808 ) ) ;
#7202=DIRECTION ( 'NONE',  ( -0.8660254037844434816, 0.000000000000000000, 0.4999999999999918399 ) ) ;
#7204=CARTESIAN_POINT ( 'NONE',  ( -3.600152184539524125, 10.00000000000000000, 12.19664001577687173 ) ) ;
#7206=ORIENTED_EDGE ( 'NONE', *, *, #5396, .T. ) ;
#7216=CARTESIAN_POINT ( 'NONE',  ( -0.3512640400060916823, 8.055266896996092996, 18.02316420754749871 ) ) ;
#7220=ORIENTED_EDGE ( 'NONE', *, *, #696, .F. ) ;
#7223=CYLINDRICAL_SURFACE ( 'NONE', #13417, 14.50000000000000000 ) ;
#7227=CARTESIAN_POINT ( 'NONE',  ( -10.68887637698740534, 7.854719008739928121, -15.43480272504890571 ) ) ;
#7230=CARTESIAN_POINT ( 'NONE',  ( 7.272992578804308828, 25.98000000000001108, 10.01041549318726709 ) ) ;
#7231=CIRCLE ( 'NONE', #12017, 26.00000000000000355 ) ;
#7234=EDGE_CURVE ( 'NONE', #13257, #17257, #13771, .T. ) ;
#7237=CARTESIAN_POINT ( 'NONE',  ( -15.78643792884158437, 8.055054264001460851, -8.704847339800664940 ) ) ;
#7238=CARTESIAN_POINT ( 'NONE',  ( 9.520470885617715595, -3.869999999999998330, 6.917026985038135400 ) ) ;
#7240=CARTESIAN_POINT ( 'NONE',  ( 0.000000000000000000, 30.93000000000001393, -13.50000000000000000 ) ) ;
#7244=VECTOR ( 'NONE', #6654, 1000.000000000000000 ) ;
#7248=CARTESIAN_POINT ( 'NONE',  ( 9.739336723526609063, 8.018126783878129160, -15.33316801648999217 ) ) ;
#7249=CARTESIAN_POINT ( 'NONE',  ( 13.50000000000000355, 28.58000000000000540, -4.386415899144233244 ) ) ;
#7250=CARTESIAN_POINT ( 'NONE',  ( -3.636496289402156190, -4.469999999999994422, 11.19198476289190758 ) ) ;
#7252=CARTESIAN_POINT ( 'NONE',  ( 12.00000000000000000, 5.563974596215566670, 1.734723475976807094E-15 ) ) ;
#7256=CIRCLE ( 'NONE', #3853, 13.50000000000000000 ) ;
#7266=CARTESIAN_POINT ( 'NONE',  ( -11.76794919243112325, 19.08000000000001606, 3.823638476888994386 ) ) ;
#7267=EDGE_CURVE ( 'NONE', #309, #6661, #4840, .T. ) ;
#7268=ORIENTED_EDGE ( 'NONE', *, *, #8980, .F. ) ;
#7276=CARTESIAN_POINT ( 'NONE',  ( -10.92172942406178926, 2.629999999999993676, -7.935100905948389460 ) ) ;
#7286=CARTESIAN_POINT ( 'NONE',  ( -25.42428528562849266, 5.918584287042170544, -5.441113646577749208 ) ) ;
#7295=ORIENTED_EDGE ( 'NONE', *, *, #8281, .T. ) ;
#7297=CARTESIAN_POINT ( 'NONE',  ( 2.621994543952811015E-15, 31.18000000000000682, -14.19474002721660355 ) ) ;
#7310=EDGE_CURVE ( 'NONE', #16538, #10472, #3337, .T. ) ;
#7317=CARTESIAN_POINT ( 'NONE',  ( -16.97418022790857961, 7.854708479871425730, 8.022689779262547560 ) ) ;
#7321=CARTESIAN_POINT ( 'NONE',  ( -11.76794919243112325, 30.93000000000001393, -2.602085213965210642E-15 ) ) ;
#7325=CARTESIAN_POINT ( 'NONE',  ( 3.636496289402157078, -14.96999999999999709, -11.19198476289190936 ) ) ;
#7327=CARTESIAN_POINT ( 'NONE',  ( 18.11515225121978290, 8.027996313748971602, 0.6918446750615231400 ) ) ;
#7329=CARTESIAN_POINT ( 'NONE',  ( 7.272992578804311492, -6.120000000000004547, -10.01041549318726709 ) ) ;
#7331=CARTESIAN_POINT ( 'NONE',  ( 7.416407864998755706, 3.013974596215577950, -10.20780970022449807 ) ) ;
#7332=CARTESIAN_POINT ( 'NONE',  ( 18.99999999999999289, 0.000000000000000000, 1.732050807568941586 ) ) ;
#7336=EDGE_CURVE ( 'NONE', #13170, #14800, #11264, .T. ) ;
#7338=CARTESIAN_POINT ( 'NONE',  ( -7.379696451821980833E-14, 6.046025403784444308, -12.00000000000000000 ) ) ;
#7339=CARTESIAN_POINT ( 'NONE',  ( -13.50000000000000000, 26.93000000000001037, -3.469446951953614189E-15 ) ) ;
#7340=CARTESIAN_POINT ( 'NONE',  ( 9.520470885617715595, -3.869999999999998330, 6.917026985038135400 ) ) ;
#7342=B_SPLINE_CURVE_WITH_KNOTS ( 'NONE', 3,
 ( #2765, #1197, #7932, #12245, #16030, #6609, #12157, #9266, #14701, #10582, #10750, #2591, #15943, #4025, #9440, #8021, #13389, #138 ),
 .UNSPECIFIED., .F., .F.,
 ( 4, 2, 2, 2, 2, 2, 2, 2, 4 ),
 ( 2.344180274388505696E-07, 0.0005273255548235158355, 0.001054416691619592837, 0.001581507828415669838, 0.002108598965211747056, 0.002635690102007827093, 0.003162781238803906696, 0.003689872375599986733, 0.004216963512396066337 ),
 .UNSPECIFIED. ) ;
#7343=UNCERTAINTY_MEASURE_WITH_UNIT (LENGTH_MEASURE( 1.000000000000000082E-05 ), #8769, 'distance_accuracy_value', 'NONE');
#7345=CARTESIAN_POINT ( 'NONE',  ( 7.999999999999904965, 7.773118517290098950, 17.32050807568881368 ) ) ;
#7347=VECTOR ( 'NONE', #2255, 1000.000000000000000 ) ;
#7352=VECTOR ( 'NONE', #15592, 1000.000000000000000 ) ;
#7354=CARTESIAN_POINT ( 'NONE',  ( 9.999999999999902300, 0.000000000000000000, 17.32050807568882789 ) ) ;
#7360=CARTESIAN_POINT ( 'NONE',  ( 11.76794919243112325, 17.42999999999999972, 1.734723475976807094E-15 ) ) ;
#7365=FACE_OUTER_BOUND ( 'NONE', #1626, .T. ) ;
#7370=CYLINDRICAL_SURFACE ( 'NONE', #4537, 12.00000000000000178 ) ;
#7375=EDGE_CURVE ( 'NONE', #14459, #9696, #4363, .T. ) ;
#7385=EDGE_LOOP ( 'NONE', ( #8732, #10405, #14565, #11853 ) ) ;
#7387=( BOUNDED_CURVE ( )  B_SPLINE_CURVE ( 2, ( #1750, #8584, #520, #11307, #15347, #17118, #2170, #12974, #693, #16945, #6267, #12808, #10170 ),
 .UNSPECIFIED., .F., .F. ) 
 B_SPLINE_CURVE_WITH_KNOTS ( ( 3, 2, 2, 2, 2, 2, 3 ),
 ( 0.4583333333333333148, 0.4611111111111111382, 0.4666666666666666741, 0.4722222222222222099, 0.4777777777777778012, 0.4833333333333333370, 0.4861111111111111049 ),
 .UNSPECIFIED. ) 
 CURVE ( )  GEOMETRIC_REPRESENTATION_ITEM ( )  RATIONAL_B_SPLINE_CURVE ( ( 0.9755282581475768211, 0.9755282581475765991, 1.000000000000000000, 0.9510565162951535312, 1.000000000000000000, 0.9510565162951535312, 1.000000000000000000, 0.9510565162951535312, 1.000000000000000000, 0.9510565162951535312, 1.000000000000000000, 0.9755282581475768211, 0.9755282581475768211 ) ) 
 REPRESENTATION_ITEM ( '' )  );
#7389=VERTEX_POINT ( 'NONE', #2248 ) ;
#7390=CARTESIAN_POINT ( 'NONE',  ( 10.92172942406179104, 30.73000000000000753, -7.935100905948385908 ) ) ;
#7395=ADVANCED_FACE ( 'NONE', ( #7676 ), #13055, .F. ) ;
#7397=CARTESIAN_POINT ( 'NONE',  ( 17.32050807568873552, 0.000000000000000000, 8.000000000000085265 ) ) ;
#7400=ORIENTED_EDGE ( 'NONE', *, *, #8549, .T. ) ;
#7403=AXIS2_PLACEMENT_3D ( 'NONE', #7689, #15698, #14636 ) ;
#7404=DIRECTION ( 'NONE',  ( 6.313931023057711093E-15, -0.000000000000000000, -1.000000000000000000 ) ) ;
#7408=CARTESIAN_POINT ( 'NONE',  ( -15.31970530204994674, 8.007293614239923585, 9.835827272001230526 ) ) ;
#7409=CARTESIAN_POINT ( 'NONE',  ( 16.03540712409202484, 8.027799080943070820, 8.457499700851130342 ) ) ;
#7410=DIRECTION ( 'NONE',  ( 0.000000000000000000, 1.000000000000000000, 0.000000000000000000 ) ) ;
#7412=CARTESIAN_POINT ( 'NONE',  ( 11.76794919243112680, 26.57999999999999829, -3.823638476888993942 ) ) ;
#7415=EDGE_CURVE ( 'NONE', #309, #2603, #3923, .T. ) ;
#7417=CARTESIAN_POINT ( 'NONE',  ( -7.409984580736203970E-16, -16.32000000000000028, 12.37355403259654985 ) ) ;
#7419=CIRCLE ( 'NONE', #16428, 26.00000000000000355 ) ;
#7420=CARTESIAN_POINT ( 'NONE',  ( 0.000000000000000000, 5.918584287042170544, 0.000000000000000000 ) ) ;
#7421=CARTESIAN_POINT ( 'NONE',  ( -11.76794919243112325, -1.920000000000006590, 3.823638476888994386 ) ) ;
#7424=CARTESIAN_POINT ( 'NONE',  ( -2.970370385949441694, 7.170662809914418290, 21.14483242576212163 ) ) ;
#7428=CARTESIAN_POINT ( 'NONE',  ( 10.35194220012931154, 7.925732005390763391, -15.34409809138587022 ) ) ;
#7429=CARTESIAN_POINT ( 'NONE',  ( 10.00000000000135891, 7.983052681821872554, -15.32050807568352191 ) ) ;
#7430=CARTESIAN_POINT ( 'NONE',  ( 10.92172942406178926, 25.13000000000001322, 7.935100905948385908 ) ) ;
#7432=DIRECTION ( 'NONE',  ( -0.000000000000000000, -1.000000000000000000, -0.000000000000000000 ) ) ;
#7444=FACE_OUTER_BOUND ( 'NONE', #13728, .T. ) ;
#7445=DIRECTION ( 'NONE',  ( -0.5000000000000041078, 0.000000000000000000, 0.8660254037844363761 ) ) ;
#7449=CARTESIAN_POINT ( 'NONE',  ( 7.272992578804308828, 13.98000000000000220, 10.01041549318726709 ) ) ;
#7450=ORIENTED_EDGE ( 'NONE', *, *, #10587, .F. ) ;
#7454=CARTESIAN_POINT ( 'NONE',  ( -10.92172942406178926, 1.629999999999992566, -7.935100905948389460 ) ) ;
#7474=ORIENTED_EDGE ( 'NONE', *, *, #4672, .F. ) ;
#7475=EDGE_LOOP ( 'NONE', ( #3931, #4286, #8907, #8947 ) ) ;
#7476=CARTESIAN_POINT ( 'NONE',  ( -13.49999999999999822, 32.08000000000001251, 4.386415899144235908 ) ) ;
#7482=CARTESIAN_POINT ( 'NONE',  ( 7.329991333342587012, -1.736202706843530252E-17, -9.501117147637041072 ) ) ;
#7483=CARTESIAN_POINT ( 'NONE',  ( -1.539363535742758637, 7.854661454367255935, 18.71158131929041701 ) ) ;
#7486=( BOUNDED_SURFACE ( )  B_SPLINE_SURFACE ( 1, 2, ( 
 ( #13679, #15174, #12370, #11227, #12550, #16513, #16601, #1577, #4420, #4594, #3250, #4328, #9736, #8412, #1664, #12463, #3074, #8500, #436, #13850, #1753, #5844, #11310, #14031, #4508, #15262, #1919, #3160, #1832, #7249, #12282, #177, #11489, #15438, #4767, #10338, #5025, #11573, #6269, #695, #7339, #12893, #8928, #12722, #16774, #2172, #4682, #8762, #609, #3599, #7511, #2004, #7430, #10172, #11656, #15521, #2257, #8848, #7685, #16948, #4849, #7598, #12976, #859, #946, #6359, #17120, #15784, #3693, #10763, #10848, #2429, #6619, #2691, #6791, #13400, #11915, #6703, #5296, #17463, #7860, #11999, #6447, #14631, #12171, #4127, #2516, #2346, #62, #13235, #5120, #7778, #15874, #9193, #17293, #5206, #10596, #15958, #9279, #7945, #16664, #12787, #4658, #673, #11550, #11465, #16841, #10149, #6777, #14965, #10815, #16273, #16010, #16178, #9678, #15028, #9333, #8000, #14682, #2570, #1338, #13368, #4089, #114, #9505, #12052, #6844, #5611, #1607, #1257, #10903, #16361, #14766, #6934, #2833, #6669, #14851, #16094, #17430, #9418, #9591, #2921, #2744, #4179, #5343, #7023, #5426, #13538, #5261, #3916, #1427, #10729, #4002, #17349, #8264, #6755, #10647, #2658, #8088, #14942, #13452, #13624, #12134, #1517, #23, #8174, #12221, #5520, #12312, #205, #10993, #4268, #8351, #13708, #3282, #3608, #12491, #11252, #8698, #376, #15701, #4621, #13878, #5782, #12659, #13793, #7107, #15111, #14059, #11167, #290, #16631, #3009, #1779, #16543, #4534, #9020, #11080, #1862, #8439, #16453, #7188, #7276, #9941, #15290, #1692, #4356, #3191, #14376, #4449, #8613, #9765, #5873, #9856, #13965, #7605, #548, #5699, #15202, #3102, #866, #8530, #5958, #12577, #465, #11338, #2264, #6276, #16715, #10027, #12402, #15375, #2179, #12983, #11664, #17040, #4945, #10346, #6453, #9112, #3787, #5213, #3958, #5303, #11839, #1296, #4044, #10516, #17388, #10685, #6367, #5384, #9458, #12088, #8040, #15967, #6627, #5126, #9371, #13242, #6710, #3699, #16132, #13157, #2353, #9200, #17471, #14551, #17215, #10769, #1131, #6542, #14721, #1043, #13407, #17301, #9286, #13070, #14464, #2525, #7785, #2609, #7954, #16051, #13324, #1216, #11750, #12006, #14806, #7691, #955, #17126, #5034, #10433, #15792, #12533, #69, #1383, #16495, #8220, #14984, #2789, #11121, #12355, #5826, #9811, #4221, #9899, #8484, #8309, #5740, #4134, #13664, #249, #12264, #16584, #161, #4400, #1559, #2699, #12446, #1648, #8128, #1473, #16315, #6800, #2965, #5474, #7064, #5566, #12178, #10855, #4489, #331, #16222, #15157, #9546, #3056, #14895, #13581, #9635, #6891, #10948, #8395, #2876, #5654, #6980, #11036, #13835, #11210, #16408, #4309, #1735, #9721, #13749 ),
 ( #419, #7148, #5914, #1904, #3330, #3419, #4751, #3236, #7499, #4837, #14011, #10157, #15507, #8569, #11558, #10240, #768, #2074, #8745, #6092, #7321, #8833, #11385, #12879, #506, #16934, #9985, #16672, #8656, #6176, #12705, #15333, #15594, #592, #6003, #14190, #16758, #15246, #4665, #10072, #13922, #11293, #15423, #4578, #3144, #14102, #1816, #16849, #1987, #7412, #12794, #680, #11472, #7230, #12618, #4553, #4467, #9872, #1443, #8280, #6861, #3119, #6951, #8368, #222, #13896, #9783, #5536, #481, #15043, #11009, #16380, #7041, #4285, #9695, #12419, #15130, #2939, #3027, #8457, #7123, #8032, #14884, #14711, #3947, #15777, #3776, #1119, #3688, #5292, #13145, #9361, #2422, #1033, #17459, #15869, #14454, #9274, #11827, #5202, #14537, #3860, #13484, #2341, #10674, #5114, #7856, #10592, #9447, #16039, #13231, #2599, #2512, #8028, #14627, #1205, #1285, #5372, #4033, #12166, #14795, #5020, #2687, #8118, #1548, #11111, #3224, #13998, #8731, #2063, #12101, #5486, #13255, #15979, #14563, #9300, #1142, #4145, #6723, #6553, #8055, #5227, #9470, #5398, #14734, #2712, #11933, #2622, #12279, #10529, #17313, #10612, #3882, #14650, #17399, #2538, #17483, #10782, #16147, #7966, #8141, #15891, #16065, #1396, #6812, #82, #2304, #7908, #3827, #11702, #9155, #3650, #13023, #14416, #10559, #10640, #5078, #17254, #10386, #14677, #15833, #7826, #3560, #14330, #13197, #2219, #7646, #15650, #14595, #17168, #905, #6316, #8974, #6582, #15740, #5253, #9063, #16004, #17079, #7732, #1083, #13108, #2390, #13283, #3738, #15918, #11791, #6496, #3910, #4984, #11879, #1171, #995, #5167, #6408, #9242, #2475, #11963, #17342, #9327, #11216, #1994, #6099, #9905, #427, #13928, #15341, #3338, #4673, #15252, #686, #10164, #8577, #10078, #15429, #15165, #11480, #15512, #16855, #7421, #3241, #6011, #1822, #8753, #5920, #4758, #12540, #3424, #16590, #4498, #3151, #4408, #7238, #12624, #9818, #16678, #512, #3063, #11301, #8490, #4585, #9993, #1743, #8664, #14021, #1911, #13841, #7329, #7155, #5833, #12712, #16765, #599, #11393, #10683, #158, #14893, #12262, #6798, #67, #1471, #2523, #15965, #16220, #12004, #1294, #17386, #4132, #5382, #5564, #9544, #2607, #16313, #2787, #12086, #5472, #13322, #17469, #16130, #16049, #17299, #4041, #7951, #8126, #1214, #6625, #5301, #9369, #9456, #1381, #3956, #8038, #12176, #14804, #2697, #13493, #8218, #13579, #8661, #15337, #4669, #4754, #1908, #3335, #14017, #8749, #7325, #14107, #683, #1991, #12709, #6007, #11390, #6096, #16762, #7417, #12799, #11476, #16852, #9990, #12537, #15161, #15070, #11041, #12450, #3060, #8399, #335, #5744, #1738, #11127, #424, #16501, #16412, #4405 ) ),
 .UNSPECIFIED., .F., .F., .F. ) 
 B_SPLINE_SURFACE_WITH_KNOTS ( ( 2, 2 ),
 ( 3, 2, 2, 2, 2, 2, 2, 2, 2, 2, 2, 2, 2, 2, 2, 2, 2, 2, 2, 2, 2, 2, 2, 2, 2, 2, 2, 2, 2, 2, 2, 2, 2, 2, 2, 2, 2, 2, 2, 2, 2, 2, 2, 2, 2, 2, 2, 2, 2, 2, 2, 2, 2, 2, 2, 2, 2, 2, 2, 2, 2, 2, 2, 2, 2, 2, 2, 2, 2, 2, 2, 2, 2, 2, 2, 2, 2, 2, 2, 2, 2, 2, 2, 2, 2, 2, 2, 2, 2, 2, 2, 2, 2, 2, 2, 2, 2, 2, 2, 2, 2, 2, 2, 2, 2, 2, 2, 2, 2, 2, 2, 2, 2, 2, 2, 2, 2, 2, 2, 2, 2, 2, 2, 2, 2, 2, 2, 2, 2, 2, 2, 2, 2, 2, 2, 2, 2, 2, 2, 2, 2, 2, 2, 2, 2, 2, 2, 2, 2, 2, 2, 2, 2, 2, 2, 2, 2, 2, 2, 2, 2, 2, 2, 2, 2, 2, 2, 2, 2, 2, 2, 2, 2, 2, 2, 2, 2, 3 ),
 ( 0.000000000000000000, 1.000000000000000000 ),
 ( 0.000000000000000000, 0.005555555555555555768, 0.01111111111111111154, 0.01666666666666666644, 0.02222222222222222307, 0.02777777777777777624, 0.03333333333333333287, 0.03888888888888888951, 0.04444444444444444614, 0.05000000000000000278, 0.05555555555555555247, 0.06111111111111110911, 0.06666666666666666574, 0.07222222222222221544, 0.07777777777777777901, 0.08333333333333332871, 0.08888888888888889228, 0.09444444444444444198, 0.1000000000000000056, 0.1055555555555555552, 0.1111111111111111049, 0.1166666666666666685, 0.1222222222222222182, 0.1277777777777777679, 0.1333333333333333315, 0.1388888888888888951, 0.1444444444444444309, 0.1499999999999999944, 0.1555555555555555580, 0.1611111111111111216, 0.1666666666666666574, 0.1722222222222222210, 0.1777777777777777846, 0.1833333333333333204, 0.1888888888888888840, 0.1944444444444444475, 0.2000000000000000111, 0.2055555555555555469, 0.2111111111111111105, 0.2166666666666666741, 0.2222222222222222099, 0.2277777777777777735, 0.2333333333333333370, 0.2388888888888889006, 0.2444444444444444364, 0.2500000000000000000, 0.2555555555555555358, 0.2611111111111111271, 0.2666666666666666630, 0.2722222222222221988, 0.2777777777777777901, 0.2833333333333333259, 0.2888888888888888618, 0.2944444444444444531, 0.2999999999999999889, 0.3055555555555555802, 0.3111111111111111160, 0.3166666666666666519, 0.3222222222222222432, 0.3277777777777777790, 0.3333333333333333148, 0.3388888888888889062, 0.3444444444444444420, 0.3499999999999999778, 0.3555555555555555691, 0.3611111111111111049, 0.3666666666666666408, 0.3722222222222222321, 0.3777777777777777679, 0.3833333333333333592, 0.3888888888888888951, 0.3944444444444444309, 0.4000000000000000222, 0.4055555555555555580, 0.4111111111111110938, 0.4166666666666666852, 0.4222222222222222210, 0.4277777777777777568, 0.4333333333333333481, 0.4388888888888888840, 0.4444444444444444198, 0.4500000000000000111, 0.4555555555555555469, 0.4611111111111111382, 0.4666666666666666741, 0.4722222222222222099, 0.4777777777777778012, 0.4833333333333333370, 0.4888888888888888729, 0.4944444444444444642, 0.5000000000000000000, 0.5055555555555555358, 0.5111111111111110716, 0.5166666666666667185, 0.5222222222222222543, 0.5277777777777777901, 0.5333333333333333259, 0.5388888888888888618, 0.5444444444444443976, 0.5500000000000000444, 0.5555555555555555802, 0.5611111111111111160, 0.5666666666666666519, 0.5722222222222221877, 0.5777777777777777235, 0.5833333333333333703, 0.5888888888888889062, 0.5944444444444444420, 0.5999999999999999778, 0.6055555555555555136, 0.6111111111111111605, 0.6166666666666666963, 0.6222222222222222321, 0.6277777777777777679, 0.6333333333333333037, 0.6388888888888888395, 0.6444444444444444864, 0.6500000000000000222, 0.6555555555555555580, 0.6611111111111110938, 0.6666666666666666297, 0.6722222222222222765, 0.6777777777777778123, 0.6833333333333333481, 0.6888888888888888840, 0.6944444444444444198, 0.6999999999999999556, 0.7055555555555556024, 0.7111111111111111382, 0.7166666666666666741, 0.7222222222222222099, 0.7277777777777777457, 0.7333333333333332815, 0.7388888888888889284, 0.7444444444444444642, 0.7500000000000000000, 0.7555555555555555358, 0.7611111111111110716, 0.7666666666666667185, 0.7722222222222222543, 0.7777777777777777901, 0.7833333333333333259, 0.7888888888888888618, 0.7944444444444443976, 0.8000000000000000444, 0.8055555555555555802, 0.8111111111111111160, 0.8166666666666666519, 0.8222222222222221877, 0.8277777777777777235, 0.8333333333333333703, 0.8388888888888889062, 0.8444444444444444420, 0.8499999999999999778, 0.8555555555555555136, 0.8611111111111111605, 0.8666666666666666963, 0.8722222222222222321, 0.8777777777777777679, 0.8833333333333333037, 0.8888888888888888395, 0.8944444444444444864, 0.9000000000000000222, 0.9055555555555555580, 0.9111111111111110938, 0.9166666666666666297, 0.9222222222222222765, 0.9277777777777778123, 0.9333333333333333481, 0.9388888888888888840, 0.9444444444444444198, 0.9499999999999999556, 0.9555555555555556024, 0.9611111111111111382, 0.9666666666666666741, 0.9722222222222222099, 0.9777777777777777457, 0.9814746806989694816 ),
 .UNSPECIFIED. ) 
 GEOMETRIC_REPRESENTATION_ITEM ( )  RATIONAL_B_SPLINE_SURFACE ( (
 ( 1.000000000000000000, 0.9510565162951535312, 1.000000000000000000, 0.9510565162951535312, 1.000000000000000000, 0.9510565162951535312, 1.000000000000000000, 0.9510565162951535312, 1.000000000000000000, 0.9510565162951535312, 1.000000000000000000, 0.9510565162951535312, 1.000000000000000000, 0.9510565162951535312, 1.000000000000000000, 0.9510565162951535312, 1.000000000000000000, 0.9510565162951535312, 1.000000000000000000, 0.9510565162951535312, 1.000000000000000000, 0.9510565162951535312, 1.000000000000000000, 0.9510565162951535312, 1.000000000000000000, 0.9510565162951535312, 1.000000000000000000, 0.9510565162951535312, 1.000000000000000000, 0.9510565162951535312, 1.000000000000000000, 0.9510565162951535312, 1.000000000000000000, 0.9510565162951535312, 1.000000000000000000, 0.9510565162951535312, 1.000000000000000000, 0.9510565162951535312, 1.000000000000000000, 0.9510565162951535312, 1.000000000000000000, 0.9510565162951535312, 1.000000000000000000, 0.9510565162951535312, 1.000000000000000000, 0.9510565162951535312, 1.000000000000000000, 0.9510565162951535312, 1.000000000000000000, 0.9510565162951535312, 1.000000000000000000, 0.9510565162951535312, 1.000000000000000000, 0.9510565162951535312, 1.000000000000000000, 0.9510565162951535312, 1.000000000000000000, 0.9510565162951535312, 1.000000000000000000, 0.9510565162951535312, 1.000000000000000000, 0.9510565162951535312, 1.000000000000000000, 0.9510565162951535312, 1.000000000000000000, 0.9510565162951535312, 1.000000000000000000, 0.9510565162951535312, 1.000000000000000000, 0.9510565162951535312, 1.000000000000000000, 0.9510565162951535312, 1.000000000000000000, 0.9510565162951535312, 1.000000000000000000, 0.9510565162951535312, 1.000000000000000000, 0.9510565162951535312, 1.000000000000000000, 0.9510565162951535312, 1.000000000000000000, 0.9510565162951535312, 1.000000000000000000, 0.9510565162951535312, 1.000000000000000000, 0.9510565162951535312, 1.000000000000000000, 0.9510565162951535312, 1.000000000000000000, 0.9510565162951535312, 1.000000000000000000, 0.9510565162951535312, 1.000000000000000000, 0.9510565162951535312, 1.000000000000000000, 0.9510565162951535312, 1.000000000000000000, 0.9510565162951535312, 1.000000000000000000, 0.9510565162951535312, 1.000000000000000000, 0.9510565162951535312, 1.000000000000000000, 0.9510565162951535312, 1.000000000000000000, 0.9510565162951535312, 1.000000000000000000, 0.9510565162951535312, 1.000000000000000000, 0.9510565162951535312, 1.000000000000000000, 0.9510565162951535312, 1.000000000000000000, 0.9510565162951535312, 1.000000000000000000, 0.9510565162951535312, 1.000000000000000000, 0.9510565162951535312, 1.000000000000000000, 0.9510565162951535312, 1.000000000000000000, 0.9510565162951535312, 1.000000000000000000, 0.9510565162951535312, 1.000000000000000000, 0.9510565162951535312, 1.000000000000000000, 0.9510565162951535312, 1.000000000000000000, 0.9510565162951535312, 1.000000000000000000, 0.9510565162951535312, 1.000000000000000000, 0.9510565162951535312, 1.000000000000000000, 0.9510565162951535312, 1.000000000000000000, 0.9510565162951535312, 1.000000000000000000, 0.9510565162951535312, 1.000000000000000000, 0.9510565162951535312, 1.000000000000000000, 0.9510565162951535312, 1.000000000000000000, 0.9510565162951535312, 1.000000000000000000, 0.9510565162951535312, 1.000000000000000000, 0.9510565162951535312, 1.000000000000000000, 0.9510565162951535312, 1.000000000000000000, 0.9510565162951535312, 1.000000000000000000, 0.9510565162951535312, 1.000000000000000000, 0.9510565162951535312, 1.000000000000000000, 0.9510565162951535312, 1.000000000000000000, 0.9510565162951535312, 1.000000000000000000, 0.9510565162951535312, 1.000000000000000000, 0.9510565162951535312, 1.000000000000000000, 0.9510565162951535312, 1.000000000000000000, 0.9510565162951535312, 1.000000000000000000, 0.9510565162951535312, 1.000000000000000000, 0.9510565162951535312, 1.000000000000000000, 0.9510565162951535312, 1.000000000000000000, 0.9510565162951535312, 1.000000000000000000, 0.9510565162951535312, 1.000000000000000000, 0.9510565162951535312, 1.000000000000000000, 0.9510565162951535312, 1.000000000000000000, 0.9510565162951535312, 1.000000000000000000, 0.9510565162951535312, 1.000000000000000000, 0.9510565162951535312, 1.000000000000000000, 0.9510565162951535312, 1.000000000000000000, 0.9510565162951535312, 1.000000000000000000, 0.9510565162951535312, 1.000000000000000000, 0.9510565162951535312, 1.000000000000000000, 0.9510565162951535312, 1.000000000000000000, 0.9510565162951535312, 1.000000000000000000, 0.9510565162951535312, 1.000000000000000000, 0.9510565162951535312, 1.000000000000000000, 0.9510565162951535312, 1.000000000000000000, 0.9510565162951535312, 1.000000000000000000, 0.9510565162951535312, 1.000000000000000000, 0.9510565162951535312, 1.000000000000000000, 0.9510565162951535312, 1.000000000000000000, 0.9510565162951535312, 1.000000000000000000, 0.9510565162951535312, 1.000000000000000000, 0.9510565162951535312, 1.000000000000000000, 0.9510565162951535312, 1.000000000000000000, 0.9510565162951535312, 1.000000000000000000, 0.9510565162951535312, 1.000000000000000000, 0.9510565162951535312, 1.000000000000000000, 0.9510565162951535312, 1.000000000000000000, 0.9510565162951535312, 1.000000000000000000, 0.9510565162951535312, 1.000000000000000000, 0.9510565162951535312, 1.000000000000000000, 0.9510565162951535312, 1.000000000000000000, 0.9510565162951535312, 1.000000000000000000, 0.9510565162951535312, 1.000000000000000000, 0.9510565162951535312, 1.000000000000000000, 0.9510565162951535312, 1.000000000000000000, 0.9510565162951535312, 1.000000000000000000, 0.9510565162951535312, 1.000000000000000000, 0.9510565162951535312, 1.000000000000000000, 0.9510565162951535312, 1.000000000000000000, 0.9510565162951535312, 1.000000000000000000, 0.9510565162951535312, 1.000000000000000000, 0.9510565162951535312, 1.000000000000000000, 0.9510565162951535312, 1.000000000000000000, 0.9510565162951535312, 1.000000000000000000, 0.9510565162951535312, 1.000000000000000000, 0.9510565162951535312, 1.000000000000000000, 0.9510565162951535312, 1.000000000000000000, 0.9510565162951535312, 1.000000000000000000, 0.9510565162951535312, 1.000000000000000000, 0.9510565162951535312, 1.000000000000000000, 0.9510565162951535312, 1.000000000000000000, 0.9510565162951535312, 1.000000000000000000, 0.9510565162951535312, 1.000000000000000000, 0.9510565162951535312, 1.000000000000000000, 0.9510565162951535312, 1.000000000000000000, 0.9510565162951535312, 1.000000000000000000, 0.9510565162951535312, 1.000000000000000000, 0.9510565162951535312, 1.000000000000000000, 0.9510565162951535312, 1.000000000000000000, 0.9510565162951535312, 1.000000000000000000, 0.9510565162951535312, 1.000000000000000000, 0.9510565162951535312, 1.000000000000000000, 0.9510565162951535312, 1.000000000000000000, 0.9510565162951535312, 1.000000000000000000, 0.9510565162951535312, 1.000000000000000000, 0.9510565162951535312, 1.000000000000000000, 0.9510565162951535312, 1.000000000000000000, 0.9510565162951535312, 1.000000000000000000, 0.9510565162951535312, 1.000000000000000000, 0.9510565162951535312, 1.000000000000000000, 0.9510565162951535312, 1.000000000000000000, 0.9510565162951535312, 1.000000000000000000, 0.9510565162951535312, 1.000000000000000000, 0.9510565162951535312, 1.000000000000000000, 0.9510565162951535312, 1.000000000000000000, 0.9510565162951535312, 1.000000000000000000, 0.9510565162951535312, 1.000000000000000000, 0.9510565162951535312, 1.000000000000000000, 0.9510565162951535312, 1.000000000000000000, 0.9510565162951535312, 1.000000000000000000, 0.9510565162951535312, 1.000000000000000000, 0.9510565162951535312, 1.000000000000000000, 0.9510565162951535312, 1.000000000000000000, 0.9510565162951535312, 1.000000000000000000, 0.9510565162951535312, 1.000000000000000000, 0.9510565162951535312, 1.000000000000000000, 0.9510565162951535312, 1.000000000000000000, 0.9674309245812854341, 0.9782075447827165426),
 ( 1.000000000000000000, 0.9510565162951535312, 1.000000000000000000, 0.9510565162951535312, 1.000000000000000000, 0.9510565162951535312, 1.000000000000000000, 0.9510565162951535312, 1.000000000000000000, 0.9510565162951535312, 1.000000000000000000, 0.9510565162951535312, 1.000000000000000000, 0.9510565162951535312, 1.000000000000000000, 0.9510565162951535312, 1.000000000000000000, 0.9510565162951535312, 1.000000000000000000, 0.9510565162951535312, 1.000000000000000000, 0.9510565162951535312, 1.000000000000000000, 0.9510565162951535312, 1.000000000000000000, 0.9510565162951535312, 1.000000000000000000, 0.9510565162951535312, 1.000000000000000000, 0.9510565162951535312, 1.000000000000000000, 0.9510565162951535312, 1.000000000000000000, 0.9510565162951535312, 1.000000000000000000, 0.9510565162951535312, 1.000000000000000000, 0.9510565162951535312, 1.000000000000000000, 0.9510565162951535312, 1.000000000000000000, 0.9510565162951535312, 1.000000000000000000, 0.9510565162951535312, 1.000000000000000000, 0.9510565162951535312, 1.000000000000000000, 0.9510565162951535312, 1.000000000000000000, 0.9510565162951535312, 1.000000000000000000, 0.9510565162951535312, 1.000000000000000000, 0.9510565162951535312, 1.000000000000000000, 0.9510565162951535312, 1.000000000000000000, 0.9510565162951535312, 1.000000000000000000, 0.9510565162951535312, 1.000000000000000000, 0.9510565162951535312, 1.000000000000000000, 0.9510565162951535312, 1.000000000000000000, 0.9510565162951535312, 1.000000000000000000, 0.9510565162951535312, 1.000000000000000000, 0.9510565162951535312, 1.000000000000000000, 0.9510565162951535312, 1.000000000000000000, 0.9510565162951535312, 1.000000000000000000, 0.9510565162951535312, 1.000000000000000000, 0.9510565162951535312, 1.000000000000000000, 0.9510565162951535312, 1.000000000000000000, 0.9510565162951535312, 1.000000000000000000, 0.9510565162951535312, 1.000000000000000000, 0.9510565162951535312, 1.000000000000000000, 0.9510565162951535312, 1.000000000000000000, 0.9510565162951535312, 1.000000000000000000, 0.9510565162951535312, 1.000000000000000000, 0.9510565162951535312, 1.000000000000000000, 0.9510565162951535312, 1.000000000000000000, 0.9510565162951535312, 1.000000000000000000, 0.9510565162951535312, 1.000000000000000000, 0.9510565162951535312, 1.000000000000000000, 0.9510565162951535312, 1.000000000000000000, 0.9510565162951535312, 1.000000000000000000, 0.9510565162951535312, 1.000000000000000000, 0.9510565162951535312, 1.000000000000000000, 0.9510565162951535312, 1.000000000000000000, 0.9510565162951535312, 1.000000000000000000, 0.9510565162951535312, 1.000000000000000000, 0.9510565162951535312, 1.000000000000000000, 0.9510565162951535312, 1.000000000000000000, 0.9510565162951535312, 1.000000000000000000, 0.9510565162951535312, 1.000000000000000000, 0.9510565162951535312, 1.000000000000000000, 0.9510565162951535312, 1.000000000000000000, 0.9510565162951535312, 1.000000000000000000, 0.9510565162951535312, 1.000000000000000000, 0.9510565162951535312, 1.000000000000000000, 0.9510565162951535312, 1.000000000000000000, 0.9510565162951535312, 1.000000000000000000, 0.9510565162951535312, 1.000000000000000000, 0.9510565162951535312, 1.000000000000000000, 0.9510565162951535312, 1.000000000000000000, 0.9510565162951535312, 1.000000000000000000, 0.9510565162951535312, 1.000000000000000000, 0.9510565162951535312, 1.000000000000000000, 0.9510565162951535312, 1.000000000000000000, 0.9510565162951535312, 1.000000000000000000, 0.9510565162951535312, 1.000000000000000000, 0.9510565162951535312, 1.000000000000000000, 0.9510565162951535312, 1.000000000000000000, 0.9510565162951535312, 1.000000000000000000, 0.9510565162951535312, 1.000000000000000000, 0.9510565162951535312, 1.000000000000000000, 0.9510565162951535312, 1.000000000000000000, 0.9510565162951535312, 1.000000000000000000, 0.9510565162951535312, 1.000000000000000000, 0.9510565162951535312, 1.000000000000000000, 0.9510565162951535312, 1.000000000000000000, 0.9510565162951535312, 1.000000000000000000, 0.9510565162951535312, 1.000000000000000000, 0.9510565162951535312, 1.000000000000000000, 0.9510565162951535312, 1.000000000000000000, 0.9510565162951535312, 1.000000000000000000, 0.9510565162951535312, 1.000000000000000000, 0.9510565162951535312, 1.000000000000000000, 0.9510565162951535312, 1.000000000000000000, 0.9510565162951535312, 1.000000000000000000, 0.9510565162951535312, 1.000000000000000000, 0.9510565162951535312, 1.000000000000000000, 0.9510565162951535312, 1.000000000000000000, 0.9510565162951535312, 1.000000000000000000, 0.9510565162951535312, 1.000000000000000000, 0.9510565162951535312, 1.000000000000000000, 0.9510565162951535312, 1.000000000000000000, 0.9510565162951535312, 1.000000000000000000, 0.9510565162951535312, 1.000000000000000000, 0.9510565162951535312, 1.000000000000000000, 0.9510565162951535312, 1.000000000000000000, 0.9510565162951535312, 1.000000000000000000, 0.9510565162951535312, 1.000000000000000000, 0.9510565162951535312, 1.000000000000000000, 0.9510565162951535312, 1.000000000000000000, 0.9510565162951535312, 1.000000000000000000, 0.9510565162951535312, 1.000000000000000000, 0.9510565162951535312, 1.000000000000000000, 0.9510565162951535312, 1.000000000000000000, 0.9510565162951535312, 1.000000000000000000, 0.9510565162951535312, 1.000000000000000000, 0.9510565162951535312, 1.000000000000000000, 0.9510565162951535312, 1.000000000000000000, 0.9510565162951535312, 1.000000000000000000, 0.9510565162951535312, 1.000000000000000000, 0.9510565162951535312, 1.000000000000000000, 0.9510565162951535312, 1.000000000000000000, 0.9510565162951535312, 1.000000000000000000, 0.9510565162951535312, 1.000000000000000000, 0.9510565162951535312, 1.000000000000000000, 0.9510565162951535312, 1.000000000000000000, 0.9510565162951535312, 1.000000000000000000, 0.9510565162951535312, 1.000000000000000000, 0.9510565162951535312, 1.000000000000000000, 0.9510565162951535312, 1.000000000000000000, 0.9510565162951535312, 1.000000000000000000, 0.9510565162951535312, 1.000000000000000000, 0.9510565162951535312, 1.000000000000000000, 0.9510565162951535312, 1.000000000000000000, 0.9510565162951535312, 1.000000000000000000, 0.9510565162951535312, 1.000000000000000000, 0.9510565162951535312, 1.000000000000000000, 0.9510565162951535312, 1.000000000000000000, 0.9510565162951535312, 1.000000000000000000, 0.9510565162951535312, 1.000000000000000000, 0.9510565162951535312, 1.000000000000000000, 0.9510565162951535312, 1.000000000000000000, 0.9510565162951535312, 1.000000000000000000, 0.9510565162951535312, 1.000000000000000000, 0.9510565162951535312, 1.000000000000000000, 0.9510565162951535312, 1.000000000000000000, 0.9510565162951535312, 1.000000000000000000, 0.9510565162951535312, 1.000000000000000000, 0.9510565162951535312, 1.000000000000000000, 0.9510565162951535312, 1.000000000000000000, 0.9510565162951535312, 1.000000000000000000, 0.9510565162951535312, 1.000000000000000000, 0.9510565162951535312, 1.000000000000000000, 0.9510565162951535312, 1.000000000000000000, 0.9510565162951535312, 1.000000000000000000, 0.9510565162951535312, 1.000000000000000000, 0.9510565162951535312, 1.000000000000000000, 0.9510565162951535312, 1.000000000000000000, 0.9510565162951535312, 1.000000000000000000, 0.9510565162951535312, 1.000000000000000000, 0.9510565162951535312, 1.000000000000000000, 0.9510565162951535312, 1.000000000000000000, 0.9510565162951535312, 1.000000000000000000, 0.9510565162951535312, 1.000000000000000000, 0.9510565162951535312, 1.000000000000000000, 0.9510565162951535312, 1.000000000000000000, 0.9510565162951535312, 1.000000000000000000, 0.9510565162951535312, 1.000000000000000000, 0.9510565162951535312, 1.000000000000000000, 0.9510565162951535312, 1.000000000000000000, 0.9510565162951535312, 1.000000000000000000, 0.9510565162951535312, 1.000000000000000000, 0.9510565162951535312, 1.000000000000000000, 0.9510565162951535312, 1.000000000000000000, 0.9674309245812854341, 0.9782075447827165426) ) ) 
 REPRESENTATION_ITEM ( '' )  SURFACE ( )  );
#7495=DIRECTION ( 'NONE',  ( 0.000000000000000000, 0.000000000000000000, 1.000000000000000000 ) ) ;
#7496=DIRECTION ( 'NONE',  ( 0.000000000000000000, 0.000000000000000000, -1.000000000000000000 ) ) ;
#7497=CARTESIAN_POINT ( 'NONE',  ( -10.92172942406178926, 5.629999999999996341, -7.935100905948389460 ) ) ;
#7499=CARTESIAN_POINT ( 'NONE',  ( 9.520470885617717371, 32.73000000000001108, -6.917026985038131848 ) ) ;
#7503=CARTESIAN_POINT ( 'NONE',  ( 18.99999999999999289, 7.773118517290098062, 1.732050807568941586 ) ) ;
#7506=LINE ( 'NONE', #7332, #3936 ) ;
#7509=CARTESIAN_POINT ( 'NONE',  ( 10.17549044795671165, 7.957350711246245822, -15.32050807568889539 ) ) ;
#7510=CARTESIAN_POINT ( 'NONE',  ( 8.197819711906403128, 7.962112819640459804, -16.44350439286869303 ) ) ;
#7511=CARTESIAN_POINT ( 'NONE',  ( 13.50000000000000000, 25.43000000000000682, 1.734723475976807094E-15 ) ) ;
#7513=ORIENTED_EDGE ( 'NONE', *, *, #6025, .F. ) ;
#7527=CARTESIAN_POINT ( 'NONE',  ( 19.00000000000000711, 7.773118517290098062, -1.732050807568807249 ) ) ;
#7529=CARTESIAN_POINT ( 'NONE',  ( 2.894739590358088936E-06, 0.6800804143413337055, 13.49999999999938360 ) ) ;
#7532=CARTESIAN_POINT ( 'NONE',  ( -9.520470885617717371, 13.23000000000001997, 6.917026985038133624 ) ) ;
#7538=CARTESIAN_POINT ( 'NONE',  ( 11.76794919243112680, 29.58000000000000540, -3.823638476888993942 ) ) ;
#7547=PLANE ( 'NONE',  #350 ) ;
#7551=LINE ( 'NONE', #14240, #185 ) ;
#7553=CARTESIAN_POINT ( 'NONE',  ( 24.73863375370599016, 5.918584287042170544, -7.999999999999936051 ) ) ;
#7555=EDGE_LOOP ( 'NONE', ( #15896, #1535, #15760, #63 ) ) ;
#7557=ORIENTED_EDGE ( 'NONE', *, *, #16322, .F. ) ;
#7559=VERTEX_POINT ( 'NONE', #16101 ) ;
#7560=CARTESIAN_POINT ( 'NONE',  ( 8.343458848123578520, 32.97999999999999687, 11.48378591275254124 ) ) ;
#7563=B_SPLINE_CURVE_WITH_KNOTS ( 'NONE', 3,
 ( #12685, #5722, #9615, #6958, #8376, #401, #1800, #14966, #8289, #1540, #12517, #16651, #229, #13732, #5634, #575, #10928, #16296 ),
 .UNSPECIFIED., .F., .F.,
 ( 4, 2, 2, 2, 2, 2, 2, 2, 4 ),
 ( 2.030049010680397961E-07, 0.0005272941439305969162, 0.001054385282960125948, 0.001581476421989654870, 0.002108567561019183793, 0.002635658700048712499, 0.003162749839078241639, 0.003689840978107770779, 0.004216932117137299485 ),
 .UNSPECIFIED. ) ;
#7568=CARTESIAN_POINT ( 'NONE',  ( 8.858858224111887836, 3.937340487231678143E-15, -8.306292331654377747 ) ) ;
#7569=CARTESIAN_POINT ( 'NONE',  ( 13.50000000000000000, 1.430000000000014593, 1.734723475976807094E-15 ) ) ;
#7571=DIRECTION ( 'NONE',  ( 0.000000000000000000, -1.000000000000000000, 0.000000000000000000 ) ) ;
#7575=VERTEX_POINT ( 'NONE', #4011 ) ;
#7576=CARTESIAN_POINT ( 'NONE',  ( 8.376189165296050732, 10.00005005279484038, 10.58723084571193596 ) ) ;
#7577=ORIENTED_EDGE ( 'NONE', *, *, #11541, .T. ) ;
#7578=CARTESIAN_POINT ( 'NONE',  ( 17.14738331135994187, 7.815232041205462998, -7.999999999999963585 ) ) ;
#7580=DIRECTION ( 'NONE',  ( 0.000000000000000000, 1.000000000000000000, 0.000000000000000000 ) ) ;
#7581=CYLINDRICAL_SURFACE ( 'NONE', #14058, 1.999999999999998224 ) ;
#7598=CARTESIAN_POINT ( 'NONE',  ( -13.49999999999999822, 23.77999999999999403, -4.386415899144240349 ) ) ;
#7599=ORIENTED_EDGE ( 'NONE', *, *, #1923, .F. ) ;
#7600=CARTESIAN_POINT ( 'NONE',  ( -8.343458848123582072, 9.379999999999999005, 11.48378591275253768 ) ) ;
#7601=CARTESIAN_POINT ( 'NONE',  ( 0.000000000000000000, 5.918584287042170544, 0.000000000000000000 ) ) ;
#7605=CARTESIAN_POINT ( 'NONE',  ( -8.549982208541774191E-16, 0.6799999999999988276, 14.19474002721660355 ) ) ;
#7607=B_SPLINE_CURVE_WITH_KNOTS ( 'NONE', 3,
 ( #16809, #644, #16552, #7286 ),
 .UNSPECIFIED., .F., .F.,
 ( 4, 4 ),
 ( 2.376698214937377243E-07, 0.007646667280170312518 ),
 .UNSPECIFIED. ) ;
#7609=( NAMED_UNIT ( * ) PLANE_ANGLE_UNIT ( ) SI_UNIT ( $, .RADIAN. ) );
#7615=CARTESIAN_POINT ( 'NONE',  ( 9.708203932499371192, 2.596025403784447683, -7.053423027509677645 ) ) ;
#7621=CARTESIAN_POINT ( 'NONE',  ( -9.520470885617717371, 10.23000000000000220, 6.917026985038133624 ) ) ;
#7629=DIRECTION ( 'NONE',  ( 0.5000000000000013323, 0.000000000000000000, -0.8660254037844379305 ) ) ;
#7631=CARTESIAN_POINT ( 'NONE',  ( -7.416407864998772581, 9.613974596215609125, -10.20780970022453360 ) ) ;
#7633=EDGE_CURVE ( 'NONE', #6360, #3099, #8182, .T. ) ;
#7646=CARTESIAN_POINT ( 'NONE',  ( 3.636496289402157078, 6.030000000000007354, -11.19198476289190936 ) ) ;
#7651=CARTESIAN_POINT ( 'NONE',  ( 10.92172942406179104, 33.73000000000001108, -7.935100905948385908 ) ) ;
#7659=EDGE_CURVE ( 'NONE', #1796, #2326, #15192, .T. ) ;
#7666=CARTESIAN_POINT ( 'NONE',  ( 15.58845726811984811, 0.000000000000000000, 11.00000000000007283 ) ) ;
#7671=CARTESIAN_POINT ( 'NONE',  ( 15.32106749056511852, 7.956441901775577641, 10.18076046065000817 ) ) ;
#7676=FACE_OUTER_BOUND ( 'NONE', #15542, .T. ) ;
#7680=DIRECTION ( 'NONE',  ( 0.000000000000000000, 1.000000000000000000, 0.000000000000000000 ) ) ;
#7685=CARTESIAN_POINT ( 'NONE',  ( -10.92172942406179104, 24.23000000000000043, 7.935100905948385908 ) ) ;
#7689=CARTESIAN_POINT ( 'NONE',  ( -8.000000000000145661, 0.000000000000000000, 17.32050807568870709 ) ) ;
#7691=CARTESIAN_POINT ( 'NONE',  ( 13.50000000000000355, -10.42000000000000703, -4.386415899144233244 ) ) ;
#7702=CIRCLE ( 'NONE', #8557, 2.000000000000001776 ) ;
#7705=ORIENTED_EDGE ( 'NONE', *, *, #13536, .F. ) ;
#7706=CARTESIAN_POINT ( 'NONE',  ( -7.272992578804310604, 13.37999999999999012, 10.01041549318726709 ) ) ;
#7707=ORIENTED_EDGE ( 'NONE', *, *, #9339, .T. ) ;
#7711=CARTESIAN_POINT ( 'NONE',  ( -13.49999999999999822, -1.220000000000006413, -4.386415899144240349 ) ) ;
#7717=CARTESIAN_POINT ( 'NONE',  ( 4.171729424061789260, 6.830000000000002736, 12.83926296998457239 ) ) ;
#7718=CIRCLE ( 'NONE', #8285, 26.00000000000000355 ) ;
#7722=CARTESIAN_POINT ( 'NONE',  ( -1.900613283885286720, 6.390856018535460592, -12.00000000000297007 ) ) ;
#7729=ORIENTED_EDGE ( 'NONE', *, *, #9920, .F. ) ;
#7732=CARTESIAN_POINT ( 'NONE',  ( -11.76794919243112325, 4.080000000000008065, 3.823638476888994386 ) ) ;
#7736=CARTESIAN_POINT ( 'NONE',  ( -13.50000000000000000, 25.93000000000000682, -3.469446951953614189E-15 ) ) ;
#7743=CARTESIAN_POINT ( 'NONE',  ( 12.05296456974564379, -3.033844236144862430E-15, -3.524706777039052330 ) ) ;
#7745=PRODUCT_DEFINITION_CONTEXT ( 'detailed design', #4161, 'design' ) ;
#7749=CYLINDRICAL_SURFACE ( 'NONE', #3281, 2.000000000000001776 ) ;
#7755=DIRECTION ( 'NONE',  ( 0.4999999999999946154, 0.000000000000000000, 0.8660254037844418162 ) ) ;
#7756=ORIENTED_EDGE ( 'NONE', *, *, #11157, .F. ) ;
#7757=CARTESIAN_POINT ( 'NONE',  ( -10.92172942406179104, 14.23000000000001997, 7.935100905948385908 ) ) ;
#7758=CARTESIAN_POINT ( 'NONE',  ( 11.76794919243112325, -12.71999999999999886, 3.823638476888996163 ) ) ;
#7762=DIRECTION ( 'NONE',  ( -0.000000000000000000, 1.000000000000000000, -0.000000000000000000 ) ) ;
#7765=B_SPLINE_CURVE_WITH_KNOTS ( 'NONE', 3,
 ( #14411, #14242, #16904, #15735 ),
 .UNSPECIFIED., .F., .F.,
 ( 4, 4 ),
 ( 0.008723199174958473981, 0.01636875612029862689 ),
 .UNSPECIFIED. ) ;
#7778=CARTESIAN_POINT ( 'NONE',  ( 13.49999999999999822, 19.27999999999999048, 4.386415899144237684 ) ) ;
#7779=ORIENTED_EDGE ( 'NONE', *, *, #5305, .T. ) ;
#7781=ADVANCED_FACE ( 'NONE', ( #16078 ), #11552, .T. ) ;
#7785=CARTESIAN_POINT ( 'NONE',  ( -13.50000000000000000, -9.070000000000002061, -3.469446951953614189E-15 ) ) ;
#7800=CARTESIAN_POINT ( 'NONE',  ( 2.279995255611139653E-15, 12.17999999999999972, -12.37355403259654985 ) ) ;
#7801=VERTEX_POINT ( 'NONE', #13435 ) ;
#7804=LINE ( 'NONE', #5054, #6832 ) ;
#7805=CARTESIAN_POINT ( 'NONE',  ( -8.549982208541774191E-16, 2.680000000000008153, 14.19474002721660355 ) ) ;
#7807=CYLINDRICAL_SURFACE ( 'NONE', #1740, 13.50000000000000000 ) ;
#7816=EDGE_CURVE ( 'NONE', #4526, #11897, #11559, .T. ) ;
#7826=CARTESIAN_POINT ( 'NONE',  ( -11.76794919243112325, 6.779999999999995808, -3.823638476888998827 ) ) ;
#7828=ORIENTED_EDGE ( 'NONE', *, *, #911, .T. ) ;
#7834=DIRECTION ( 'NONE',  ( 0.000000000000000000, -1.000000000000000000, 0.000000000000000000 ) ) ;
#7836=CYLINDRICAL_SURFACE ( 'NONE', #8838, 13.50000000000000000 ) ;
#7838=CARTESIAN_POINT ( 'NONE',  ( -19.29752010712865129, 5.918584287042170544, 17.42428528562837542 ) ) ;
#7854=ADVANCED_FACE ( 'NONE', ( #189 ), #5595, .F. ) ;
#7856=CARTESIAN_POINT ( 'NONE',  ( 3.636496289402157078, 18.03000000000001890, -11.19198476289190936 ) ) ;
#7857=DIRECTION ( 'NONE',  ( 0.000000000000000000, 0.000000000000000000, -1.000000000000000000 ) ) ;
#7860=CARTESIAN_POINT ( 'NONE',  ( -13.50000000000000000, 20.93000000000000327, -3.469446951953614189E-15 ) ) ;
#7861=VERTEX_POINT ( 'NONE', #4692 ) ;
#7862=CARTESIAN_POINT ( 'NONE',  ( -1.328658795546723038E-07, 9.679996299052479714, 13.49999999999999822 ) ) ;
#7864=CARTESIAN_POINT ( 'NONE',  ( 11.76794919243112325, 29.28000000000001180, 3.823638476888996163 ) ) ;
#7871=AXIS2_PLACEMENT_3D ( 'NONE', #12711, #2163, #16764 ) ;
#7879=ORIENTED_EDGE ( 'NONE', *, *, #12638, .F. ) ;
#7881=CARTESIAN_POINT ( 'NONE',  ( -7.272992578804307939, 3.479999999999997762, -10.01041549318726886 ) ) ;
#7886=CARTESIAN_POINT ( 'NONE',  ( 13.49999999999999822, -8.720000000000002416, 4.386415899144237684 ) ) ;
#7905=ORIENTED_EDGE ( 'NONE', *, *, #13634, .T. ) ;
#7908=CARTESIAN_POINT ( 'NONE',  ( 7.272992578804311492, 8.880000000000000782, -10.01041549318726709 ) ) ;
#7910=ORIENTED_EDGE ( 'NONE', *, *, #5848, .T. ) ;
#7911=CARTESIAN_POINT ( 'NONE',  ( -4.171729424061791036, 23.52999999999999403, 12.83926296998457239 ) ) ;
#7932=CARTESIAN_POINT ( 'NONE',  ( 10.69176227072922281, 7.854010657973331533, 15.43600950528676385 ) ) ;
#7934=EDGE_CURVE ( 'NONE', #11444, #9328, #12958, .T. ) ;
#7945=CARTESIAN_POINT ( 'NONE',  ( -13.49999999999999822, 18.08000000000000185, 4.386415899144235908 ) ) ;
#7946=ORIENTED_EDGE ( 'NONE', *, *, #13536, .T. ) ;
#7951=CARTESIAN_POINT ( 'NONE',  ( -9.520470885617715595, -11.36999999999999744, -6.917026985038136289 ) ) ;
#7953=ADVANCED_FACE ( 'NONE', ( #359 ), #13860, .F. ) ;
#7954=CARTESIAN_POINT ( 'NONE',  ( -10.92172942406178926, -9.369999999999995666, -7.935100905948389460 ) ) ;
#7966=CARTESIAN_POINT ( 'NONE',  ( -11.76794919243112325, 10.08000000000000718, 3.823638476888994386 ) ) ;
#7968=DIRECTION ( 'NONE',  ( -0.000000000000000000, -1.000000000000000000, -0.000000000000000000 ) ) ;
#7969=CARTESIAN_POINT ( 'NONE',  ( -9.520470885617715595, 3.629999999999994564, -6.917026985038136289 ) ) ;
#7973=CARTESIAN_POINT ( 'NONE',  ( 13.50000000000000000, -11.56999999999999673, 1.734723475976807094E-15 ) ) ;
#7977=EDGE_CURVE ( 'NONE', #14800, #13257, #4432, .T. ) ;
#7980=CARTESIAN_POINT ( 'NONE',  ( 1.653273178848926472E-15, 30.93000000000001393, 13.50000000000000000 ) ) ;
#7986=DIRECTION ( 'NONE',  ( 0.000000000000000000, 1.000000000000000000, 0.000000000000000000 ) ) ;
#7992=ORIENTED_EDGE ( 'NONE', *, *, #12689, .T. ) ;
#7996=VERTEX_POINT ( 'NONE', #12473 ) ;
#7997=CARTESIAN_POINT ( 'NONE',  ( 10.92172942406179104, 18.72999999999999687, -7.935100905948385908 ) ) ;
#8000=CARTESIAN_POINT ( 'NONE',  ( -8.343458848123582072, 15.37999999999999901, 11.48378591275254124 ) ) ;
#8016=ORIENTED_EDGE ( 'NONE', *, *, #3771, .T. ) ;
#8021=CARTESIAN_POINT ( 'NONE',  ( 8.022689779262613285, 7.854708479871425730, 16.97418022790854764 ) ) ;
#8028=CARTESIAN_POINT ( 'NONE',  ( 7.272992578804308828, 16.98000000000000753, 10.01041549318726709 ) ) ;
#8032=CARTESIAN_POINT ( 'NONE',  ( -11.76794919243112325, 21.77999999999999758, -3.823638476888998827 ) ) ;
#8035=CARTESIAN_POINT ( 'NONE',  ( -1.363343349470708815E-11, 9.313974596216116453, -12.00000000000000355 ) ) ;
#8038=CARTESIAN_POINT ( 'NONE',  ( 11.76794919243112325, -12.71999999999999886, 3.823638476888996163 ) ) ;
#8040=CARTESIAN_POINT ( 'NONE',  ( 4.171729424061789260, -5.170000000000000817, 12.83926296998457239 ) ) ;
#8046=VECTOR ( 'NONE', #14184, 1000.000000000000000 ) ;
#8049=EDGE_CURVE ( 'NONE', #2258, #3134, #13347, .T. ) ;
#8052=SHAPE_REPRESENTATION ( 'Nut', ( #16654 ), #11308 ) ;
#8055=CARTESIAN_POINT ( 'NONE',  ( -11.76794919243112325, 12.92999999999999616, -2.602085213965210642E-15 ) ) ;
#8057=CARTESIAN_POINT ( 'NONE',  ( -13.49999999999999822, 7.779999999999992255, -4.386415899144240349 ) ) ;
#8058=CARTESIAN_POINT ( 'NONE',  ( -3.636496289402152637, 3.329999999999999627, -11.19198476289190936 ) ) ;
#8062=CARTESIAN_POINT ( 'NONE',  ( 10.92172942406178926, -11.86999999999999922, 7.935100905948385908 ) ) ;
#8070=DIRECTION ( 'NONE',  ( 0.000000000000000000, 0.000000000000000000, -1.000000000000000000 ) ) ;
#8071=DIRECTION ( 'NONE',  ( -0.000000000000000000, -1.000000000000000000, -0.000000000000000000 ) ) ;
#8074=EDGE_CURVE ( 'NONE', #3274, #2674, #5057, .T. ) ;
#8083=ORIENTED_EDGE ( 'NONE', *, *, #17010, .T. ) ;
#8084=CARTESIAN_POINT ( 'NONE',  ( -13.49999999999999822, 22.77999999999999403, -4.386415899144240349 ) ) ;
#8088=CARTESIAN_POINT ( 'NONE',  ( -10.92172942406179104, 9.230000000000002203, 7.935100905948385908 ) ) ;
#8089=DIRECTION ( 'NONE',  ( -0.000000000000000000, -1.000000000000000000, -0.000000000000000000 ) ) ;
#8103=EDGE_LOOP ( 'NONE', ( #925, #12439, #8610, #781 ) ) ;
#8111=AXIS2_PLACEMENT_3D ( 'NONE', #2756, #9779, #8188 ) ;
#8118=CARTESIAN_POINT ( 'NONE',  ( -7.272992578804307939, 15.47999999999999865, -10.01041549318726886 ) ) ;
#8119=FACE_OUTER_BOUND ( 'NONE', #10296, .T. ) ;
#8122=ORIENTED_EDGE ( 'NONE', *, *, #14797, .F. ) ;
#8126=CARTESIAN_POINT ( 'NONE',  ( -7.272992578804307939, -11.51999999999999957, -10.01041549318726886 ) ) ;
#8128=CARTESIAN_POINT ( 'NONE',  ( -10.92172942406178926, -15.37000000000000099, -7.935100905948389460 ) ) ;
#8131=EDGE_CURVE ( 'NONE', #6426, #1275, #8316, .T. ) ;
#8141=CARTESIAN_POINT ( 'NONE',  ( -11.76794919243112325, 9.929999999999994387, -2.602085213965210642E-15 ) ) ;
#8144=CARTESIAN_POINT ( 'NONE',  ( -7.409984580736203970E-16, -1.320000000000003615, 12.37355403259654985 ) ) ;
#8148=CARTESIAN_POINT ( 'NONE',  ( -8.343458848123576743, -10.51999999999999780, -11.48378591275254301 ) ) ;
#8156=CARTESIAN_POINT ( 'NONE',  ( -3.556480217745532916E-14, 9.046025403784437202, -12.00000000000000000 ) ) ;
#8159=LINE ( 'NONE', #13524, #10243 ) ;
#8164=CARTESIAN_POINT ( 'NONE',  ( -17.99988701463194474, 8.062211464643718628, -0.1761320247424245089 ) ) ;
#8169=CARTESIAN_POINT ( 'NONE',  ( 4.171729424061789260, 11.83000000000000718, 12.83926296998457239 ) ) ;
#8174=CARTESIAN_POINT ( 'NONE',  ( 2.621994543952811015E-15, 8.179999999999994387, -14.19474002721660355 ) ) ;
#8182=CIRCLE ( 'NONE', #13782, 26.00000000000000355 ) ;
#8184=CARTESIAN_POINT ( 'NONE',  ( 0.6926531483078161022, 8.027905821154647015, -18.11545820097779469 ) ) ;
#8186=CARTESIAN_POINT ( 'NONE',  ( -11.20634389893962712, 10.00000000000000178, -4.929649438907175885 ) ) ;
#8188=DIRECTION ( 'NONE',  ( 0.000000000000000000, 0.000000000000000000, 1.000000000000000000 ) ) ;
#8195=CARTESIAN_POINT ( 'NONE',  ( -9.520470885617717371, -13.76999999999999780, 6.917026985038133624 ) ) ;
#8209=VERTEX_POINT ( 'NONE', #11044 ) ;
#8212=ORIENTED_EDGE ( 'NONE', *, *, #422, .T. ) ;
#8214=CARTESIAN_POINT ( 'NONE',  ( 0.6607497744049288801, -1.070778138966299504E-15, -12.02517454154194709 ) ) ;
#8215=PRODUCT_DEFINITION_FORMATION_WITH_SPECIFIED_SOURCE ( 'ANY', '', #12276, .NOT_KNOWN. ) ;
#8218=CARTESIAN_POINT ( 'NONE',  ( -3.636496289402156190, -13.46999999999999531, 11.19198476289190758 ) ) ;
#8219=DIRECTION ( 'NONE',  ( 0.000000000000000000, 1.000000000000000000, 0.000000000000000000 ) ) ;
#8220=CARTESIAN_POINT ( 'NONE',  ( -13.49999999999999822, -11.92000000000000348, 4.386415899144235908 ) ) ;
#8233=DIRECTION ( 'NONE',  ( 0.000000000000000000, 0.000000000000000000, 1.000000000000000000 ) ) ;
#8235=CARTESIAN_POINT ( 'NONE',  ( -8.343458848123578520, 7.480000000000002203, -11.48378591275254124 ) ) ;
#8236=CARTESIAN_POINT ( 'NONE',  ( 2.279995255611139653E-15, 6.179999999999999716, -12.37355403259654985 ) ) ;
#8239=CARTESIAN_POINT ( 'NONE',  ( -4.171729424061791036, -6.469999999999996199, 12.83926296998457239 ) ) ;
#8243=DIRECTION ( 'NONE',  ( -0.000000000000000000, -1.000000000000000000, -0.000000000000000000 ) ) ;
#8246=CARTESIAN_POINT ( 'NONE',  ( -10.92957602604999146, 9.999999999999998224, 4.954227274842499362 ) ) ;
#8251=CIRCLE ( 'NONE', #13313, 26.00000000000000355 ) ;
#8254=CARTESIAN_POINT ( 'NONE',  ( -18.71385749420392841, 7.854010659623983592, 1.541332980592373225 ) ) ;
#8257=CARTESIAN_POINT ( 'NONE',  ( -7.416407864998736166, 3.346025403784435248, -10.20780970022448031 ) ) ;
#8258=LINE ( 'NONE', #9672, #11854 ) ;
#8259=CARTESIAN_POINT ( 'NONE',  ( -13.50000000000000000, 10.92999999999999616, -3.469446951953614189E-15 ) ) ;
#8264=CARTESIAN_POINT ( 'NONE',  ( 4.171729424061789260, 9.830000000000005400, 12.83926296998457239 ) ) ;
#8278=CARTESIAN_POINT ( 'NONE',  ( -10.11735578038046235, 9.999999999999994671, 6.713151495386600942 ) ) ;
#8279=CARTESIAN_POINT ( 'NONE',  ( -8.247312284513380831, 7.985359057032879626, -16.32246862014511990 ) ) ;
#8280=CARTESIAN_POINT ( 'NONE',  ( -11.76794919243112325, 25.08000000000001251, 3.823638476888994386 ) ) ;
#8281=EDGE_CURVE ( 'NONE', #2565, #15915, #2776, .T. ) ;
#8284=VERTEX_POINT ( 'NONE', #6616 ) ;
#8285=AXIS2_PLACEMENT_3D ( 'NONE', #4681, #11401, #11226 ) ;
#8289=CARTESIAN_POINT ( 'NONE',  ( -8.845307762532344853, 8.062143948122718839, 15.67790026899615619 ) ) ;
#8300=DIRECTION ( 'NONE',  ( -0.000000000000000000, 1.000000000000000000, -0.000000000000000000 ) ) ;
#8304=CARTESIAN_POINT ( 'NONE',  ( -11.82076925184314931, -1.497824325258514019E-15, -5.475814512136048862 ) ) ;
#8308=CARTESIAN_POINT ( 'NONE',  ( 18.99999999999999289, 7.773118517290098062, 1.732050807568941586 ) ) ;
#8309=CARTESIAN_POINT ( 'NONE',  ( 13.50000000000000355, -13.42000000000000703, -4.386415899144233244 ) ) ;
#8316=LINE ( 'NONE', #7240, #5635 ) ;
#8321=ADVANCED_FACE ( 'NONE', ( #8119 ), #13485, .T. ) ;
#8323=CARTESIAN_POINT ( 'NONE',  ( -12.00000000000000178, 0.7960254037844517461, -2.718289652585035561E-15 ) ) ;
#8324=CARTESIAN_POINT ( 'NONE',  ( 2.138189846611488143, 3.756881418804832506, 13.50000003176731589 ) ) ;
#8325=CARTESIAN_POINT ( 'NONE',  ( -9.520470885617715595, -8.369999999999995666, -6.917026985038136289 ) ) ;
#8327=CARTESIAN_POINT ( 'NONE',  ( -8.891200544363830713E-16, 2.680000000000005045, 13.49999999999999822 ) ) ;
#8336=DIRECTION ( 'NONE',  ( 0.000000000000000000, 0.000000000000000000, -1.000000000000000000 ) ) ;
#8342=ORIENTED_EDGE ( 'NONE', *, *, #5396, .F. ) ;
#8346=CARTESIAN_POINT ( 'NONE',  ( -8.549982208541774191E-16, 8.679999999999994387, 14.19474002721660355 ) ) ;
#8351=CARTESIAN_POINT ( 'NONE',  ( 10.92172942406178926, 7.129999999999997229, 7.935100905948385908 ) ) ;
#8352=LINE ( 'NONE', #378, #4008 ) ;
#8358=ADVANCED_FACE ( 'NONE', ( #13569 ), #10844, .T. ) ;
#8362=CARTESIAN_POINT ( 'NONE',  ( -7.689041659587561917, 9.999999999999992895, -10.05412496806502887 ) ) ;
#8366=LINE ( 'NONE', #4195, #12779 ) ;
#8368=CARTESIAN_POINT ( 'NONE',  ( -7.272992578804307939, 24.48000000000000398, -10.01041549318726886 ) ) ;
#8371=AXIS2_PLACEMENT_3D ( 'NONE', #13762, #4238, #8233 ) ;
#8373=CARTESIAN_POINT ( 'NONE',  ( 9.520470885617717371, -15.26999999999999957, -6.917026985038131848 ) ) ;
#8376=CARTESIAN_POINT ( 'NONE',  ( -8.177092975168962496, 7.956016782093530360, 16.47957145870427453 ) ) ;
#8379=VECTOR ( 'NONE', #969, 1000.000000000000000 ) ;
#8385=ORIENTED_EDGE ( 'NONE', *, *, #15485, .F. ) ;
#8389=ORIENTED_EDGE ( 'NONE', *, *, #3103, .T. ) ;
#8395=CARTESIAN_POINT ( 'NONE',  ( -8.343458848123576743, -18.52000000000000668, -11.48378591275254301 ) ) ;
#8399=CARTESIAN_POINT ( 'NONE',  ( 3.636496289402157078, -17.96999999999999886, -11.19198476289190936 ) ) ;
#8402=CARTESIAN_POINT ( 'NONE',  ( -16.64312382832864046, 7.924527542031521321, -8.110285629053153755 ) ) ;
#8409=CARTESIAN_POINT ( 'NONE',  ( 22.26874168100111362, 6.548282979925672542, 8.000000000000099476 ) ) ;
#8410=DIRECTION ( 'NONE',  ( -0.4999999999999881761, 0.000000000000000000, -0.8660254037844454800 ) ) ;
#8411=FACE_OUTER_BOUND ( 'NONE', #11186, .T. ) ;
#8412=CARTESIAN_POINT ( 'NONE',  ( 8.343458848123578520, 30.98000000000000043, 11.48378591275254124 ) ) ;
#8413=CARTESIAN_POINT ( 'NONE',  ( 7.272992578804311492, -3.120000000000004992, -10.01041549318726709 ) ) ;
#8415=CARTESIAN_POINT ( 'NONE',  ( -2.138189944381236884, 1.256881422320270003, -13.50000000000000000 ) ) ;
#8420=EDGE_CURVE ( 'NONE', #15651, #42, #10984, .T. ) ;
#8429=CARTESIAN_POINT ( 'NONE',  ( -7.272992578804310604, 25.38000000000000256, 10.01041549318726709 ) ) ;
#8430=ORIENTED_EDGE ( 'NONE', *, *, #1972, .F. ) ;
#8434=CARTESIAN_POINT ( 'NONE',  ( 10.92172942406178926, 6.129999999999996341, 7.935100905948385908 ) ) ;
#8439=CARTESIAN_POINT ( 'NONE',  ( -13.49999999999999822, 3.080000000000009841, 4.386415899144235908 ) ) ;
#8440=CARTESIAN_POINT ( 'NONE',  ( 17.42428528562858148, 0.000000000000000000, -19.29752010712846300 ) ) ;
#8446=ADVANCED_FACE ( 'NONE', ( #12945 ), #5091, .F. ) ;
#8450=CARTESIAN_POINT ( 'NONE',  ( 0.3535656791965426926, 8.055112074840369729, 18.02368563757056563 ) ) ;
#8455=CARTESIAN_POINT ( 'NONE',  ( -15.28534784291377235, 6.548267719634618622, -18.06260399879766965 ) ) ;
#8457=CARTESIAN_POINT ( 'NONE',  ( -11.76794919243112325, 22.08000000000000540, 3.823638476888994386 ) ) ;
#8460=VERTEX_POINT ( 'NONE', #11627 ) ;
#8462=CARTESIAN_POINT ( 'NONE',  ( -11.76794919243112325, -17.06999999999999318, -2.602085213965210642E-15 ) ) ;
#8465=CARTESIAN_POINT ( 'NONE',  ( -7.999999999999776179, 7.773118517290098062, -17.32050807568887762 ) ) ;
#8473=VECTOR ( 'NONE', #1054, 1000.000000000000000 ) ;
#8475=ORIENTED_EDGE ( 'NONE', *, *, #3286, .T. ) ;
#8480=DIRECTION ( 'NONE',  ( 0.000000000000000000, 0.000000000000000000, -1.000000000000000000 ) ) ;
#8484=CARTESIAN_POINT ( 'NONE',  ( 10.92172942406179104, -13.26999999999999780, -7.935100905948385908 ) ) ;
#8490=CARTESIAN_POINT ( 'NONE',  ( -11.76794919243112325, -4.919999999999999041, 3.823638476888994386 ) ) ;
#8497=CARTESIAN_POINT ( 'NONE',  ( -0.3535656791965650081, 8.055112074840376835, -18.02368563757054432 ) ) ;
#8498=LINE ( 'NONE', #14998, #11744 ) ;
#8499=FACE_OUTER_BOUND ( 'NONE', #11335, .T. ) ;
#8500=CARTESIAN_POINT ( 'NONE',  ( -8.343458848123582072, 30.38000000000000611, 11.48378591275254124 ) ) ;
#8501=CARTESIAN_POINT ( 'NONE',  ( 9.520470885617715595, -6.869999999999993889, 6.917026985038135400 ) ) ;
#8504=CARTESIAN_POINT ( 'NONE',  ( 7.416407864998740607, 6.013974596215558854, -10.20780970022447676 ) ) ;
#8514=CARTESIAN_POINT ( 'NONE',  ( -12.00000000000002842, 1.063974596215591317, -2.718289652585047788E-15 ) ) ;
#8518=CARTESIAN_POINT ( 'NONE',  ( -19.00000000000001776, 7.773118517290098950, 1.732050807568674466 ) ) ;
#8519=CARTESIAN_POINT ( 'NONE',  ( 9.520470885617717371, 26.73000000000000398, -6.917026985038131848 ) ) ;
#8520=VERTEX_POINT ( 'NONE', #15930 ) ;
#8522=PLANE ( 'NONE',  #2311 ) ;
#8524=CARTESIAN_POINT ( 'NONE',  ( 2.621994543952811015E-15, 10.18000000000000327, -14.19474002721660355 ) ) ;
#8526=ADVANCED_FACE ( 'NONE', ( #15752 ), #6327, .F. ) ;
#8530=CARTESIAN_POINT ( 'NONE',  ( -13.49999999999999822, -0.2200000000000017775, -4.386415899144240349 ) ) ;
#8539=( LENGTH_UNIT ( ) NAMED_UNIT ( * ) SI_UNIT ( .MILLI., .METRE. ) );
#8544=CARTESIAN_POINT ( 'NONE',  ( -7.999999999999670486, 5.918584287042171432, -24.73863375370606477 ) ) ;
#8545=CARTESIAN_POINT ( 'NONE',  ( -8.992807909601426175, 8.063463562524669115, -15.58762070717333970 ) ) ;
#8549=EDGE_CURVE ( 'NONE', #2603, #9217, #352, .T. ) ;
#8552=VECTOR ( 'NONE', #17041, 1000.000000000000000 ) ;
#8557=AXIS2_PLACEMENT_3D ( 'NONE', #30, #2929, #14857 ) ;
#8561=VERTEX_POINT ( 'NONE', #830 ) ;
#8566=CARTESIAN_POINT ( 'NONE',  ( -16.47733079524789090, 7.956441929884681130, 8.178053476329983695 ) ) ;
#8569=CARTESIAN_POINT ( 'NONE',  ( 7.272992578804308828, 31.98000000000000043, 10.01041549318726709 ) ) ;
#8572=VECTOR ( 'NONE', #4784, 1000.000000000000000 ) ;
#8576=EDGE_CURVE ( 'NONE', #13571, #9800, #2594, .T. ) ;
#8577=CARTESIAN_POINT ( 'NONE',  ( 9.520470885617715595, -0.8699999999999957767, 6.917026985038135400 ) ) ;
#8579=CARTESIAN_POINT ( 'NONE',  ( 3.708203932499376076, 1.963974596215575019, 11.41267819554186680 ) ) ;
#8583=LINE ( 'NONE', #13934, #12046 ) ;
#8584=CARTESIAN_POINT ( 'NONE',  ( 1.900613283894418970, 8.969143981464171134, -12.00000000000000711 ) ) ;
#8588=CARTESIAN_POINT ( 'NONE',  ( -11.76794919243112325, -11.06999999999999673, -2.602085213965210642E-15 ) ) ;
#8590=CARTESIAN_POINT ( 'NONE',  ( 6.750022565184456980, -18.07073825016061619, 11.69132992304556673 ) ) ;
#8593=CARTESIAN_POINT ( 'NONE',  ( -8.891200544363830713E-16, 2.680000000000005045, 13.49999999999999822 ) ) ;
#8596=EDGE_CURVE ( 'NONE', #6661, #5891, #2486, .T. ) ;
#8597=CARTESIAN_POINT ( 'NONE',  ( 7.347880794884122694E-16, 0.000000000000000000, -20.00000000000000000 ) ) ;
#8604=CARTESIAN_POINT ( 'NONE',  ( -9.520470885617715595, 18.63000000000000611, -6.917026985038136289 ) ) ;
#8605=VERTEX_POINT ( 'NONE', #10396 ) ;
#8609=CARTESIAN_POINT ( 'NONE',  ( 13.50000000000000355, 3.580000000000008953, -4.386415899144233244 ) ) ;
#8610=ORIENTED_EDGE ( 'NONE', *, *, #17286, .F. ) ;
#8613=CARTESIAN_POINT ( 'NONE',  ( 13.50000000000000000, 1.430000000000014593, 1.734723475976807094E-15 ) ) ;
#8622=EDGE_CURVE ( 'NONE', #3432, #5466, #11130, .T. ) ;
#8627=VECTOR ( 'NONE', #6340, 1000.000000000000000 ) ;
#8634=ORIENTED_EDGE ( 'NONE', *, *, #9164, .F. ) ;
#8635=CARTESIAN_POINT ( 'NONE',  ( 10.92172942406178926, 33.13000000000002387, 7.935100905948385908 ) ) ;
#8638=CARTESIAN_POINT ( 'NONE',  ( 8.378362625313673817, -1.749711886770878784E-15, 10.58551083881864407 ) ) ;
#8648=CARTESIAN_POINT ( 'NONE',  ( 10.92172942406179104, 9.730000000000016414, -7.935100905948385908 ) ) ;
#8656=CARTESIAN_POINT ( 'NONE',  ( 9.520470885617717371, 29.73000000000000753, -6.917026985038131848 ) ) ;
#8657=STYLED_ITEM('',(#17526),#3260);
#8661=CARTESIAN_POINT ( 'NONE',  ( -9.520470885617717371, -13.76999999999999780, 6.917026985038133624 ) ) ;
#8664=CARTESIAN_POINT ( 'NONE',  ( -7.272992578804307939, -5.520000000000001350, -10.01041549318726886 ) ) ;
#8674=DIRECTION ( 'NONE',  ( 0.000000000000000000, 1.000000000000000000, 0.000000000000000000 ) ) ;
#8675=CARTESIAN_POINT ( 'NONE',  ( -7.272992578804310604, -4.620000000000000995, 10.01041549318726709 ) ) ;
#8686=PLANE ( 'NONE',  #4997 ) ;
#8690=CARTESIAN_POINT ( 'NONE',  ( 3.636496289402154414, 19.83000000000001251, 11.19198476289190758 ) ) ;
#8691=ORIENTED_EDGE ( 'NONE', *, *, #15210, .T. ) ;
#8695=CARTESIAN_POINT ( 'NONE',  ( -10.92172942406179104, 5.230000000000012861, 7.935100905948385908 ) ) ;
#8696=CARTESIAN_POINT ( 'NONE',  ( -7.272992578804307939, 33.47999999999999687, -10.01041549318726886 ) ) ;
#8697=DIRECTION ( 'NONE',  ( -0.000000000000000000, 1.000000000000000000, -0.000000000000000000 ) ) ;
#8698=CARTESIAN_POINT ( 'NONE',  ( -10.92172942406179104, 6.230000000000012861, 7.935100905948385908 ) ) ;
#8701=CARTESIAN_POINT ( 'NONE',  ( 17.42428528562858148, 0.000000000000000000, -19.29752010712846300 ) ) ;
#8715=ORIENTED_EDGE ( 'NONE', *, *, #1763, .F. ) ;
#8718=CARTESIAN_POINT ( 'NONE',  ( -10.92172942406179104, 32.23000000000001108, 7.935100905948385908 ) ) ;
#8725=CARTESIAN_POINT ( 'NONE',  ( 12.11540212872241007, -1.688490311990081981E-15, 5.028035910480880943 ) ) ;
#8728=CARTESIAN_POINT ( 'NONE',  ( 17.32050807568873196, 0.000000000000000000, 10.00000000000008171 ) ) ;
#8731=CARTESIAN_POINT ( 'NONE',  ( 9.520470885617717371, 14.72999999999999332, -6.917026985038131848 ) ) ;
#8732=ORIENTED_EDGE ( 'NONE', *, *, #4932, .T. ) ;
#8733=LINE ( 'NONE', #837, #5573 ) ;
#8735=CARTESIAN_POINT ( 'NONE',  ( 13.50000000000000000, 9.429999999999994387, 1.734723475976807094E-15 ) ) ;
#8741=CARTESIAN_POINT ( 'NONE',  ( 17.14741290055379253, 7.815224843475954586, 8.000000000000085265 ) ) ;
#8743=CARTESIAN_POINT ( 'NONE',  ( -20.00000000000000000, 0.000000000000000000, -2.102236684100764122E-13 ) ) ;
#8745=CARTESIAN_POINT ( 'NONE',  ( -9.520470885617717371, 31.23000000000000753, 6.917026985038133624 ) ) ;
#8749=CARTESIAN_POINT ( 'NONE',  ( 2.279995255611139653E-15, -14.82000000000000384, -12.37355403259654985 ) ) ;
#8753=CARTESIAN_POINT ( 'NONE',  ( -7.272992578804307939, -2.520000000000001794, -10.01041549318726886 ) ) ;
#8759=LINE ( 'NONE', #4764, #12889 ) ;
#8760=CARTESIAN_POINT ( 'NONE',  ( 18.99999999999999289, 0.000000000000000000, 1.732050807568941586 ) ) ;
#8761=CARTESIAN_POINT ( 'NONE',  ( 8.402223690147334167, 8.016752490022669875, -16.11047477678861739 ) ) ;
#8762=CARTESIAN_POINT ( 'NONE',  ( 8.343458848123583849, 25.88000000000000611, -11.48378591275253768 ) ) ;
#8764=EDGE_CURVE ( 'NONE', #1172, #2325, #14266, .T. ) ;
#8766=CARTESIAN_POINT ( 'NONE',  ( -24.73863375370588003, 5.918584287042170544, -8.000000000000282441 ) ) ;
#8767=VECTOR ( 'NONE', #10366, 1000.000000000000000 ) ;
#8769=( LENGTH_UNIT ( ) NAMED_UNIT ( * ) SI_UNIT ( .MILLI., .METRE. ) );
#8780=CARTESIAN_POINT ( 'NONE',  ( -11.76794919243112325, 24.93000000000000682, -2.602085213965210642E-15 ) ) ;
#8788=CARTESIAN_POINT ( 'NONE',  ( -1.732050807568877859, 7.773118517290099838, -18.99999999999999645 ) ) ;
#8790=DIRECTION ( 'NONE',  ( 0.8660254037844332675, -0.000000000000000000, 0.5000000000000092149 ) ) ;
#8795=CARTESIAN_POINT ( 'NONE',  ( -12.00000000000000178, 7.213974596215562585, 3.899036354794875425 ) ) ;
#8803=ORIENTED_EDGE ( 'NONE', *, *, #12815, .T. ) ;
#8806=ORIENTED_EDGE ( 'NONE', *, *, #11694, .F. ) ;
#8807=CARTESIAN_POINT ( 'NONE',  ( -4.171729424061791036, 29.53000000000000114, 12.83926296998457239 ) ) ;
#8813=CARTESIAN_POINT ( 'NONE',  ( 10.72039879472368185, -3.110307960253515263E-15, -6.101375431309464581 ) ) ;
#8821=DIRECTION ( 'NONE',  ( 0.000000000000000000, -1.000000000000000000, 0.000000000000000000 ) ) ;
#8822=ORIENTED_EDGE ( 'NONE', *, *, #5305, .F. ) ;
#8823=AXIS2_PLACEMENT_3D ( 'NONE', #2635, #13346, #1236 ) ;
#8828=CARTESIAN_POINT ( 'NONE',  ( 15.31996850146886580, 8.007813437504038845, 9.831838144771181121 ) ) ;
#8833=CARTESIAN_POINT ( 'NONE',  ( -11.76794919243112325, 30.78000000000001180, -3.823638476888998827 ) ) ;
#8836=( BOUNDED_CURVE ( )  B_SPLINE_CURVE ( 2, ( #6051, #16805, #4712, #2036, #730, #6138, #11517, #11604, #10458, #14317, #7717, #17065, #5063 ),
 .UNSPECIFIED., .F., .F. ) 
 B_SPLINE_CURVE_WITH_KNOTS ( ( 3, 2, 2, 2, 2, 2, 3 ),
 ( 0.4669843698996809511, 0.4698145782021032613, 0.4754749948069478260, 0.4811354114117924463, 0.4867958280166371221, 0.4924562446214816869, 0.4952864492504068794 ),
 .UNSPECIFIED. ) 
 CURVE ( )  GEOMETRIC_REPRESENTATION_ITEM ( )  RATIONAL_B_SPLINE_CURVE ( ( 0.9755282581475768211, 0.9755282581475770431, 1.000000000000000000, 0.9510565162951535312, 1.000000000000000000, 0.9510565162951535312, 1.000000000000000000, 0.9510565162951535312, 1.000000000000000000, 0.9510565162951535312, 1.000000000000000000, 0.9755282899109183337, 0.9755282581476180104 ) ) 
 REPRESENTATION_ITEM ( '' )  );
#8838=AXIS2_PLACEMENT_3D ( 'NONE', #1349, #10485, #16018 ) ;
#8839=CARTESIAN_POINT ( 'NONE',  ( 18.02388005911709001, 8.055054232036098938, -0.3546005442045098710 ) ) ;
#8846=DIRECTION ( 'NONE',  ( 0.000000000000000000, 0.000000000000000000, 1.000000000000000000 ) ) ;
#8847=CARTESIAN_POINT ( 'NONE',  ( -13.49999999999999822, 2.779999999999990923, -4.386415899144240349 ) ) ;
#8848=CARTESIAN_POINT ( 'NONE',  ( -8.343458848123582072, 24.38000000000000611, 11.48378591275254124 ) ) ;
#8851=VECTOR ( 'NONE', #13639, 1000.000000000000000 ) ;
#8859=VECTOR ( 'NONE', #12110, 1000.000000000000000 ) ;
#8860=ADVANCED_FACE ( 'NONE', ( #14952 ), #12142, .F. ) ;
#8863=DIRECTION ( 'NONE',  ( -0.5000000000000093259, 0.000000000000000000, 0.8660254037844333785 ) ) ;
#8868=CARTESIAN_POINT ( 'NONE',  ( 3.636496289402157078, 12.03000000000001357, -11.19198476289190936 ) ) ;
#8869=VERTEX_POINT ( 'NONE', #14690 ) ;
#8873=CARTESIAN_POINT ( 'NONE',  ( 3.636496289402157078, 30.03000000000000114, -11.19198476289190936 ) ) ;
#8881=CARTESIAN_POINT ( 'NONE',  ( 15.58845726811991916, 0.000000000000000000, -10.99999999999996092 ) ) ;
#8887=CARTESIAN_POINT ( 'NONE',  ( 8.375056734751542109, 9.999950376471138824, 10.58801762894534271 ) ) ;
#8889=ORIENTED_EDGE ( 'NONE', *, *, #8131, .T. ) ;
#8891=ORIENTED_EDGE ( 'NONE', *, *, #5478, .T. ) ;
#8892=ORIENTED_EDGE ( 'NONE', *, *, #8420, .T. ) ;
#8893=CARTESIAN_POINT ( 'NONE',  ( -10.92172942406178926, 28.63000000000001677, -7.935100905948389460 ) ) ;
#8898=EDGE_CURVE ( 'NONE', #3099, #11984, #6594, .T. ) ;
#8900=DIRECTION ( 'NONE',  ( 0.000000000000000000, 1.000000000000000000, 0.000000000000000000 ) ) ;
#8903=CARTESIAN_POINT ( 'NONE',  ( 8.000000000000019540, 0.000000000000000000, -24.73863375370596174 ) ) ;
#8907=ORIENTED_EDGE ( 'NONE', *, *, #3175, .T. ) ;
#8908=CARTESIAN_POINT ( 'NONE',  ( 0.000000000000000000, 9.000000000000000000, 0.000000000000000000 ) ) ;
#8910=CARTESIAN_POINT ( 'NONE',  ( 0.000000000000000000, 9.999999999999998224, 0.000000000000000000 ) ) ;
#8914=CARTESIAN_POINT ( 'NONE',  ( 15.50189495701170372, 7.815232006635826956, 10.85006967914017473 ) ) ;
#8922=CARTESIAN_POINT ( 'NONE',  ( 0.000000000000000000, 9.000000000000000000, 0.000000000000000000 ) ) ;
#8926=CARTESIAN_POINT ( 'NONE',  ( 17.32050807568873552, 0.000000000000000000, 8.000000000000085265 ) ) ;
#8927=CARTESIAN_POINT ( 'NONE',  ( 8.992436155572725909, 8.063482198985079563, -15.58776297682138079 ) ) ;
#8928=CARTESIAN_POINT ( 'NONE',  ( -10.92172942406178926, 26.63000000000001322, -7.935100905948389460 ) ) ;
#8929=EDGE_LOOP ( 'NONE', ( #16993, #133, #2280, #6885 ) ) ;
#8930=DIRECTION ( 'NONE',  ( -0.000000000000000000, -1.000000000000000000, -0.000000000000000000 ) ) ;
#8947=ORIENTED_EDGE ( 'NONE', *, *, #10230, .T. ) ;
#8948=CARTESIAN_POINT ( 'NONE',  ( -7.272992578804307939, 15.47999999999999865, -10.01041549318726886 ) ) ;
#8949=ORIENTED_EDGE ( 'NONE', *, *, #3945, .F. ) ;
#8953=CARTESIAN_POINT ( 'NONE',  ( 10.92172942406178926, -2.869999999999997442, 7.935100905948385908 ) ) ;
#8965=LINE ( 'NONE', #11608, #1572 ) ;
#8970=DIRECTION ( 'NONE',  ( 0.000000000000000000, 0.000000000000000000, 1.000000000000000000 ) ) ;
#8974=CARTESIAN_POINT ( 'NONE',  ( 9.520470885617715595, 5.129999999999995453, 6.917026985038135400 ) ) ;
#8977=CARTESIAN_POINT ( 'NONE',  ( 10.92172942406179104, 27.73000000000000398, -7.935100905948385908 ) ) ;
#8980=EDGE_CURVE ( 'NONE', #546, #1713, #1162, .T. ) ;
#8984=CARTESIAN_POINT ( 'NONE',  ( 2.138192755968095327, 0.7568815234145580551, 13.49999908646005231 ) ) ;
#8986=DIRECTION ( 'NONE',  ( -0.000000000000000000, -1.000000000000000000, -0.000000000000000000 ) ) ;
#8993=CARTESIAN_POINT ( 'NONE',  ( -10.92172942406179104, 17.22999999999999687, 7.935100905948385908 ) ) ;
#8997=FACE_OUTER_BOUND ( 'NONE', #5511, .T. ) ;
#9002=B_SPLINE_CURVE_WITH_KNOTS ( 'NONE', 3,
 ( #689, #11064, #10081, #14024 ),
 .UNSPECIFIED., .F., .F.,
 ( 4, 4 ),
 ( 2.376698214958262694E-07, 0.007646667280170315988 ),
 .UNSPECIFIED. ) ;
#9010=LINE ( 'NONE', #8926, #7347 ) ;
#9012=EDGE_LOOP ( 'NONE', ( #12130, #5818, #10531, #16006, #10387, #16708, #2410, #12595, #6497, #6602, #8892, #3619, #4440, #14328, #5718, #3601, #12763, #3136, #14781, #6555, #10129, #9414, #9083, #9787, #13194, #13363, #9410, #5865, #3367, #14090, #8891, #12740, #15497, #13912, #2052, #14075, #2762, #653, #5691, #15959, #13617, #3952, #12953, #11448, #3670, #2736, #9175, #5422, #3847, #11766, #7206 ) ) ;
#9013=CYLINDRICAL_SURFACE ( 'NONE', #10691, 26.00000000000000355 ) ;
#9016=CIRCLE ( 'NONE', #2771, 26.00000000000000355 ) ;
#9017=CARTESIAN_POINT ( 'NONE',  ( 0.000000000000000000, 9.000000000000000000, 0.000000000000000000 ) ) ;
#9020=CARTESIAN_POINT ( 'NONE',  ( -4.171729424061791036, 3.530000000000005578, 12.83926296998457239 ) ) ;
#9037=CARTESIAN_POINT ( 'NONE',  ( 3.636496289402154414, 10.83000000000000540, 11.19198476289190758 ) ) ;
#9041=CARTESIAN_POINT ( 'NONE',  ( 8.000000000000023093, 7.773118517290098062, -17.32050807568876394 ) ) ;
#9042=CARTESIAN_POINT ( 'NONE',  ( -13.49999999999999822, 1.780000000000000693, -4.386415899144240349 ) ) ;
#9048=CARTESIAN_POINT ( 'NONE',  ( 17.32050807568873552, 0.000000000000000000, 8.000000000000085265 ) ) ;
#9055=EDGE_CURVE ( 'NONE', #4638, #2220, #13244, .T. ) ;
#9058=CARTESIAN_POINT ( 'NONE',  ( 2.222800136090958073E-15, 0.04602540378443767399, -12.00000000000000000 ) ) ;
#9060=ORIENTED_EDGE ( 'NONE', *, *, #6355, .F. ) ;
#9063=CARTESIAN_POINT ( 'NONE',  ( -3.636496289402156190, 4.530000000000006466, 11.19198476289190758 ) ) ;
#9066=EDGE_LOOP ( 'NONE', ( #3864, #16044, #13985, #7513 ) ) ;
#9067=CARTESIAN_POINT ( 'NONE',  ( 10.92172942406178926, 27.13000000000001677, 7.935100905948385908 ) ) ;
#9074=CARTESIAN_POINT ( 'NONE',  ( 12.54984920316064922, 1.934905186679871999E-15, -1.651895503087821737 ) ) ;
#9075=CARTESIAN_POINT ( 'NONE',  ( 10.92172942406178926, 1.129999999999992122, 7.935100905948385908 ) ) ;
#9083=ORIENTED_EDGE ( 'NONE', *, *, #10587, .T. ) ;
#9085=CARTESIAN_POINT ( 'NONE',  ( 0.000000000000000000, 0.000000000000000000, 0.000000000000000000 ) ) ;
#9086=VERTEX_POINT ( 'NONE', #14752 ) ;
#9087=CARTESIAN_POINT ( 'NONE',  ( 4.171729424061789260, 17.83000000000001251, 12.83926296998457239 ) ) ;
#9091=FACE_OUTER_BOUND ( 'NONE', #9012, .T. ) ;
#9092=CARTESIAN_POINT ( 'NONE',  ( 2.785879211291982797E-06, 6.680077384874748780, 13.49999999999942979 ) ) ;
#9100=VECTOR ( 'NONE', #5872, 1000.000000000000000 ) ;
#9112=CARTESIAN_POINT ( 'NONE',  ( -13.49999999999999822, -2.920000000000003926, 4.386415899144235908 ) ) ;
#9125=AXIS2_PLACEMENT_3D ( 'NONE', #9649, #14999, #16148 ) ;
#9129=CARTESIAN_POINT ( 'NONE',  ( 7.272992578804311492, 8.880000000000000782, -10.01041549318726709 ) ) ;
#9130=VERTEX_POINT ( 'NONE', #2466 ) ;
#9133=DIRECTION ( 'NONE',  ( 0.000000000000000000, 1.000000000000000000, 0.000000000000000000 ) ) ;
#9134=CARTESIAN_POINT ( 'NONE',  ( 13.50000000000000000, -2.569999999999995843, 1.734723475976807094E-15 ) ) ;
#9140=CARTESIAN_POINT ( 'NONE',  ( -9.708203932499419153, 9.763974596215597046, -7.053423027509717613 ) ) ;
#9149=CARTESIAN_POINT ( 'NONE',  ( 16.82677684650033356, 7.170662809914418290, -13.14483242576210742 ) ) ;
#9155=CARTESIAN_POINT ( 'NONE',  ( 11.76794919243112325, 8.429999999999992610, 1.734723475976807094E-15 ) ) ;
#9158=CARTESIAN_POINT ( 'NONE',  ( -8.343458848123582072, 23.38000000000000966, 11.48378591275254124 ) ) ;
#9164=EDGE_CURVE ( 'NONE', #9213, #2258, #10324, .T. ) ;
#9165=CARTESIAN_POINT ( 'NONE',  ( -20.00000000000000000, 0.000000000000000000, -2.102236684100764122E-13 ) ) ;
#9172=ORIENTED_EDGE ( 'NONE', *, *, #16392, .F. ) ;
#9175=ORIENTED_EDGE ( 'NONE', *, *, #11201, .T. ) ;
#9176=CARTESIAN_POINT ( 'NONE',  ( 10.92172942406178926, 18.13000000000000611, 7.935100905948385908 ) ) ;
#9184=CIRCLE ( 'NONE', #14503, 14.50000000000000000 ) ;
#9193=CARTESIAN_POINT ( 'NONE',  ( 8.343458848123578520, 18.98000000000000043, 11.48378591275254124 ) ) ;
#9195=CYLINDRICAL_SURFACE ( 'NONE', #2766, 26.00000000000000355 ) ;
#9200=CARTESIAN_POINT ( 'NONE',  ( 2.621994543952811015E-15, -6.820000000000003837, -14.19474002721660355 ) ) ;
#9213=VERTEX_POINT ( 'NONE', #2641 ) ;
#9214=CARTESIAN_POINT ( 'NONE',  ( 0.000000000000000000, 5.918584287042170544, 0.000000000000000000 ) ) ;
#9215=CARTESIAN_POINT ( 'NONE',  ( 3.636496289402154414, 7.830000000000003624, 11.19198476289190758 ) ) ;
#9217=VERTEX_POINT ( 'NONE', #16942 ) ;
#9221=CARTESIAN_POINT ( 'NONE',  ( 2.621994543952811015E-15, -7.820000000000002061, -14.19474002721660355 ) ) ;
#9226=CARTESIAN_POINT ( 'NONE',  ( 19.29752010712851984, 5.918584287042171432, -17.42428528562851042 ) ) ;
#9230=B_SPLINE_CURVE_WITH_KNOTS ( 'NONE', 3,
 ( #16320, #1480, #13927, #8402, #12270, #13669, #167, #7237, #5571, #511, #10954, #5919, #12360, #254, #13754, #2971, #1653, #16677 ),
 .UNSPECIFIED., .F., .F.,
 ( 4, 2, 2, 2, 2, 2, 2, 2, 4 ),
 ( 2.030049010680398225E-07, 0.0005272941439305965910, 0.001054385282960125297, 0.001581476421989653786, 0.002108567561019182492, 0.002635658700048711198, 0.003162749839078239471, 0.003689840978107768177, 0.004216932117137296883 ),
 .UNSPECIFIED. ) ;
#9231=CARTESIAN_POINT ( 'NONE',  ( -7.416407864998736166, 6.613974596215566493, -10.20780970022448031 ) ) ;
#9241=VECTOR ( 'NONE', #7202, 999.9999999999998863 ) ;
#9242=CARTESIAN_POINT ( 'NONE',  ( -7.409984580736203970E-16, 1.680000000000003491, 12.37355403259654985 ) ) ;
#9243=ORIENTED_EDGE ( 'NONE', *, *, #2187, .F. ) ;
#9245=CARTESIAN_POINT ( 'NONE',  ( 13.49999999999999822, 27.28000000000000469, 4.386415899144237684 ) ) ;
#9248=CARTESIAN_POINT ( 'NONE',  ( 17.42428528562858148, 5.918584287042170544, -19.29752010712846300 ) ) ;
#9253=DIRECTION ( 'NONE',  ( -0.000000000000000000, 1.000000000000000000, -0.000000000000000000 ) ) ;
#9259=VERTEX_POINT ( 'NONE', #10977 ) ;
#9260=ADVANCED_FACE ( 'NONE', ( #11396 ), #275, .F. ) ;
#9261=EDGE_LOOP ( 'NONE', ( #9958, #12047, #6166, #11677 ) ) ;
#9263=EDGE_LOOP ( 'NONE', ( #10642, #14001, #2064, #11071 ) ) ;
#9266=CARTESIAN_POINT ( 'NONE',  ( 9.319033143235019523, 8.055054230040793684, 15.43183772185606806 ) ) ;
#9274=CARTESIAN_POINT ( 'NONE',  ( -7.272992578804310604, 19.38000000000000256, 10.01041549318726709 ) ) ;
#9277=EDGE_CURVE ( 'NONE', #15564, #17188, #605, .T. ) ;
#9279=CARTESIAN_POINT ( 'NONE',  ( -10.92172942406179104, 18.22999999999999687, 7.935100905948385908 ) ) ;
#9282=CARTESIAN_POINT ( 'NONE',  ( -11.76794919243112325, 27.78000000000000114, -3.823638476888998827 ) ) ;
#9286=CARTESIAN_POINT ( 'NONE',  ( -4.171729424061791036, -8.469999999999998863, 12.83926296998457239 ) ) ;
#9291=VECTOR ( 'NONE', #2872, 1000.000000000000000 ) ;
#9300=CARTESIAN_POINT ( 'NONE',  ( -7.409984580736203970E-16, 13.67999999999999616, 12.37355403259654985 ) ) ;
#9302=CARTESIAN_POINT ( 'NONE',  ( 11.76794919243112325, 2.430000000000015703, 1.734723475976807094E-15 ) ) ;
#9305=CARTESIAN_POINT ( 'NONE',  ( 7.999999999999904965, 0.000000000000000000, 17.32050807568881368 ) ) ;
#9306=CARTESIAN_POINT ( 'NONE',  ( 8.343458848123583849, -11.12000000000000632, -11.48378591275253768 ) ) ;
#9309=AXIS2_PLACEMENT_3D ( 'NONE', #3570, #7834, #11714 ) ;
#9316=CARTESIAN_POINT ( 'NONE',  ( 19.29752010712840615, 5.918584287042170544, 17.42428528562864898 ) ) ;
#9318=VECTOR ( 'NONE', #3597, 999.9999999999998863 ) ;
#9324=ORIENTED_EDGE ( 'NONE', *, *, #4456, .T. ) ;
#9327=CARTESIAN_POINT ( 'NONE',  ( -11.76794919243112325, 1.080000000000000959, 3.823638476888994386 ) ) ;
#9328=VERTEX_POINT ( 'NONE', #2905 ) ;
#9329=ORIENTED_EDGE ( 'NONE', *, *, #10408, .F. ) ;
#9330=CARTESIAN_POINT ( 'NONE',  ( -10.92172942406179104, 23.23000000000000043, 7.935100905948385908 ) ) ;
#9331=DIRECTION ( 'NONE',  ( 0.000000000000000000, 0.000000000000000000, -1.000000000000000000 ) ) ;
#9333=CARTESIAN_POINT ( 'NONE',  ( -4.171729424061791036, 15.53000000000001535, 12.83926296998457239 ) ) ;
#9339=EDGE_CURVE ( 'NONE', #9499, #3828, #9002, .T. ) ;
#9342=LINE ( 'NONE', #10739, #6009 ) ;
#9344=CARTESIAN_POINT ( 'NONE',  ( -10.92957602604999146, 9.999999999999998224, 4.954227274842499362 ) ) ;
#9348=ORIENTED_EDGE ( 'NONE', *, *, #7977, .T. ) ;
#9350=ORIENTED_EDGE ( 'NONE', *, *, #10230, .F. ) ;
#9356=EDGE_CURVE ( 'NONE', #2325, #7575, #134, .T. ) ;
#9360=DIRECTION ( 'NONE',  ( 0.000000000000000000, 0.000000000000000000, 1.000000000000000000 ) ) ;
#9361=CARTESIAN_POINT ( 'NONE',  ( 11.76794919243112325, 20.28000000000000824, 3.823638476888996163 ) ) ;
#9362=CARTESIAN_POINT ( 'NONE',  ( 0.000000000000000000, 5.918584287042170544, 0.000000000000000000 ) ) ;
#9365=VERTEX_POINT ( 'NONE', #6102 ) ;
#9366=CARTESIAN_POINT ( 'NONE',  ( -3.659578208143946298, 3.720968205702268948E-15, -11.78367615807299806 ) ) ;
#9369=CARTESIAN_POINT ( 'NONE',  ( 7.272992578804311492, -12.12000000000000455, -10.01041549318726709 ) ) ;
#9371=CARTESIAN_POINT ( 'NONE',  ( -10.92172942406179104, -5.769999999999997797, 7.935100905948385908 ) ) ;
#9385=CARTESIAN_POINT ( 'NONE',  ( -13.49999999999999822, 8.079999999999996518, 4.386415899144235020 ) ) ;
#9386=CARTESIAN_POINT ( 'NONE',  ( 7.272992578804308828, 1.980000000000001315, 10.01041549318726709 ) ) ;
#9390=CARTESIAN_POINT ( 'NONE',  ( -8.343458848123582072, -9.620000000000002771, 11.48378591275254124 ) ) ;
#9399=EDGE_CURVE ( 'NONE', #368, #9696, #7506, .T. ) ;
#9402=VECTOR ( 'NONE', #5988, 999.9999999999998863 ) ;
#9410=ORIENTED_EDGE ( 'NONE', *, *, #640, .F. ) ;
#9413=ORIENTED_EDGE ( 'NONE', *, *, #16937, .T. ) ;
#9414=ORIENTED_EDGE ( 'NONE', *, *, #7659, .F. ) ;
#9415=CARTESIAN_POINT ( 'NONE',  ( -13.49999999999999822, 19.78000000000000824, -4.386415899144240349 ) ) ;
#9418=CARTESIAN_POINT ( 'NONE',  ( -13.49999999999999822, 12.08000000000000185, 4.386415899144235908 ) ) ;
#9432=ORIENTED_EDGE ( 'NONE', *, *, #4773, .F. ) ;
#9433=VERTEX_POINT ( 'NONE', #776 ) ;
#9440=CARTESIAN_POINT ( 'NONE',  ( 8.111079018422898912, 7.924936010579560097, 16.64104048077467013 ) ) ;
#9447=CARTESIAN_POINT ( 'NONE',  ( 9.520470885617717371, 17.72999999999999687, -6.917026985038131848 ) ) ;
#9452=CARTESIAN_POINT ( 'NONE',  ( -10.78033876856473228, 1.259542957514470777E-16, -7.094692149502226819 ) ) ;
#9456=CARTESIAN_POINT ( 'NONE',  ( 9.520470885617717371, -12.26999999999999602, -6.917026985038131848 ) ) ;
#9457=CYLINDRICAL_SURFACE ( 'NONE', #3793, 26.00000000000000355 ) ;
#9458=CARTESIAN_POINT ( 'NONE',  ( 10.92172942406178926, -4.869999999999999218, 7.935100905948385908 ) ) ;
#9470=CARTESIAN_POINT ( 'NONE',  ( -9.520470885617715595, 12.63000000000000256, -6.917026985038136289 ) ) ;
#9472=CARTESIAN_POINT ( 'NONE',  ( -8.891200544363830713E-16, 8.679999999999999716, 13.49999999999999822 ) ) ;
#9473=CARTESIAN_POINT ( 'NONE',  ( -3.636496289402152637, 6.330000000000001847, -11.19198476289190936 ) ) ;
#9474=EDGE_CURVE ( 'NONE', #2562, #17099, #5643, .T. ) ;
#9477=DIRECTION ( 'NONE',  ( -7.483177508809139424E-15, 0.000000000000000000, 1.000000000000000000 ) ) ;
#9478=CARTESIAN_POINT ( 'NONE',  ( -13.49999999999999822, -4.219999999999998863, -4.386415899144240349 ) ) ;
#9483=CARTESIAN_POINT ( 'NONE',  ( 0.000000000000000000, 30.93000000000001393, 0.000000000000000000 ) ) ;
#9487=CARTESIAN_POINT ( 'NONE',  ( -1.900613283894451611, 9.122906826104705047, -11.99999999999999645 ) ) ;
#9494=CARTESIAN_POINT ( 'NONE',  ( -18.36027427702395798, 7.956016705491392393, 1.158215859972792527 ) ) ;
#9498=CARTESIAN_POINT ( 'NONE',  ( 8.343458848123578520, 11.98000000000000753, 11.48378591275254124 ) ) ;
#9499=VERTEX_POINT ( 'NONE', #6352 ) ;
#9500=EDGE_CURVE ( 'NONE', #2957, #7801, #16053, .T. ) ;
#9505=CARTESIAN_POINT ( 'NONE',  ( -4.171729424061787483, 14.33000000000000895, -12.83926296998457417 ) ) ;
#9511=DIRECTION ( 'NONE',  ( 0.000000000000000000, 1.000000000000000000, 0.000000000000000000 ) ) ;
#9513=CARTESIAN_POINT ( 'NONE',  ( 25.42428528562852819, 0.000000000000000000, 5.441113646577569796 ) ) ;
#9514=CARTESIAN_POINT ( 'NONE',  ( -9.653558740436345431, 10.00000000000000355, -7.932758269264289730 ) ) ;
#9516=VECTOR ( 'NONE', #13950, 1000.000000000000000 ) ;
#9517=CARTESIAN_POINT ( 'NONE',  ( 4.171729424061789260, 5.830000000000001847, 12.83926296998457239 ) ) ;
#9520=DIRECTION ( 'NONE',  ( -0.8660254037844393737, 0.000000000000000000, 0.4999999999999986122 ) ) ;
#9521=ORIENTED_EDGE ( 'NONE', *, *, #1628, .F. ) ;
#9528=AXIS2_PLACEMENT_3D ( 'NONE', #11812, #8821, #15496 ) ;
#9536=DIRECTION ( 'NONE',  ( 0.000000000000000000, 0.000000000000000000, -1.000000000000000000 ) ) ;
#9541=CARTESIAN_POINT ( 'NONE',  ( 23.28534784291401749, 6.548267719634618622, -4.206197538246383871 ) ) ;
#9544=CARTESIAN_POINT ( 'NONE',  ( 11.76794919243112325, -9.569999999999994955, 1.734723475976807094E-15 ) ) ;
#9546=CARTESIAN_POINT ( 'NONE',  ( -4.171729424061791036, -17.46999999999999886, 12.83926296998457239 ) ) ;
#9558=CARTESIAN_POINT ( 'NONE',  ( -25.42428528562860990, 5.918584287042170544, 5.441113646577212748 ) ) ;
#9561=CARTESIAN_POINT ( 'NONE',  ( 11.76794919243112325, 5.279999999999999361, 3.823638476888996163 ) ) ;
#9564=CARTESIAN_POINT ( 'NONE',  ( -10.92172942406178926, -4.369999999999999218, -7.935100905948389460 ) ) ;
#9569=AXIS2_PLACEMENT_3D ( 'NONE', #4486, #1813, #8480 ) ;
#9573=ADVANCED_FACE ( 'NONE', ( #11807 ), #3842, .F. ) ;
#9576=CARTESIAN_POINT ( 'NONE',  ( 19.00000000000000711, 0.000000000000000000, -1.732050807568807027 ) ) ;
#9577=CARTESIAN_POINT ( 'NONE',  ( 1.509281292405760415E-13, 1.813974596215571777, 12.00000000000000000 ) ) ;
#9582=AXIS2_PLACEMENT_3D ( 'NONE', #12455, #5748, #14992 ) ;
#9583=VERTEX_POINT ( 'NONE', #10488 ) ;
#9585=DIRECTION ( 'NONE',  ( -0.000000000000000000, -1.000000000000000000, -0.000000000000000000 ) ) ;
#9586=CARTESIAN_POINT ( 'NONE',  ( -4.171729424061791036, 14.53000000000001535, 12.83926296998457239 ) ) ;
#9591=CARTESIAN_POINT ( 'NONE',  ( -13.50000000000000000, 11.92999999999999616, -3.469446951953614189E-15 ) ) ;
#9600=CARTESIAN_POINT ( 'NONE',  ( 0.000000000000000000, 9.000000000000000000, -12.00000000000000178 ) ) ;
#9603=CARTESIAN_POINT ( 'NONE',  ( -11.79534111549779141, 9.999999999999998224, -2.590977554098922386 ) ) ;
#9607=PLANE ( 'NONE',  #127 ) ;
#9613=VECTOR ( 'NONE', #7017, 1000.000000000000000 ) ;
#9615=CARTESIAN_POINT ( 'NONE',  ( -8.022095340454590939, 7.854010772509913529, 16.97734196418684505 ) ) ;
#9630=CARTESIAN_POINT ( 'NONE',  ( -13.39048759961674229, -1.988777493506887074E-15, 0.05228750988018425472 ) ) ;
#9635=CARTESIAN_POINT ( 'NONE',  ( -13.50000000000000000, -18.06999999999999673, -3.469446951953614189E-15 ) ) ;
#9647=CARTESIAN_POINT ( 'NONE',  ( -1.645451467107404531, 7.815250021811911196, -18.85000554241877779 ) ) ;
#9649=CARTESIAN_POINT ( 'NONE',  ( 17.32050807568879236, 0.000000000000000000, -9.999999999999960920 ) ) ;
#9650=CARTESIAN_POINT ( 'NONE',  ( 3.636496289402157078, 6.030000000000007354, -11.19198476289190936 ) ) ;
#9652=CARTESIAN_POINT ( 'NONE',  ( 9.235079662642815990, -17.96812680894470660, 10.25657514373247814 ) ) ;
#9656=EDGE_CURVE ( 'NONE', #2472, #16171, #3322, .T. ) ;
#9670=ORIENTED_EDGE ( 'NONE', *, *, #3504, .F. ) ;
#9671=CARTESIAN_POINT ( 'NONE',  ( -8.891200544363830713E-16, 4.546025403784440755, 12.00000000000000000 ) ) ;
#9672=CARTESIAN_POINT ( 'NONE',  ( -17.32050807568884210, 0.000000000000000000, 7.999999999999840128 ) ) ;
#9673=CARTESIAN_POINT ( 'NONE',  ( 13.50000000000000355, 9.580000000000008953, -4.386415899144233244 ) ) ;
#9674=ORIENTED_EDGE ( 'NONE', *, *, #11426, .T. ) ;
#9678=CARTESIAN_POINT ( 'NONE',  ( 4.171729424061789260, 15.83000000000001073, 12.83926296998457239 ) ) ;
#9686=DIRECTION ( 'NONE',  ( 0.000000000000000000, 0.000000000000000000, 1.000000000000000000 ) ) ;
#9689=CARTESIAN_POINT ( 'NONE',  ( -10.63672848954992389, 9.999999999999994671, -6.255867060675207370 ) ) ;
#9693=CARTESIAN_POINT ( 'NONE',  ( -10.92957602604999146, 9.999999999999998224, 4.954227274842499362 ) ) ;
#9695=CARTESIAN_POINT ( 'NONE',  ( 3.636496289402154414, 22.83000000000001606, 11.19198476289190758 ) ) ;
#9696=VERTEX_POINT ( 'NONE', #2383 ) ;
#9698=ORIENTED_EDGE ( 'NONE', *, *, #1666, .T. ) ;
#9700=CARTESIAN_POINT ( 'NONE',  ( 7.272992578804311492, -15.12000000000000277, -10.01041549318726709 ) ) ;
#9704=CARTESIAN_POINT ( 'NONE',  ( 2.138189944381242213, 1.103118577679735202, -13.49999999999999822 ) ) ;
#9713=EDGE_LOOP ( 'NONE', ( #16661, #11899, #7946, #8083, #7474 ) ) ;
#9721=CARTESIAN_POINT ( 'NONE',  ( 9.235077742801747647, -19.96812692063823391, 10.25657778616701954 ) ) ;
#9726=FACE_OUTER_BOUND ( 'NONE', #11982, .T. ) ;
#9729=CARTESIAN_POINT ( 'NONE',  ( 1.900613283894400762, 5.969143981464174686, -12.00000000000001599 ) ) ;
#9734=CARTESIAN_POINT ( 'NONE',  ( -8.000000000000191847, 5.918584287042170544, 24.73863375370590134 ) ) ;
#9736=CARTESIAN_POINT ( 'NONE',  ( 10.92172942406178926, 31.13000000000002032, 7.935100905948385908 ) ) ;
#9737=CARTESIAN_POINT ( 'NONE',  ( -3.636496289402152637, -2.669999999999998597, -11.19198476289190936 ) ) ;
#9739=CARTESIAN_POINT ( 'NONE',  ( -8.343458848123578520, 1.479999999999995097, -11.48378591275254124 ) ) ;
#9740=ADVANCED_FACE ( 'NONE', ( #11697 ), #6147, .F. ) ;
#9749=DIRECTION ( 'NONE',  ( 0.000000000000000000, 0.000000000000000000, 1.000000000000000000 ) ) ;
#9750=CARTESIAN_POINT ( 'NONE',  ( -18.06260399879729306, 6.548267719634618622, -15.28534784291422177 ) ) ;
#9755=CARTESIAN_POINT ( 'NONE',  ( -3.636496289402156190, 22.52999999999999403, 11.19198476289190758 ) ) ;
#9760=CARTESIAN_POINT ( 'NONE',  ( 4.171729424061791924, 7.030000000000008242, -12.83926296998457239 ) ) ;
#9761=ORIENTED_EDGE ( 'NONE', *, *, #16269, .T. ) ;
#9765=CARTESIAN_POINT ( 'NONE',  ( 13.49999999999999822, 1.279999999999994476, 4.386415899144237684 ) ) ;
#9768=CARTESIAN_POINT ( 'NONE',  ( -17.42428528562830792, 5.918584287042170544, -19.29752010712871169 ) ) ;
#9775=CARTESIAN_POINT ( 'NONE',  ( 1.157795017994313280, 7.956106560002609740, 18.35996578475045382 ) ) ;
#9779=DIRECTION ( 'NONE',  ( 0.000000000000000000, 1.000000000000000000, 0.000000000000000000 ) ) ;
#9781=CARTESIAN_POINT ( 'NONE',  ( -10.76106711467583210, 10.00000000000000000, 5.407306280985056723 ) ) ;
#9783=CARTESIAN_POINT ( 'NONE',  ( 3.636496289402157078, 24.02999999999999403, -11.19198476289190936 ) ) ;
#9786=VECTOR ( 'NONE', #8300, 1000.000000000000000 ) ;
#9787=ORIENTED_EDGE ( 'NONE', *, *, #13167, .T. ) ;
#9790=PLANE ( 'NONE',  #13832 ) ;
#9793=CIRCLE ( 'NONE', #12030, 26.00000000000000355 ) ;
#9800=VERTEX_POINT ( 'NONE', #7529 ) ;
#9801=CARTESIAN_POINT ( 'NONE',  ( 15.67642540545348773, 8.062211465790062093, -8.847408738254129545 ) ) ;
#9807=CIRCLE ( 'NONE', #6419, 12.00000000000000178 ) ;
#9811=CARTESIAN_POINT ( 'NONE',  ( 2.621994543952811015E-15, -12.82000000000000206, -14.19474002721660355 ) ) ;
#9817=CARTESIAN_POINT ( 'NONE',  ( -17.32050807568884210, 0.000000000000000000, 7.999999999999840128 ) ) ;
#9818=CARTESIAN_POINT ( 'NONE',  ( 3.636496289402154414, -4.169999999999999929, 11.19198476289190758 ) ) ;
#9821=EDGE_CURVE ( 'NONE', #13302, #2326, #3450, .T. ) ;
#9822=DIRECTION ( 'NONE',  ( 0.000000000000000000, 0.000000000000000000, -1.000000000000000000 ) ) ;
#9827=FACE_OUTER_BOUND ( 'NONE', #6862, .T. ) ;
#9830=CARTESIAN_POINT ( 'NONE',  ( -11.76794919243112325, -5.069999999999998508, -2.602085213965210642E-15 ) ) ;
#9832=CARTESIAN_POINT ( 'NONE',  ( -10.92172942406179104, -15.76999999999999957, 7.935100905948385908 ) ) ;
#9841=CARTESIAN_POINT ( 'NONE',  ( 15.58845726811984811, 0.000000000000000000, 11.00000000000007283 ) ) ;
#9846=CARTESIAN_POINT ( 'NONE',  ( 7.272992578804308828, 25.98000000000001108, 10.01041549318726709 ) ) ;
#9851=CARTESIAN_POINT ( 'NONE',  ( 10.92172942406179104, 9.730000000000016414, -7.935100905948385908 ) ) ;
#9852=ORIENTED_EDGE ( 'NONE', *, *, #14970, .F. ) ;
#9856=CARTESIAN_POINT ( 'NONE',  ( 8.343458848123578520, 0.9799999999999967626, 11.48378591275254124 ) ) ;
#9857=CARTESIAN_POINT ( 'NONE',  ( -9.708203932499371192, 7.096025403784452124, 7.053423027509678533 ) ) ;
#9870=CARTESIAN_POINT ( 'NONE',  ( -9.328000102585853881, 10.00000000000000000, 7.920114137930480247 ) ) ;
#9871=CARTESIAN_POINT ( 'NONE',  ( 0.000000000000000000, 9.000000000000000000, 0.000000000000000000 ) ) ;
#9872=CARTESIAN_POINT ( 'NONE',  ( -7.272992578804310604, 25.38000000000000256, 10.01041549318726709 ) ) ;
#9873=ORIENTED_EDGE ( 'NONE', *, *, #4854, .F. ) ;
#9878=CARTESIAN_POINT ( 'NONE',  ( 0.000000000000000000, 30.93000000000001393, 0.000000000000000000 ) ) ;
#9895=CARTESIAN_POINT ( 'NONE',  ( -15.67642540545354990, 8.062211465790062093, 8.847408738254019411 ) ) ;
#9899=CARTESIAN_POINT ( 'NONE',  ( 8.343458848123583849, -13.12000000000000099, -11.48378591275253768 ) ) ;
#9905=CARTESIAN_POINT ( 'NONE',  ( -7.272992578804307939, 0.4799999999999978728, -10.01041549318726886 ) ) ;
#9913=AXIS2_PLACEMENT_3D ( 'NONE', #11818, #17197, #6174 ) ;
#9914=CARTESIAN_POINT ( 'NONE',  ( -8.343458848123582072, 3.380000000000000782, 11.48378591275253768 ) ) ;
#9915=CARTESIAN_POINT ( 'NONE',  ( -7.409984580736203970E-16, -4.320000000000003837, 12.37355403259654985 ) ) ;
#9917=CARTESIAN_POINT ( 'NONE',  ( 2.621994543952811015E-15, -16.82000000000000028, -14.19474002721660355 ) ) ;
#9920=EDGE_CURVE ( 'NONE', #17255, #15482, #12460, .T. ) ;
#9926=CARTESIAN_POINT ( 'NONE',  ( 1.732050807568875195, 0.000000000000000000, -19.00000000000000000 ) ) ;
#9928=DIRECTION ( 'NONE',  ( -0.000000000000000000, 1.000000000000000000, -0.000000000000000000 ) ) ;
#9932=CARTESIAN_POINT ( 'NONE',  ( 7.272992578804308828, 19.98000000000000043, 10.01041549318726709 ) ) ;
#9933=VERTEX_POINT ( 'NONE', #1917 ) ;
#9937=CARTESIAN_POINT ( 'NONE',  ( -8.549982208541774191E-16, 5.680000000000001492, 14.19474002721660355 ) ) ;
#9941=CARTESIAN_POINT ( 'NONE',  ( -8.343458848123576743, 2.479999999999999982, -11.48378591275254301 ) ) ;
#9943=DIRECTION ( 'NONE',  ( 1.000000000000000000, 0.000000000000000000, 3.741588754404568134E-15 ) ) ;
#9950=LINE ( 'NONE', #4886, #6850 ) ;
#9951=CARTESIAN_POINT ( 'NONE',  ( 1.297534681090666941, 7.924607901204606009, 18.46823281779985848 ) ) ;
#9956=CARTESIAN_POINT ( 'NONE',  ( -3.145802693531244643, 10.00000000000000533, 12.35297229877298086 ) ) ;
#9958=ORIENTED_EDGE ( 'NONE', *, *, #3175, .F. ) ;
#9961=CARTESIAN_POINT ( 'NONE',  ( -7.272992578804310604, -13.62000000000000632, 10.01041549318726709 ) ) ;
#9977=DIRECTION ( 'NONE',  ( -0.000000000000000000, -1.000000000000000000, -0.000000000000000000 ) ) ;
#9981=CARTESIAN_POINT ( 'NONE',  ( -16.64104048077470210, 7.924936010579560097, 8.111079018422834963 ) ) ;
#9985=CARTESIAN_POINT ( 'NONE',  ( 3.636496289402157078, 30.03000000000000114, -11.19198476289190936 ) ) ;
#9988=CIRCLE ( 'NONE', #6874, 1.999999999999997335 ) ;
#9990=CARTESIAN_POINT ( 'NONE',  ( -11.76794919243112325, -16.92000000000000526, 3.823638476888994386 ) ) ;
#9993=CARTESIAN_POINT ( 'NONE',  ( -11.76794919243112325, -5.220000000000004192, -3.823638476888998827 ) ) ;
#10001=CARTESIAN_POINT ( 'NONE',  ( 0.000000000000000000, 0.000000000000000000, 0.000000000000000000 ) ) ;
#10002=CARTESIAN_POINT ( 'NONE',  ( 11.76794919243112325, -3.720000000000000195, 3.823638476888996163 ) ) ;
#10005=CARTESIAN_POINT ( 'NONE',  ( -6.299567892059761753, -18.60957387106638450, 19.22554806868047805 ) ) ;
#10015=DIRECTION ( 'NONE',  ( 0.000000000000000000, 0.000000000000000000, 1.000000000000000000 ) ) ;
#10019=CARTESIAN_POINT ( 'NONE',  ( -7.409984580736203970E-16, 19.68000000000001393, 12.37355403259654985 ) ) ;
#10020=ORIENTED_EDGE ( 'NONE', *, *, #1385, .T. ) ;
#10024=CARTESIAN_POINT ( 'NONE',  ( 13.50000000000000000, 3.430000000000016591, 1.734723475976807094E-15 ) ) ;
#10025=LINE ( 'NONE', #11250, #2653 ) ;
#10027=CARTESIAN_POINT ( 'NONE',  ( 13.50000000000000355, -1.420000000000000373, -4.386415899144233244 ) ) ;
#10045=ORIENTED_EDGE ( 'NONE', *, *, #11403, .T. ) ;
#10047=ORIENTED_EDGE ( 'NONE', *, *, #3945, .T. ) ;
#10048=CARTESIAN_POINT ( 'NONE',  ( 9.520470885617715595, -18.86999999999999744, 6.917026985038135400 ) ) ;
#10054=CARTESIAN_POINT ( 'NONE',  ( 8.378362625313673817, -1.749711886770878784E-15, 10.58551083881864407 ) ) ;
#10063=ORIENTED_EDGE ( 'NONE', *, *, #7336, .T. ) ;
#10069=CARTESIAN_POINT ( 'NONE',  ( -8.291044507619272909E-14, 7.180000000000005045, -13.50000000000000000 ) ) ;
#10072=CARTESIAN_POINT ( 'NONE',  ( -11.76794919243112325, 28.08000000000000540, 3.823638476888994386 ) ) ;
#10077=DIRECTION ( 'NONE',  ( -0.000000000000000000, -1.000000000000000000, -0.000000000000000000 ) ) ;
#10078=CARTESIAN_POINT ( 'NONE',  ( 7.272992578804308828, -1.020000000000005347, 10.01041549318726709 ) ) ;
#10081=CARTESIAN_POINT ( 'NONE',  ( 18.06260399879740675, 6.548267719634615958, 15.28534784291409387 ) ) ;
#10086=FACE_OUTER_BOUND ( 'NONE', #8929, .T. ) ;
#10087=CARTESIAN_POINT ( 'NONE',  ( -10.92172942406178926, 2.629999999999993676, -7.935100905948389460 ) ) ;
#10089=DIRECTION ( 'NONE',  ( -0.000000000000000000, -1.000000000000000000, -0.000000000000000000 ) ) ;
#10100=LINE ( 'NONE', #12824, #14845 ) ;
#10104=CARTESIAN_POINT ( 'NONE',  ( -11.76794919243112325, 18.93000000000000327, -2.602085213965210642E-15 ) ) ;
#10109=CARTESIAN_POINT ( 'NONE',  ( 3.636496289402157078, 33.03000000000000114, -11.19198476289190936 ) ) ;
#10110=CARTESIAN_POINT ( 'NONE',  ( -8.000000000000191847, 5.918584287042170544, 24.73863375370590134 ) ) ;
#10118=DIRECTION ( 'NONE',  ( -0.8660254037844383745, 0.000000000000000000, -0.5000000000000006661 ) ) ;
#10119=CARTESIAN_POINT ( 'NONE',  ( 2.207926304393408011E-15, 8.062177826491096155, 17.99999999999999645 ) ) ;
#10126=ORIENTED_EDGE ( 'NONE', *, *, #10503, .F. ) ;
#10128=ORIENTED_EDGE ( 'NONE', *, *, #56, .T. ) ;
#10129=ORIENTED_EDGE ( 'NONE', *, *, #9821, .T. ) ;
#10130=CARTESIAN_POINT ( 'NONE',  ( 10.92172942406178926, 30.13000000000001677, 7.935100905948385908 ) ) ;
#10137=EDGE_CURVE ( 'NONE', #5802, #6127, #12162, .T. ) ;
#10140=CARTESIAN_POINT ( 'NONE',  ( -1.005545769327274827E-13, 2.180000000000013483, -13.50000000000000000 ) ) ;
#10145=CYLINDRICAL_SURFACE ( 'NONE', #14283, 26.00000000000000355 ) ;
#10149=CARTESIAN_POINT ( 'NONE',  ( 8.343458848123583849, 16.87999999999999545, -11.48378591275253768 ) ) ;
#10151=AXIS2_PLACEMENT_3D ( 'NONE', #11803, #14605, #17090 ) ;
#10157=CARTESIAN_POINT ( 'NONE',  ( 11.76794919243112325, 32.28000000000000114, 3.823638476888996163 ) ) ;
#10160=EDGE_CURVE ( 'NONE', #9800, #11548, #17063, .T. ) ;
#10162=CARTESIAN_POINT ( 'NONE',  ( 18.36027427702394732, 7.956016705491392393, -1.158215859972921313 ) ) ;
#10163=AXIS2_PLACEMENT_3D ( 'NONE', #1118, #7680, #9360 ) ;
#10164=CARTESIAN_POINT ( 'NONE',  ( 11.76794919243112325, -0.7200000000000004174, 3.823638476888996163 ) ) ;
#10167=CARTESIAN_POINT ( 'NONE',  ( -8.343458848123578520, 4.480000000000010196, -11.48378591275254124 ) ) ;
#10170=CARTESIAN_POINT ( 'NONE',  ( -8.891200544363830713E-16, 7.546025403784439867, 12.00000000000000000 ) ) ;
#10171=CARTESIAN_POINT ( 'NONE',  ( -2.138190042150991399, 3.603118574164297261, 13.49999996823268233 ) ) ;
#10172=CARTESIAN_POINT ( 'NONE',  ( 8.343458848123578520, 24.98000000000000398, 11.48378591275254124 ) ) ;
#10173=ORIENTED_EDGE ( 'NONE', *, *, #1224, .T. ) ;
#10178=CARTESIAN_POINT ( 'NONE',  ( 13.50000000000000355, 3.580000000000008953, -4.386415899144233244 ) ) ;
#10187=CARTESIAN_POINT ( 'NONE',  ( -3.636496289402152637, 12.33000000000000718, -11.19198476289190936 ) ) ;
#10188=EDGE_CURVE ( 'NONE', #1191, #7389, #16169, .T. ) ;
#10193=CARTESIAN_POINT ( 'NONE',  ( -13.50000000000000000, -1.069999999999987628, -3.469446951953614189E-15 ) ) ;
#10194=CARTESIAN_POINT ( 'NONE',  ( -11.76794919243112325, 30.93000000000001393, -2.602085213965210642E-15 ) ) ;
#10213=EDGE_LOOP ( 'NONE', ( #4985, #1249, #16263, #13471 ) ) ;
#10214=ORIENTED_EDGE ( 'NONE', *, *, #848, .F. ) ;
#10215=CARTESIAN_POINT ( 'NONE',  ( 13.49999999999999822, 33.28000000000002245, 4.386415899144237684 ) ) ;
#10230=EDGE_CURVE ( 'NONE', #11897, #4019, #7387, .T. ) ;
#10231=VERTEX_POINT ( 'NONE', #15605 ) ;
#10235=DIRECTION ( 'NONE',  ( 0.000000000000000000, 0.000000000000000000, 1.000000000000000000 ) ) ;
#10237=DIRECTION ( 'NONE',  ( 4.676985943005715098E-16, 0.000000000000000000, 1.000000000000000000 ) ) ;
#10238=CARTESIAN_POINT ( 'NONE',  ( 17.32050807568879236, 0.000000000000000000, -9.999999999999960920 ) ) ;
#10240=CARTESIAN_POINT ( 'NONE',  ( -7.409984580736203970E-16, 31.68000000000000682, 12.37355403259654985 ) ) ;
#10243=VECTOR ( 'NONE', #11151, 1000.000000000000000 ) ;
#10251=CARTESIAN_POINT ( 'NONE',  ( 15.28534784291402993, 6.548267719634617734, -18.06260399879745293 ) ) ;
#10253=ORIENTED_EDGE ( 'NONE', *, *, #5724, .F. ) ;
#10254=LINE ( 'NONE', #13152, #17451 ) ;
#10255=CARTESIAN_POINT ( 'NONE',  ( -17.42428528562871293, 5.918584287042171432, 19.29752010712834220 ) ) ;
#10262=SHAPE_REPRESENTATION_RELATIONSHIP ( 'NONE' , 'NONE' ,  #8052, #15536 ) ;
#10270=EDGE_CURVE ( 'NONE', #9130, #908, #12120, .T. ) ;
#10274=CARTESIAN_POINT ( 'NONE',  ( -11.76794919243112325, 16.08000000000000895, 3.823638476888994386 ) ) ;
#10278=CARTESIAN_POINT ( 'NONE',  ( -15.58845726811976817, 0.000000000000000000, -11.00000000000018296 ) ) ;
#10279=CARTESIAN_POINT ( 'NONE',  ( 13.50000000000000355, -2.420000000000005258, -4.386415899144233244 ) ) ;
#10280=CARTESIAN_POINT ( 'NONE',  ( -3.636496289402156190, 31.53000000000000114, 11.19198476289190758 ) ) ;
#10281=CARTESIAN_POINT ( 'NONE',  ( -8.000000000000177636, 6.548282979925672542, 22.26874168100108875 ) ) ;
#10285=CARTESIAN_POINT ( 'NONE',  ( -11.48042453290631215, 9.879967940401300552, -4.614170634023106565 ) ) ;
#10296=EDGE_LOOP ( 'NONE', ( #11357, #13024, #5804, #4918 ) ) ;
#10300=CARTESIAN_POINT ( 'NONE',  ( 13.50000000000000000, 30.43000000000001393, 1.734723475976807094E-15 ) ) ;
#10306=CARTESIAN_POINT ( 'NONE',  ( 11.54774696664502009, -1.688490311990082769E-15, 6.357251958165095473 ) ) ;
#10307=CARTESIAN_POINT ( 'NONE',  ( 13.50000000000000355, 1.579999999999999405, -4.386415899144233244 ) ) ;
#10315=CARTESIAN_POINT ( 'NONE',  ( 8.375056734751542109, 9.999950376471138824, 10.58801762894534271 ) ) ;
#10320=CARTESIAN_POINT ( 'NONE',  ( -17.32050807568865736, 0.000000000000000000, -10.00000000000020428 ) ) ;
#10323=CYLINDRICAL_SURFACE ( 'NONE', #14426, 12.00000000000000178 ) ;
#10324=( BOUNDED_CURVE ( )  B_SPLINE_CURVE ( 2, ( #100, #5330, #5157, #4074, #10802, #15909, #13354, #12036, #3818, #12119, #17333, #16164, #17415 ),
 .UNSPECIFIED., .F., .F. ) 
 B_SPLINE_CURVE_WITH_KNOTS ( ( 3, 2, 2, 2, 2, 2, 3 ),
 ( 0.1297968370382597270, 0.1335521526262006542, 0.1410627838020607483, 0.1485734149779206759, 0.1560840461537806034, 0.1635946773296405587, 0.1673499929175705225 ),
 .UNSPECIFIED. ) 
 CURVE ( )  GEOMETRIC_REPRESENTATION_ITEM ( )  RATIONAL_B_SPLINE_CURVE ( ( 0.9755282581475767101, 0.9755282581475053227, 1.000000000000000000, 0.9510565162951534202, 1.000000000000000000, 0.9510565162951534202, 1.000000000000000000, 0.9510565162951534202, 1.000000000000000000, 0.9510565162951534202, 1.000000000000000000, 0.9755282581475767101, 0.9755282581475767101 ) ) 
 REPRESENTATION_ITEM ( '' )  );
#10327=EDGE_CURVE ( 'NONE', #368, #3099, #4680, .T. ) ;
#10329=CARTESIAN_POINT ( 'NONE',  ( 18.35881383260823441, 7.956441918454667750, 1.156263389813445341 ) ) ;
#10336=CARTESIAN_POINT ( 'NONE',  ( 11.00000000000001599, 7.773118517290098062, -15.58845726811988364 ) ) ;
#10338=CARTESIAN_POINT ( 'NONE',  ( -8.549982208541774191E-16, 27.68000000000000327, 14.19474002721660355 ) ) ;
#10341=CARTESIAN_POINT ( 'NONE',  ( 0.000000000000000000, 9.000000000000000000, 0.000000000000000000 ) ) ;
#10346=CARTESIAN_POINT ( 'NONE',  ( -8.343458848123582072, -2.620000000000006324, 11.48378591275254124 ) ) ;
#10353=AXIS2_PLACEMENT_3D ( 'NONE', #7354, #15274, #9749 ) ;
#10360=CARTESIAN_POINT ( 'NONE',  ( -8.891200544363830713E-16, 5.680000000000002380, 13.49999999999999822 ) ) ;
#10361=EDGE_LOOP ( 'NONE', ( #7910, #11202, #6704, #9324, #16838 ) ) ;
#10362=CARTESIAN_POINT ( 'NONE',  ( -11.76794919243112325, 13.07999999999999829, 3.823638476888994386 ) ) ;
#10363=EDGE_LOOP ( 'NONE', ( #15286, #3393, #9432, #4613 ) ) ;
#10366=DIRECTION ( 'NONE',  ( -0.000000000000000000, 1.000000000000000000, -0.000000000000000000 ) ) ;
#10367=CARTESIAN_POINT ( 'NONE',  ( 13.50000000000000000, 0.4300000000000137046, 1.734723475976807094E-15 ) ) ;
#10383=VERTEX_POINT ( 'NONE', #4847 ) ;
#10386=CARTESIAN_POINT ( 'NONE',  ( -9.520470885617717371, 7.230000000000014637, 6.917026985038133624 ) ) ;
#10387=ORIENTED_EDGE ( 'NONE', *, *, #3850, .F. ) ;
#10390=CARTESIAN_POINT ( 'NONE',  ( 13.49999999999999822, 21.28000000000000469, 4.386415899144237684 ) ) ;
#10396=CARTESIAN_POINT ( 'NONE',  ( -1.003751346110120011E-07, 3.679997203684337137, 13.49999999999999822 ) ) ;
#10400=DIRECTION ( 'NONE',  ( 0.000000000000000000, 0.000000000000000000, 1.000000000000000000 ) ) ;
#10405=ORIENTED_EDGE ( 'NONE', *, *, #11641, .T. ) ;
#10406=CARTESIAN_POINT ( 'NONE',  ( 13.50000000000000000, 15.42999999999999972, 1.734723475976807094E-15 ) ) ;
#10408=EDGE_CURVE ( 'NONE', #12936, #12048, #6080, .T. ) ;
#10411=LINE ( 'NONE', #2331, #1002 ) ;
#10424=ADVANCED_FACE ( 'NONE', ( #10086 ), #2084, .F. ) ;
#10426=DIRECTION ( 'NONE',  ( 0.000000000000000000, 0.000000000000000000, -1.000000000000000000 ) ) ;
#10428=DIRECTION ( 'NONE',  ( 0.000000000000000000, -0.2588190451025143002, -0.9659258262890700886 ) ) ;
#10431=CARTESIAN_POINT ( 'NONE',  ( 17.42428528562844292, 5.918584287042172321, 19.29752010712858024 ) ) ;
#10433=CARTESIAN_POINT ( 'NONE',  ( 8.343458848123578520, -11.02000000000000846, 11.48378591275254124 ) ) ;
#10435=AXIS2_PLACEMENT_3D ( 'NONE', #7089, #11236, #11062 ) ;
#10446=ORIENTED_EDGE ( 'NONE', *, *, #4165, .F. ) ;
#10448=CARTESIAN_POINT ( 'NONE',  ( 11.76794919243112680, 11.58000000000000362, -3.823638476888993942 ) ) ;
#10453=CARTESIAN_POINT ( 'NONE',  ( 4.171729424061791924, -1.969999999999999529, -12.83926296998457239 ) ) ;
#10458=CARTESIAN_POINT ( 'NONE',  ( 10.92172942406178926, 7.129999999999997229, 7.935100905948385908 ) ) ;
#10472=VERTEX_POINT ( 'NONE', #3346 ) ;
#10473=EDGE_CURVE ( 'NONE', #6360, #2328, #9010, .T. ) ;
#10476=ORIENTED_EDGE ( 'NONE', *, *, #10755, .T. ) ;
#10477=CARTESIAN_POINT ( 'NONE',  ( 13.50000000000000000, 27.43000000000001037, 1.734723475976807094E-15 ) ) ;
#10478=CARTESIAN_POINT ( 'NONE',  ( 0.000000000000000000, 5.918584287042170544, 0.000000000000000000 ) ) ;
#10485=DIRECTION ( 'NONE',  ( 0.000000000000000000, -1.000000000000000000, 0.000000000000000000 ) ) ;
#10488=CARTESIAN_POINT ( 'NONE',  ( 19.29752010712851984, 0.000000000000000000, -17.42428528562851042 ) ) ;
#10493=ORIENTED_EDGE ( 'NONE', *, *, #8281, .F. ) ;
#10494=CARTESIAN_POINT ( 'NONE',  ( 2.621994543952811015E-15, 16.18000000000000327, -14.19474002721660355 ) ) ;
#10497=CYLINDRICAL_SURFACE ( 'NONE', #11881, 1.999999999999997335 ) ;
#10503=EDGE_CURVE ( 'NONE', #9086, #12936, #14685, .T. ) ;
#10506=CIRCLE ( 'NONE', #4583, 12.00000000000000178 ) ;
#10512=ORIENTED_EDGE ( 'NONE', *, *, #6120, .T. ) ;
#10513=CARTESIAN_POINT ( 'NONE',  ( -13.49999999999999822, 8.780000000000004690, -4.386415899144240349 ) ) ;
#10516=CARTESIAN_POINT ( 'NONE',  ( 8.343458848123583849, -4.120000000000001883, -11.48378591275253768 ) ) ;
#10529=CARTESIAN_POINT ( 'NONE',  ( 11.76794919243112680, 11.58000000000000362, -3.823638476888993942 ) ) ;
#10531=ORIENTED_EDGE ( 'NONE', *, *, #277, .T. ) ;
#10532=CARTESIAN_POINT ( 'NONE',  ( 7.272992578804308828, 7.980000000000000426, 10.01041549318726709 ) ) ;
#10533=ORIENTED_EDGE ( 'NONE', *, *, #4247, .F. ) ;
#10537=CARTESIAN_POINT ( 'NONE',  ( -13.49999999999999822, -6.920000000000000817, 4.386415899144235908 ) ) ;
#10542=FACE_OUTER_BOUND ( 'NONE', #11446, .T. ) ;
#10548=B_SPLINE_CURVE_WITH_KNOTS ( 'NONE', 3,
 ( #10315, #7576, #6248, #14180 ),
 .UNSPECIFIED., .F., .F.,
 ( 4, 4 ),
 ( 0.5895808622224875117, 0.5895837205860048336 ),
 .UNSPECIFIED. ) ;
#10556=ORIENTED_EDGE ( 'NONE', *, *, #558, .F. ) ;
#10559=CARTESIAN_POINT ( 'NONE',  ( 3.636496289402154414, 7.830000000000003624, 11.19198476289190758 ) ) ;
#10560=ORIENTED_EDGE ( 'NONE', *, *, #2507, .F. ) ;
#10562=CARTESIAN_POINT ( 'NONE',  ( 8.343458848123578520, 20.98000000000001464, 11.48378591275254124 ) ) ;
#10576=ORIENTED_EDGE ( 'NONE', *, *, #3206, .F. ) ;
#10582=CARTESIAN_POINT ( 'NONE',  ( 8.847408738254074478, 8.062211465790062093, 15.67642540545352148 ) ) ;
#10586=CIRCLE ( 'NONE', #3513, 1.999999999999998224 ) ;
#10587=EDGE_CURVE ( 'NONE', #1796, #7861, #10922, .T. ) ;
#10592=CARTESIAN_POINT ( 'NONE',  ( 7.272992578804311492, 17.87999999999999190, -10.01041549318726709 ) ) ;
#10593=DIRECTION ( 'NONE',  ( -0.000000000000000000, -1.000000000000000000, -0.000000000000000000 ) ) ;
#10596=CARTESIAN_POINT ( 'NONE',  ( -4.171729424061791036, 18.53000000000001890, 12.83926296998457239 ) ) ;
#10599=CARTESIAN_POINT ( 'NONE',  ( -7.272992578804310604, 28.38000000000000966, 10.01041549318726709 ) ) ;
#10612=CARTESIAN_POINT ( 'NONE',  ( 11.76794919243112325, 11.27999999999999936, 3.823638476888996163 ) ) ;
#10614=CARTESIAN_POINT ( 'NONE',  ( -10.92172942406179104, 8.230000000000014637, 7.935100905948385908 ) ) ;
#10615=CARTESIAN_POINT ( 'NONE',  ( -3.636496289402156190, 4.530000000000006466, 11.19198476289190758 ) ) ;
#10619=CARTESIAN_POINT ( 'NONE',  ( -10.92172942406179104, -9.769999999999994245, 7.935100905948385908 ) ) ;
#10620=LINE ( 'NONE', #12199, #8859 ) ;
#10626=( BOUNDED_CURVE ( )  B_SPLINE_CURVE ( 2, ( #12669, #3383, #561, #5968, #15472, #8795, #16724, #4631, #14153, #9231, #5156, #7722, #3727 ),
 .UNSPECIFIED., .F., .T. ) 
 B_SPLINE_CURVE_WITH_KNOTS ( ( 3, 2, 2, 2, 2, 2, 3 ),
 ( 0.05470091489015040803, 0.05845616897609282742, 0.06596667714797772863, 0.07347718531986256740, 0.08098769349174740617, 0.08849820166363223106, 0.09225345574959326056 ),
 .UNSPECIFIED. ) 
 CURVE ( )  GEOMETRIC_REPRESENTATION_ITEM ( )  RATIONAL_B_SPLINE_CURVE ( ( 0.9755282581475767101, 0.9755282581475767101, 1.000000000000000000, 0.9510565162951534202, 1.000000000000000000, 0.9510565162951534202, 1.000000000000000000, 0.9510565162951534202, 1.000000000000000000, 0.9510565162951534202, 1.000000000000000000, 0.9755282581474559178, 0.9755282581475767101 ) ) 
 REPRESENTATION_ITEM ( '' )  );
#10636=ORIENTED_EDGE ( 'NONE', *, *, #4932, .F. ) ;
#10640=CARTESIAN_POINT ( 'NONE',  ( -7.409984580736203970E-16, 7.679999999999995275, 12.37355403259654985 ) ) ;
#10642=ORIENTED_EDGE ( 'NONE', *, *, #558, .T. ) ;
#10643=CARTESIAN_POINT ( 'NONE',  ( 13.50000000000000355, 27.58000000000000895, -4.386415899144233244 ) ) ;
#10647=CARTESIAN_POINT ( 'NONE',  ( -4.171729424061791036, 9.530000000000010019, 12.83926296998457239 ) ) ;
#10653=DIRECTION ( 'NONE',  ( -0.000000000000000000, 1.000000000000000000, -0.000000000000000000 ) ) ;
#10657=DIRECTION ( 'NONE',  ( 0.000000000000000000, 1.000000000000000000, 0.000000000000000000 ) ) ;
#10661=ORIENTED_EDGE ( 'NONE', *, *, #10904, .T. ) ;
#10674=CARTESIAN_POINT ( 'NONE',  ( -3.636496289402152637, 18.33000000000001251, -11.19198476289190936 ) ) ;
#10680=EDGE_CURVE ( 'NONE', #908, #8520, #8258, .T. ) ;
#10682=CARTESIAN_POINT ( 'NONE',  ( 10.99999999999990941, 7.773118517290098062, 15.58845726811995824 ) ) ;
#10683=CARTESIAN_POINT ( 'NONE',  ( 3.636496289402154414, -7.169999999999995488, 11.19198476289190758 ) ) ;
#10685=CARTESIAN_POINT ( 'NONE',  ( 13.50000000000000355, -4.420000000000007923, -4.386415899144233244 ) ) ;
#10691=AXIS2_PLACEMENT_3D ( 'NONE', #17295, #15786, #14370 ) ;
#10698=AXIS2_PLACEMENT_3D ( 'NONE', #932, #3499, #10237 ) ;
#10700=CARTESIAN_POINT ( 'NONE',  ( -9.520470885617717371, 1.230000000000008864, 6.917026985038133624 ) ) ;
#10704=CARTESIAN_POINT ( 'NONE',  ( 4.171729424061789260, -9.169999999999998153, 12.83926296998457239 ) ) ;
#10712=B_SPLINE_CURVE_WITH_KNOTS ( 'NONE', 3,
 ( #17062, #3376, #15724, #8788 ),
 .UNSPECIFIED., .F., .F.,
 ( 4, 4 ),
 ( 2.383248697944731098E-07, 0.007646667935218613710 ),
 .UNSPECIFIED. ) ;
#10724=ORIENTED_EDGE ( 'NONE', *, *, #10904, .F. ) ;
#10725=EDGE_LOOP ( 'NONE', ( #16994, #5121, #13468, #2129 ) ) ;
#10726=CARTESIAN_POINT ( 'NONE',  ( -8.343458848123582072, 26.37999999999999901, 11.48378591275254124 ) ) ;
#10729=CARTESIAN_POINT ( 'NONE',  ( 13.49999999999999822, 10.28000000000000114, 4.386415899144237684 ) ) ;
#10730=B_SPLINE_CURVE_WITH_KNOTS ( 'NONE', 3,
 ( #2961, #11381, #7227, #13744, #12613, #11117 ),
 .UNSPECIFIED., .F., .F.,
 ( 4, 2, 4 ),
 ( 2.344180274388505696E-07, 0.0005321324433834107633, 0.001064030468739382692 ),
 .UNSPECIFIED. ) ;
#10739=CARTESIAN_POINT ( 'NONE',  ( 7.999999999999849010, 0.000000000000000000, 24.73863375370601148 ) ) ;
#10744=ORIENTED_EDGE ( 'NONE', *, *, #3581, .F. ) ;
#10747=ORIENTED_EDGE ( 'NONE', *, *, #3261, .F. ) ;
#10750=CARTESIAN_POINT ( 'NONE',  ( 8.708180880075632402, 8.055324230341707192, 15.78346433836038898 ) ) ;
#10755=EDGE_CURVE ( 'NONE', #7575, #1725, #17201, .T. ) ;
#10758=EDGE_CURVE ( 'NONE', #9365, #4394, #1421, .T. ) ;
#10763=CARTESIAN_POINT ( 'NONE',  ( 13.50000000000000355, 22.58000000000000895, -4.386415899144233244 ) ) ;
#10764=EDGE_LOOP ( 'NONE', ( #12869, #7577, #10253, #6955 ) ) ;
#10769=CARTESIAN_POINT ( 'NONE',  ( 13.50000000000000355, -7.419999999999999929, -4.386415899144233244 ) ) ;
#10782=CARTESIAN_POINT ( 'NONE',  ( -7.272992578804310604, 10.37999999999999901, 10.01041549318726709 ) ) ;
#10784=CARTESIAN_POINT ( 'NONE',  ( 11.76794919243112325, -0.7200000000000004174, 3.823638476888996163 ) ) ;
#10788=CARTESIAN_POINT ( 'NONE',  ( 8.343458848123583849, -5.120000000000007212, -11.48378591275253768 ) ) ;
#10791=DIRECTION ( 'NONE',  ( -0.8660254037844365982, -0.000000000000000000, -0.5000000000000036637 ) ) ;
#10798=CARTESIAN_POINT ( 'NONE',  ( -7.416407864998736166, 9.346025403784448571, -10.20780970022448031 ) ) ;
#10800=EDGE_CURVE ( 'NONE', #2220, #11282, #16003, .T. ) ;
#10802=CARTESIAN_POINT ( 'NONE',  ( -9.708203932499369415, 4.363974596215572710, 7.053423027509678533 ) ) ;
#10803=CARTESIAN_POINT ( 'NONE',  ( -3.708203932499378297, 1.663974596215580748, 11.41267819554186858 ) ) ;
#10807=CARTESIAN_POINT ( 'NONE',  ( -18.46851087777848477, 7.924527533097216470, 1.297848593170422893 ) ) ;
#10810=CARTESIAN_POINT ( 'NONE',  ( 13.49999999999999822, 12.28000000000001002, 4.386415899144237684 ) ) ;
#10815=CARTESIAN_POINT ( 'NONE',  ( 13.50000000000000000, 16.42999999999999972, 1.734723475976807094E-15 ) ) ;
#10822=DIRECTION ( 'NONE',  ( -0.000000000000000000, 1.000000000000000000, -0.000000000000000000 ) ) ;
#10832=CARTESIAN_POINT ( 'NONE',  ( 11.76794919243112325, 23.43000000000000682, 1.734723475976807094E-15 ) ) ;
#10844=CYLINDRICAL_SURFACE ( 'NONE', #6761, 26.00000000000000355 ) ;
#10846=ORIENTED_EDGE ( 'NONE', *, *, #5899, .F. ) ;
#10848=CARTESIAN_POINT ( 'NONE',  ( 13.50000000000000000, 22.43000000000000682, 1.734723475976807094E-15 ) ) ;
#10849=ORIENTED_EDGE ( 'NONE', *, *, #5434, .F. ) ;
#10855=CARTESIAN_POINT ( 'NONE',  ( 13.49999999999999822, -16.72000000000000597, 4.386415899144237684 ) ) ;
#10868=CARTESIAN_POINT ( 'NONE',  ( 15.58845726811984811, 0.000000000000000000, 11.00000000000007283 ) ) ;
#10869=DIRECTION ( 'NONE',  ( -0.000000000000000000, -1.000000000000000000, -0.000000000000000000 ) ) ;
#10871=CARTESIAN_POINT ( 'NONE',  ( 9.520470885617715595, 2.129999999999992788, 6.917026985038135400 ) ) ;
#10875=CARTESIAN_POINT ( 'NONE',  ( 2.621994543952811015E-15, -10.82000000000000206, -14.19474002721660355 ) ) ;
#10887=DIRECTION ( 'NONE',  ( -0.000000000000000000, -1.000000000000000000, -0.000000000000000000 ) ) ;
#10897=CARTESIAN_POINT ( 'NONE',  ( -4.171729424061791036, 11.53000000000001180, 12.83926296998457239 ) ) ;
#10898=ORIENTED_EDGE ( 'NONE', *, *, #160, .T. ) ;
#10902=AXIS2_PLACEMENT_3D ( 'NONE', #12998, #880, #15682 ) ;
#10903=CARTESIAN_POINT ( 'NONE',  ( 13.50000000000000000, 13.42999999999999794, 1.734723475976807094E-15 ) ) ;
#10904=EDGE_CURVE ( 'NONE', #1713, #14459, #17058, .T. ) ;
#10912=CARTESIAN_POINT ( 'NONE',  ( -7.779800476318354832E-16, 7.813974596215564006, 12.00000000000000355 ) ) ;
#10916=AXIS2_PLACEMENT_3D ( 'NONE', #1012, #11978, #6681 ) ;
#10917=DIRECTION ( 'NONE',  ( 0.000000000000000000, 0.000000000000000000, 1.000000000000000000 ) ) ;
#10919=CARTESIAN_POINT ( 'NONE',  ( -8.000000000000197176, 0.000000000000000000, 24.73863375370590134 ) ) ;
#10920=CARTESIAN_POINT ( 'NONE',  ( -9.870106908097179499, 8.002076557278329005, -15.32050807568887940 ) ) ;
#10921=ORIENTED_EDGE ( 'NONE', *, *, #9277, .F. ) ;
#10922=LINE ( 'NONE', #6953, #4211 ) ;
#10925=CARTESIAN_POINT ( 'NONE',  ( -9.520470885617715595, -14.37000000000000099, -6.917026985038136289 ) ) ;
#10928=CARTESIAN_POINT ( 'NONE',  ( -10.85006967914022979, 7.815232006635826956, 15.50189495701166464 ) ) ;
#10929=CIRCLE ( 'NONE', #13178, 13.50000000000000000 ) ;
#10937=EDGE_CURVE ( 'NONE', #546, #14568, #1114, .T. ) ;
#10939=ORIENTED_EDGE ( 'NONE', *, *, #56, .F. ) ;
#10940=CARTESIAN_POINT ( 'NONE',  ( 15.43600950528672477, 7.854010657973331533, -10.69176227072927432 ) ) ;
#10944=CARTESIAN_POINT ( 'NONE',  ( 24.73863375370592976, 0.000000000000000000, 8.000000000000104805 ) ) ;
#10948=CARTESIAN_POINT ( 'NONE',  ( -10.92172942406178926, -18.36999999999999744, -7.935100905948389460 ) ) ;
#10954=CARTESIAN_POINT ( 'NONE',  ( -15.43323788540784314, 8.055324194567102580, -9.314791131849441186 ) ) ;
#10962=CARTESIAN_POINT ( 'NONE',  ( -19.00000000000001776, 7.773118517290098950, 1.732050807568674466 ) ) ;
#10965=CARTESIAN_POINT ( 'NONE',  ( 7.272992578804308828, -1.020000000000005347, 10.01041549318726709 ) ) ;
#10967=CARTESIAN_POINT ( 'NONE',  ( -8.343458848123576743, -16.52000000000000313, -11.48378591275254301 ) ) ;
#10968=CARTESIAN_POINT ( 'NONE',  ( -17.32050807568884210, 0.000000000000000000, 7.999999999999840128 ) ) ;
#10977=CARTESIAN_POINT ( 'NONE',  ( 10.99999999999990941, 7.773118517290098062, 15.58845726811995824 ) ) ;
#10984=CIRCLE ( 'NONE', #3353, 1.999999999999997335 ) ;
#10987=CARTESIAN_POINT ( 'NONE',  ( -10.92172942406178926, 10.63000000000000078, -7.935100905948389460 ) ) ;
#10993=CARTESIAN_POINT ( 'NONE',  ( 13.50000000000000000, 7.429999999999992610, 1.734723475976807094E-15 ) ) ;
#11003=CARTESIAN_POINT ( 'NONE',  ( -8.050362892394746339, 10.00000000000000000, -9.725060096452381231 ) ) ;
#11007=CARTESIAN_POINT ( 'NONE',  ( -0.3072279589061667204, 9.999999999999998224, 12.93108829551862726 ) ) ;
#11008=CARTESIAN_POINT ( 'NONE',  ( -8.774331155933998261, 8.058088662093549459, -15.73461071973920511 ) ) ;
#11009=CARTESIAN_POINT ( 'NONE',  ( 11.76794919243112325, 23.43000000000000682, 1.734723475976807094E-15 ) ) ;
#11015=AXIS2_PLACEMENT_3D ( 'NONE', #16885, #3715, #2455 ) ;
#11024=EDGE_CURVE ( 'NONE', #7559, #16001, #7804, .T. ) ;
#11029=VERTEX_POINT ( 'NONE', #10278 ) ;
#11031=CARTESIAN_POINT ( 'NONE',  ( -13.35468963145571841, 1.171226224988986705E-15, -0.4314527491507029744 ) ) ;
#11032=CARTESIAN_POINT ( 'NONE',  ( 24.73863375370592976, 5.918584287042170544, 8.000000000000106581 ) ) ;
#11036=CARTESIAN_POINT ( 'NONE',  ( 8.343458848123583849, -19.12000000000000455, -11.48378591275253768 ) ) ;
#11041=CARTESIAN_POINT ( 'NONE',  ( -7.272992578804307939, -17.52000000000000313, -10.01041549318726886 ) ) ;
#11044=CARTESIAN_POINT ( 'NONE',  ( 10.00000000000002132, 0.000000000000000000, -15.32050807568876394 ) ) ;
#11045=CARTESIAN_POINT ( 'NONE',  ( -7.379696451821980833E-14, 6.046025403784444308, -12.00000000000000000 ) ) ;
#11051=CARTESIAN_POINT ( 'NONE',  ( 13.50000000000000355, 4.580000000000007176, -4.386415899144233244 ) ) ;
#11053=CARTESIAN_POINT ( 'NONE',  ( 7.272992578804308828, -10.02000000000000490, 10.01041549318726709 ) ) ;
#11055=CARTESIAN_POINT ( 'NONE',  ( -8.343458848123576743, -13.52000000000000135, -11.48378591275254301 ) ) ;
#11062=DIRECTION ( 'NONE',  ( 0.000000000000000000, 0.000000000000000000, -1.000000000000000000 ) ) ;
#11063=FACE_OUTER_BOUND ( 'NONE', #11099, .T. ) ;
#11064=CARTESIAN_POINT ( 'NONE',  ( 16.82677684650024474, 7.170662809914417402, 13.14483242576222821 ) ) ;
#11070=CARTESIAN_POINT ( 'NONE',  ( -18.11581985354938951, 8.027799059190092734, 0.6932941240385166459 ) ) ;
#11071=ORIENTED_EDGE ( 'NONE', *, *, #13672, .F. ) ;
#11075=CARTESIAN_POINT ( 'NONE',  ( 8.343458848123583849, 9.879999999999999005, -11.48378591275253768 ) ) ;
#11080=CARTESIAN_POINT ( 'NONE',  ( -8.343458848123582072, 3.380000000000000338, 11.48378591275254124 ) ) ;
#11090=CARTESIAN_POINT ( 'NONE',  ( 7.312260103668256263E-16, 8.062177826491094379, -18.00000000000000000 ) ) ;
#11096=CARTESIAN_POINT ( 'NONE',  ( -8.056527170155236561, 10.00000000000000355, 9.383171173929708786 ) ) ;
#11098=ORIENTED_EDGE ( 'NONE', *, *, #10503, .T. ) ;
#11099=EDGE_LOOP ( 'NONE', ( #9761, #9413, #16357, #4105 ) ) ;
#11111=CARTESIAN_POINT ( 'NONE',  ( 2.279995255611139653E-15, 15.18000000000000504, -12.37355403259654985 ) ) ;
#11113=EDGE_LOOP ( 'NONE', ( #697, #6952, #1085, #15282 ) ) ;
#11115=ORIENTED_EDGE ( 'NONE', *, *, #2530, .T. ) ;
#11117=CARTESIAN_POINT ( 'NONE',  ( -9.999999999999776179, 7.983052681820796970, -15.32050807568890427 ) ) ;
#11121=CARTESIAN_POINT ( 'NONE',  ( -10.92172942406178926, -12.36999999999999922, -7.935100905948389460 ) ) ;
#11125=EDGE_CURVE ( 'NONE', #8460, #11876, #3539, .T. ) ;
#11127=CARTESIAN_POINT ( 'NONE',  ( 11.76794919243112325, -18.56999999999999673, 1.734723475976807094E-15 ) ) ;
#11130=B_SPLINE_CURVE_WITH_KNOTS ( 'NONE', 3,
 ( #6242, #2317, #2229, #1093 ),
 .UNSPECIFIED., .F., .F.,
 ( 4, 4 ),
 ( 2.376698214939480797E-07, 0.007646667280170309916 ),
 .UNSPECIFIED. ) ;
#11139=CARTESIAN_POINT ( 'NONE',  ( -3.636496289402152637, -8.669999999999996376, -11.19198476289190936 ) ) ;
#11141=CARTESIAN_POINT ( 'NONE',  ( 8.343458848123583849, -14.12000000000000455, -11.48378591275253768 ) ) ;
#11147=CIRCLE ( 'NONE', #2935, 26.00000000000000355 ) ;
#11151=DIRECTION ( 'NONE',  ( -0.000000000000000000, 1.000000000000000000, -0.000000000000000000 ) ) ;
#11152=DIRECTION ( 'NONE',  ( 0.000000000000000000, 1.000000000000000000, 0.000000000000000000 ) ) ;
#11156=CARTESIAN_POINT ( 'NONE',  ( 7.272992578804311492, 20.87999999999999545, -10.01041549318726709 ) ) ;
#11157=EDGE_CURVE ( 'NONE', #17140, #11029, #7129, .T. ) ;
#11158=ORIENTED_EDGE ( 'NONE', *, *, #13269, .T. ) ;
#11162=CARTESIAN_POINT ( 'NONE',  ( 4.171729424061791924, 4.030000000000005578, -12.83926296998457239 ) ) ;
#11167=CARTESIAN_POINT ( 'NONE',  ( 13.50000000000000355, 4.580000000000007176, -4.386415899144233244 ) ) ;
#11168=CARTESIAN_POINT ( 'NONE',  ( 3.708203932499371192, 0.1639745962155645387, -11.41267819554184371 ) ) ;
#11169=CARTESIAN_POINT ( 'NONE',  ( -1.900613283894470484, 6.122906826104709488, -11.99999999999998934 ) ) ;
#11177=CARTESIAN_POINT ( 'NONE',  ( 1.732050807568877415, 7.773118517290098950, -19.00000000000000000 ) ) ;
#11183=CARTESIAN_POINT ( 'NONE',  ( -8.891200544363830713E-16, 4.546025403784440755, 12.00000000000000000 ) ) ;
#11185=EDGE_CURVE ( 'NONE', #16216, #16109, #13906, .T. ) ;
#11186=EDGE_LOOP ( 'NONE', ( #17424, #286, #16398, #4174 ) ) ;
#11192=CYLINDRICAL_SURFACE ( 'NONE', #1707, 13.50000000000000000 ) ;
#11201=EDGE_CURVE ( 'NONE', #2220, #5991, #5493, .T. ) ;
#11202=ORIENTED_EDGE ( 'NONE', *, *, #4672, .T. ) ;
#11206=CARTESIAN_POINT ( 'NONE',  ( -15.34211313687887923, 8.027799056124987231, 9.658320279281683796 ) ) ;
#11210=CARTESIAN_POINT ( 'NONE',  ( 13.50000000000000355, -19.42000000000000171, -4.386415899144233244 ) ) ;
#11215=DIRECTION ( 'NONE',  ( 0.000000000000000000, 0.000000000000000000, -1.000000000000000000 ) ) ;
#11216=CARTESIAN_POINT ( 'NONE',  ( -11.76794919243112325, 0.9300000000000141487, -2.602085213965210642E-15 ) ) ;
#11224=CARTESIAN_POINT ( 'NONE',  ( -0.8575635061788702274, 8.007388461842872118, -18.18484536092591242 ) ) ;
#11225=CARTESIAN_POINT ( 'NONE',  ( -23.28534784291404591, 6.548267719634617734, 4.206197538246222223 ) ) ;
#11226=DIRECTION ( 'NONE',  ( 0.000000000000000000, 0.000000000000000000, 1.000000000000000000 ) ) ;
#11227=CARTESIAN_POINT ( 'NONE',  ( -8.343458848123576743, 32.47999999999999687, -11.48378591275254301 ) ) ;
#11228=CARTESIAN_POINT ( 'NONE',  ( -7.409984580736203970E-16, -10.32000000000000384, 12.37355403259654985 ) ) ;
#11230=CARTESIAN_POINT ( 'NONE',  ( -8.343458848123582072, 2.380000000000003002, 11.48378591275253768 ) ) ;
#11236=DIRECTION ( 'NONE',  ( -0.000000000000000000, -1.000000000000000000, -0.000000000000000000 ) ) ;
#11237=CARTESIAN_POINT ( 'NONE',  ( -8.891200544363830713E-16, 7.546025403784439867, 12.00000000000000000 ) ) ;
#11238=DIRECTION ( 'NONE',  ( -0.4999999999999953371, 0.000000000000000000, -0.8660254037844412611 ) ) ;
#11239=CARTESIAN_POINT ( 'NONE',  ( -11.88920123096388792, 9.999999999999994671, -1.626927807140451154 ) ) ;
#11243=CARTESIAN_POINT ( 'NONE',  ( -7.409984580736203970E-16, 25.67999999999999616, 12.37355403259654985 ) ) ;
#11248=CARTESIAN_POINT ( 'NONE',  ( 4.171729424061791924, 10.03000000000001180, -12.83926296998457239 ) ) ;
#11250=CARTESIAN_POINT ( 'NONE',  ( 0.000000000000000000, 9.000000000000000000, -12.00000000000000178 ) ) ;
#11252=CARTESIAN_POINT ( 'NONE',  ( -8.343458848123582072, 6.380000000000007887, 11.48378591275254124 ) ) ;
#11253=CARTESIAN_POINT ( 'NONE',  ( -1.732050807568877859, 0.000000000000000000, -18.99999999999999645 ) ) ;
#11260=EDGE_CURVE ( 'NONE', #12048, #2472, #8251, .T. ) ;
#11262=DIRECTION ( 'NONE',  ( -0.8660254037844326014, 0.000000000000000000, -0.5000000000000103251 ) ) ;
#11264=CIRCLE ( 'NONE', #1641, 26.00000000000000355 ) ;
#11268=LINE ( 'NONE', #10919, #1200 ) ;
#11275=CARTESIAN_POINT ( 'NONE',  ( 0.000000000000000000, 9.000000000000000000, -14.50000000000000000 ) ) ;
#11282=VERTEX_POINT ( 'NONE', #1255 ) ;
#11285=CARTESIAN_POINT ( 'NONE',  ( 8.343458848123580296, 8.980000000000011084, 11.48378591275253768 ) ) ;
#11293=CARTESIAN_POINT ( 'NONE',  ( -11.76794919243112325, 27.78000000000000114, -3.823638476888998827 ) ) ;
#11296=EDGE_CURVE ( 'NONE', #6427, #14305, #12050, .T. ) ;
#11301=CARTESIAN_POINT ( 'NONE',  ( -9.520470885617717371, -4.769999999999996021, 6.917026985038133624 ) ) ;
#11306=CARTESIAN_POINT ( 'NONE',  ( 0.000000000000000000, 9.999999999999998224, 0.000000000000000000 ) ) ;
#11307=CARTESIAN_POINT ( 'NONE',  ( 7.416407864998740607, 8.746025403784440044, -10.20780970022447676 ) ) ;
#11308=( GEOMETRIC_REPRESENTATION_CONTEXT ( 3 ) GLOBAL_UNCERTAINTY_ASSIGNED_CONTEXT ( ( #7343 ) ) GLOBAL_UNIT_ASSIGNED_CONTEXT ( ( #8769, #7609, #1842 ) ) REPRESENTATION_CONTEXT ( 'NONE', 'WORKASPACE' ) );
#11309=CARTESIAN_POINT ( 'NONE',  ( -4.171729424061791036, 3.530000000000005578, 12.83926296998457239 ) ) ;
#11310=CARTESIAN_POINT ( 'NONE',  ( -10.92172942406178926, 29.63000000000001677, -7.935100905948389460 ) ) ;
#11311=CARTESIAN_POINT ( 'NONE',  ( -9.520470885617717371, -4.769999999999996021, 6.917026985038133624 ) ) ;
#11313=CARTESIAN_POINT ( 'NONE',  ( 10.92172942406178926, -14.86999999999999389, 7.935100905948385908 ) ) ;
#11317=CARTESIAN_POINT ( 'NONE',  ( 8.343458848123583849, 3.879999999999999893, -11.48378591275253768 ) ) ;
#11321=CARTESIAN_POINT ( 'NONE',  ( 17.32050807568873196, 0.000000000000000000, 10.00000000000008171 ) ) ;
#11325=DIRECTION ( 'NONE',  ( 0.8660254037844363761, 0.000000000000000000, 0.5000000000000041078 ) ) ;
#11329=CARTESIAN_POINT ( 'NONE',  ( 2.279995255611139653E-15, 24.17999999999999261, -12.37355403259654985 ) ) ;
#11334=CARTESIAN_POINT ( 'NONE',  ( 4.171729424061789260, 8.830000000000005400, 12.83926296998457239 ) ) ;
#11335=EDGE_LOOP ( 'NONE', ( #17228, #13469, #17142, #8385 ) ) ;
#11338=CARTESIAN_POINT ( 'NONE',  ( 2.621994543952811015E-15, -0.8199999999999973976, -14.19474002721660355 ) ) ;
#11343=LINE ( 'NONE', #15381, #2395 ) ;
#11357=ORIENTED_EDGE ( 'NONE', *, *, #16042, .T. ) ;
#11361=CARTESIAN_POINT ( 'NONE',  ( 3.636496289402157078, -17.96999999999999886, -11.19198476289190936 ) ) ;
#11369=CARTESIAN_POINT ( 'NONE',  ( -0.8552964561740145077, 8.007719221390686926, 18.18372103750109758 ) ) ;
#11372=VECTOR ( 'NONE', #13894, 1000.000000000000114 ) ;
#11376=ORIENTED_EDGE ( 'NONE', *, *, #7267, .F. ) ;
#11381=CARTESIAN_POINT ( 'NONE',  ( -10.84872848410749668, 7.815608730986070007, -15.50112061769889493 ) ) ;
#11385=CARTESIAN_POINT ( 'NONE',  ( -9.520470885617715595, 30.63000000000001677, -6.917026985038136289 ) ) ;
#11390=CARTESIAN_POINT ( 'NONE',  ( 9.520470885617715595, -15.86999999999999567, 6.917026985038135400 ) ) ;
#11393=CARTESIAN_POINT ( 'NONE',  ( 7.272992578804308828, -7.020000000000005791, 10.01041549318726709 ) ) ;
#11396=FACE_OUTER_BOUND ( 'NONE', #9713, .T. ) ;
#11400=DIRECTION ( 'NONE',  ( 0.000000000000000000, 1.000000000000000000, 0.000000000000000000 ) ) ;
#11401=DIRECTION ( 'NONE',  ( 0.000000000000000000, 1.000000000000000000, 0.000000000000000000 ) ) ;
#11402=CARTESIAN_POINT ( 'NONE',  ( -7.409984580736203970E-16, -7.320000000000002949, 12.37355403259654985 ) ) ;
#11403=EDGE_CURVE ( 'NONE', #1796, #15915, #3101, .T. ) ;
#11416=FACE_OUTER_BOUND ( 'NONE', #655, .T. ) ;
#11417=FACE_OUTER_BOUND ( 'NONE', #3319, .T. ) ;
#11421=CARTESIAN_POINT ( 'NONE',  ( 11.76794919243112325, 17.28000000000001535, 3.823638476888996163 ) ) ;
#11422=ORIENTED_EDGE ( 'NONE', *, *, #7415, .F. ) ;
#11426=EDGE_CURVE ( 'NONE', #2957, #2562, #7187, .T. ) ;
#11430=AXIS2_PLACEMENT_3D ( 'NONE', #1295, #6799, #4220 ) ;
#11432=DIRECTION ( 'NONE',  ( 0.000000000000000000, 0.000000000000000000, -1.000000000000000000 ) ) ;
#11437=LINE ( 'NONE', #4459, #16819 ) ;
#11440=DIRECTION ( 'NONE',  ( -0.000000000000000000, 1.000000000000000000, -0.000000000000000000 ) ) ;
#11444=VERTEX_POINT ( 'NONE', #4533 ) ;
#11446=EDGE_LOOP ( 'NONE', ( #998, #16748, #1513, #1808 ) ) ;
#11448=ORIENTED_EDGE ( 'NONE', *, *, #3771, .F. ) ;
#11465=CARTESIAN_POINT ( 'NONE',  ( 2.621994543952811015E-15, 17.17999999999999972, -14.19474002721660355 ) ) ;
#11469=CARTESIAN_POINT ( 'NONE',  ( 15.43323788540791419, 8.055324194567102580, 9.314791131849325723 ) ) ;
#11472=CARTESIAN_POINT ( 'NONE',  ( 9.520470885617715595, 26.13000000000001322, 6.917026985038135400 ) ) ;
#11473=AXIS2_PLACEMENT_3D ( 'NONE', #6485, #13014, #6307 ) ;
#11476=CARTESIAN_POINT ( 'NONE',  ( -7.272992578804310604, -16.62000000000000099, 10.01041549318726709 ) ) ;
#11478=CARTESIAN_POINT ( 'NONE',  ( -11.00000000000012612, 0.000000000000000000, 15.58845726811980725 ) ) ;
#11479=EDGE_CURVE ( 'NONE', #201, #3761, #4878, .T. ) ;
#11480=CARTESIAN_POINT ( 'NONE',  ( -3.636496289402156190, -1.469999999999999085, 11.19198476289190758 ) ) ;
#11485=AXIS2_PLACEMENT_3D ( 'NONE', #15363, #9928, #7093 ) ;
#11489=CARTESIAN_POINT ( 'NONE',  ( 10.92172942406178926, 28.13000000000001677, 7.935100905948385908 ) ) ;
#11500=DIRECTION ( 'NONE',  ( 0.8660254037844332675, 0.000000000000000000, 0.5000000000000092149 ) ) ;
#11501=CARTESIAN_POINT ( 'NONE',  ( 15.58845726811991916, 0.000000000000000000, -10.99999999999996092 ) ) ;
#11505=CARTESIAN_POINT ( 'NONE',  ( 11.76794919243112325, 14.42999999999999794, 1.734723475976807094E-15 ) ) ;
#11506=ORIENTED_EDGE ( 'NONE', *, *, #6522, .F. ) ;
#11510=CARTESIAN_POINT ( 'NONE',  ( 13.49999999999999822, 0.2799999999999969180, 4.386415899144237684 ) ) ;
#11511=CARTESIAN_POINT ( 'NONE',  ( -7.272992578804307939, 30.48000000000000398, -10.01041549318726886 ) ) ;
#11517=CARTESIAN_POINT ( 'NONE',  ( 13.50000000000000000, 7.429999999999992610, 1.734723475976807094E-15 ) ) ;
#11532=CARTESIAN_POINT ( 'NONE',  ( 8.343458848123578520, 29.98000000000001819, 11.48378591275254124 ) ) ;
#11538=DIRECTION ( 'NONE',  ( 0.000000000000000000, 0.000000000000000000, 1.000000000000000000 ) ) ;
#11540=VECTOR ( 'NONE', #16045, 1000.000000000000000 ) ;
#11541=EDGE_CURVE ( 'NONE', #1725, #13215, #15956, .T. ) ;
#11548=VERTEX_POINT ( 'NONE', #633 ) ;
#11550=CARTESIAN_POINT ( 'NONE',  ( -4.171729424061787483, 17.33000000000001251, -12.83926296998457417 ) ) ;
#11552=CONICAL_SURFACE ( 'NONE', #12671, 14.50000000000000000, 1.308996938995753867 ) ;
#11555=CARTESIAN_POINT ( 'NONE',  ( 15.58845726811984811, 7.773118517290097174, 11.00000000000007283 ) ) ;
#11558=CARTESIAN_POINT ( 'NONE',  ( 3.636496289402154414, 31.82999999999999829, 11.19198476289190758 ) ) ;
#11559=( BOUNDED_CURVE ( )  B_SPLINE_CURVE ( 2, ( #8246, #1322, #6738, #12117, #2728, #10798, #4072, #9487, #8156 ),
 .UNSPECIFIED., .F., .F. ) 
 B_SPLINE_CURVE_WITH_KNOTS ( ( 3, 2, 2, 2, 3 ),
 ( 0.4406885646056058481, 0.4444444444444444198, 0.4500000000000000111, 0.4555555555555555469, 0.4583333333333333148 ),
 .UNSPECIFIED. ) 
 CURVE ( )  GEOMETRIC_REPRESENTATION_ITEM ( )  RATIONAL_B_SPLINE_CURVE ( ( 0.9785624164268468261, 0.9669113481358797557, 1.000000000000000000, 0.9510565162951535312, 1.000000000000000000, 0.9510565162951535312, 1.000000000000000000, 0.9755282581475770431, 0.9755282581475768211 ) ) 
 REPRESENTATION_ITEM ( '' )  );
#11563=FACE_OUTER_BOUND ( 'NONE', #5778, .T. ) ;
#11571=DIRECTION ( 'NONE',  ( -0.000000000000000000, -1.000000000000000000, -0.000000000000000000 ) ) ;
#11572=DIRECTION ( 'NONE',  ( 0.000000000000000000, 1.000000000000000000, 0.000000000000000000 ) ) ;
#11573=CARTESIAN_POINT ( 'NONE',  ( -8.343458848123582072, 27.38000000000001322, 11.48378591275254124 ) ) ;
#11581=CARTESIAN_POINT ( 'NONE',  ( 2.445080149700053643E-15, 4.180000000000004157, -13.50000000000000000 ) ) ;
#11592=CARTESIAN_POINT ( 'NONE',  ( 7.272992578804311492, 11.88000000000000966, -10.01041549318726709 ) ) ;
#11597=CARTESIAN_POINT ( 'NONE',  ( 8.343458848123578520, -0.02000000000000811892, 11.48378591275254124 ) ) ;
#11598=CARTESIAN_POINT ( 'NONE',  ( -11.76794919243112325, 30.78000000000001180, -3.823638476888998827 ) ) ;
#11600=EDGE_CURVE ( 'NONE', #9328, #14888, #12819, .T. ) ;
#11604=CARTESIAN_POINT ( 'NONE',  ( 13.49999999999999822, 7.279999999999993143, 4.386415899144236796 ) ) ;
#11608=CARTESIAN_POINT ( 'NONE',  ( 1.653273178848926472E-15, 30.93000000000001393, 13.50000000000000000 ) ) ;
#11616=CARTESIAN_POINT ( 'NONE',  ( 5.684616793965449943, 0.08402701657420055814, -10.77050272896347494 ) ) ;
#11620=CARTESIAN_POINT ( 'NONE',  ( -4.171729424061787483, 34.32999999999999829, -12.83926296998457417 ) ) ;
#11627=CARTESIAN_POINT ( 'NONE',  ( 8.000000000000019540, 5.918584287042170544, -24.73863375370596174 ) ) ;
#11631=CARTESIAN_POINT ( 'NONE',  ( 7.416407864998740607, 5.746025403784432051, -10.20780970022447676 ) ) ;
#11633=ORIENTED_EDGE ( 'NONE', *, *, #3832, .T. ) ;
#11634=DIRECTION ( 'NONE',  ( -0.000000000000000000, 1.000000000000000000, -0.000000000000000000 ) ) ;
#11640=DIRECTION ( 'NONE',  ( -7.483177508809139424E-15, 0.000000000000000000, 1.000000000000000000 ) ) ;
#11641=EDGE_CURVE ( 'NONE', #4826, #9259, #5888, .T. ) ;
#11647=CARTESIAN_POINT ( 'NONE',  ( 18.00011380242310466, 8.062143945083761309, -0.1786886709310844257 ) ) ;
#11656=CARTESIAN_POINT ( 'NONE',  ( 4.171729424061789260, 24.83000000000001961, 12.83926296998457239 ) ) ;
#11657=ORIENTED_EDGE ( 'NONE', *, *, #498, .F. ) ;
#11658=CARTESIAN_POINT ( 'NONE',  ( -8.343458848123578520, 8.480000000000000426, -11.48378591275254124 ) ) ;
#11659=( BOUNDED_CURVE ( )  B_SPLINE_CURVE ( 2, ( #12020, #17400, #5315, #5488, #4239, #11051, #83, #14909, #5753, #1752, #15173, #8324, #13678 ),
 .UNSPECIFIED., .F., .F. ) 
 B_SPLINE_CURVE_WITH_KNOTS ( ( 3, 2, 2, 2, 2, 2, 3 ),
 ( 0.5235885359481271539, 0.5264187442505494641, 0.5320791608553940844, 0.5377395774602385936, 0.5433999940650832139, 0.5490604106699278342, 0.5518906191050926280 ),
 .UNSPECIFIED. ) 
 CURVE ( )  GEOMETRIC_REPRESENTATION_ITEM ( )  RATIONAL_B_SPLINE_CURVE ( ( 0.9755282581475768211, 0.9755282581475772652, 1.000000000000000000, 0.9510565162951535312, 1.000000000000000000, 0.9510565162951535312, 1.000000000000000000, 0.9510565162951535312, 1.000000000000000000, 0.9510565162951535312, 1.000000000000000000, 0.9755282569998020570, 0.9755282581475768211 ) ) 
 REPRESENTATION_ITEM ( '' )  );
#11660=ADVANCED_FACE ( 'NONE', ( #11748 ), #14374, .F. ) ;
#11664=CARTESIAN_POINT ( 'NONE',  ( 4.171729424061789260, -2.169999999999998153, 12.83926296998457239 ) ) ;
#11677=ORIENTED_EDGE ( 'NONE', *, *, #7816, .T. ) ;
#11678=CARTESIAN_POINT ( 'NONE',  ( 9.520470885617715595, 17.13000000000000611, 6.917026985038135400 ) ) ;
#11682=CARTESIAN_POINT ( 'NONE',  ( 8.000000000000021316, 6.548282979925672542, -22.26874168100114559 ) ) ;
#11683=CARTESIAN_POINT ( 'NONE',  ( -4.171729424061791036, -3.469999999999993978, 12.83926296998457239 ) ) ;
#11694=EDGE_CURVE ( 'NONE', #5098, #4526, #10506, .T. ) ;
#11697=FACE_OUTER_BOUND ( 'NONE', #3912, .T. ) ;
#11702=CARTESIAN_POINT ( 'NONE',  ( 11.76794919243112680, 8.579999999999994742, -3.823638476888993942 ) ) ;
#11706=CARTESIAN_POINT ( 'NONE',  ( -8.343458848123582072, 32.38000000000000966, 11.48378591275254124 ) ) ;
#11714=DIRECTION ( 'NONE',  ( 0.000000000000000000, 0.000000000000000000, -1.000000000000000000 ) ) ;
#11715=AXIS2_PLACEMENT_3D ( 'NONE', #10341, #6362, #3434 ) ;
#11722=ORIENTED_EDGE ( 'NONE', *, *, #12269, .T. ) ;
#11726=DIRECTION ( 'NONE',  ( 0.000000000000000000, 1.000000000000000000, 0.000000000000000000 ) ) ;
#11729=CARTESIAN_POINT ( 'NONE',  ( -8.343458848123578520, 5.480000000000007532, -11.48378591275254124 ) ) ;
#11732=CARTESIAN_POINT ( 'NONE',  ( 18.46710335681945025, 7.924935997292879897, 1.296119813004090515 ) ) ;
#11742=ORIENTED_EDGE ( 'NONE', *, *, #6336, .T. ) ;
#11744=VECTOR ( 'NONE', #12461, 1000.000000000000000 ) ;
#11745=CARTESIAN_POINT ( 'NONE',  ( 1.900613283899841299, 4.890856018536052119, 11.99999999999824496 ) ) ;
#11748=FACE_OUTER_BOUND ( 'NONE', #10764, .T. ) ;
#11750=CARTESIAN_POINT ( 'NONE',  ( 4.171729424061791924, -9.969999999999998863, -12.83926296998457239 ) ) ;
#11755=AXIS2_PLACEMENT_3D ( 'NONE', #12627, #5924, #13844 ) ;
#11760=( BOUNDED_CURVE ( )  B_SPLINE_CURVE ( 2, ( #1351, #7119, #4281, #6767, #7037, #12145, #12415, #35, #4101, #13637, #9517, #218, #5624 ),
 .UNSPECIFIED., .F., .F. ) 
 B_SPLINE_CURVE_WITH_KNOTS ( ( 3, 2, 2, 2, 2, 2, 3 ),
 ( 0.5138888888888888395, 0.5166666666666667185, 0.5222222222222222543, 0.5277777777777777901, 0.5333333333333333259, 0.5388888888888888618, 0.5416666666666666297 ),
 .UNSPECIFIED. ) 
 CURVE ( )  GEOMETRIC_REPRESENTATION_ITEM ( )  RATIONAL_B_SPLINE_CURVE ( ( 0.9755282581475768211, 0.9755282581475762660, 1.000000000000000000, 0.9510565162951535312, 1.000000000000000000, 0.9510565162951535312, 1.000000000000000000, 0.9510565162951535312, 1.000000000000000000, 0.9510565162951535312, 1.000000000000000000, 0.9755282581475768211, 0.9755282581475768211 ) ) 
 REPRESENTATION_ITEM ( '' )  );
#11765=CARTESIAN_POINT ( 'NONE',  ( -7.272992578804307939, 9.480000000000009308, -10.01041549318726886 ) ) ;
#11766=ORIENTED_EDGE ( 'NONE', *, *, #8596, .T. ) ;
#11787=EDGE_LOOP ( 'NONE', ( #7220, #12607, #10020, #8803 ) ) ;
#11791=CARTESIAN_POINT ( 'NONE',  ( 3.636496289402157078, 3.030000000000004690, -11.19198476289190936 ) ) ;
#11795=CARTESIAN_POINT ( 'NONE',  ( 13.50000000000000000, 24.43000000000000682, 1.734723475976807094E-15 ) ) ;
#11803=CARTESIAN_POINT ( 'NONE',  ( 0.000000000000000000, 9.000000000000000000, 0.000000000000000000 ) ) ;
#11807=FACE_OUTER_BOUND ( 'NONE', #12347, .T. ) ;
#11808=B_SPLINE_CURVE_WITH_KNOTS ( 'NONE', 3,
 ( #4546, #15387, #734, #9951, #9775, #4717, #15215, #8450, #12756, #10119 ),
 .UNSPECIFIED., .F., .F.,
 ( 4, 2, 2, 2, 4 ),
 ( 2.344023999656933974E-07, 0.0005276420589627336087, 0.001055049715525501657, 0.001582457372088269705, 0.002109865028651037970 ),
 .UNSPECIFIED. ) ;
#11812=CARTESIAN_POINT ( 'NONE',  ( 0.000000000000000000, 30.93000000000001393, 0.000000000000000000 ) ) ;
#11814=CARTESIAN_POINT ( 'NONE',  ( 2.621994543952811015E-15, 13.17999999999999616, -14.19474002721660355 ) ) ;
#11815=CARTESIAN_POINT ( 'NONE',  ( 7.272992578804311492, -12.12000000000000455, -10.01041549318726709 ) ) ;
#11818=CARTESIAN_POINT ( 'NONE',  ( 10.00000000000002132, 0.000000000000000000, -17.32050807568876394 ) ) ;
#11826=VECTOR ( 'NONE', #16613, 1000.000000000000000 ) ;
#11827=CARTESIAN_POINT ( 'NONE',  ( -9.520470885617717371, 19.22999999999999687, 6.917026985038133624 ) ) ;
#11830=DIRECTION ( 'NONE',  ( 0.5000000000000008882, -0.000000000000000000, 0.8660254037844381525 ) ) ;
#11833=CARTESIAN_POINT ( 'NONE',  ( -4.171729424061791036, 9.530000000000010019, 12.83926296998457239 ) ) ;
#11838=ADVANCED_FACE ( 'NONE', ( #17038 ), #17385, .T. ) ;
#11839=CARTESIAN_POINT ( 'NONE',  ( -4.171729424061787483, -3.669999999999999485, -12.83926296998457417 ) ) ;
#11841=VECTOR ( 'NONE', #13935, 1000.000000000000000 ) ;
#11853=ORIENTED_EDGE ( 'NONE', *, *, #16344, .F. ) ;
#11854=VECTOR ( 'NONE', #3909, 1000.000000000000000 ) ;
#11855=CARTESIAN_POINT ( 'NONE',  ( 11.76794919243112325, 8.280000000000006466, 3.823638476888996163 ) ) ;
#11856=ORIENTED_EDGE ( 'NONE', *, *, #14987, .F. ) ;
#11860=CARTESIAN_POINT ( 'NONE',  ( -13.49999999999999822, -3.920000000000001705, 4.386415899144235908 ) ) ;
#11873=DIRECTION ( 'NONE',  ( 0.8660254037844379305, 0.000000000000000000, 0.5000000000000012212 ) ) ;
#11876=VERTEX_POINT ( 'NONE', #4943 ) ;
#11879=CARTESIAN_POINT ( 'NONE',  ( 11.76794919243112325, 2.430000000000015703, 1.734723475976807094E-15 ) ) ;
#11881=AXIS2_PLACEMENT_3D ( 'NONE', #8743, #14100, #1984 ) ;
#11882=EDGE_LOOP ( 'NONE', ( #13725, #7400, #8122, #11376 ) ) ;
#11883=CARTESIAN_POINT ( 'NONE',  ( 13.50000000000000000, 21.43000000000000327, 1.734723475976807094E-15 ) ) ;
#11897=VERTEX_POINT ( 'NONE', #3606 ) ;
#11898=VERTEX_POINT ( 'NONE', #13068 ) ;
#11899=ORIENTED_EDGE ( 'NONE', *, *, #8576, .F. ) ;
#11900=CARTESIAN_POINT ( 'NONE',  ( -8.343458848123582072, 17.37999999999999545, 11.48378591275254124 ) ) ;
#11915=CARTESIAN_POINT ( 'NONE',  ( -4.171729424061791036, 21.52999999999999403, 12.83926296998457239 ) ) ;
#11916=ORIENTED_EDGE ( 'NONE', *, *, #12929, .F. ) ;
#11918=CARTESIAN_POINT ( 'NONE',  ( -9.520470885617717371, 28.23000000000000398, 6.917026985038133624 ) ) ;
#11933=CARTESIAN_POINT ( 'NONE',  ( 3.636496289402157078, 12.03000000000001357, -11.19198476289190936 ) ) ;
#11936=CARTESIAN_POINT ( 'NONE',  ( -3.636496289402156190, 7.530000000000009130, 11.19198476289190758 ) ) ;
#11941=B_SPLINE_CURVE_WITH_KNOTS ( 'NONE', 3,
 ( #8308, #6978, #2698, #12354 ),
 .UNSPECIFIED., .F., .F.,
 ( 4, 4 ),
 ( 2.376698214938428888E-07, 0.007646667280170312518 ),
 .UNSPECIFIED. ) ;
#11942=CARTESIAN_POINT ( 'NONE',  ( -13.50000000000000000, -7.070000000000000284, -3.469446951953614189E-15 ) ) ;
#11947=LINE ( 'NONE', #7980, #14816 ) ;
#11948=AXIS2_PLACEMENT_3D ( 'NONE', #1234, #17406, #2721 ) ;
#11952=CARTESIAN_POINT ( 'NONE',  ( 1.732050807568877415, 7.773118517290098950, -19.00000000000000000 ) ) ;
#11953=DIRECTION ( 'NONE',  ( 0.000000000000000000, 0.000000000000000000, 1.000000000000000000 ) ) ;
#11963=CARTESIAN_POINT ( 'NONE',  ( -7.272992578804310604, 1.379999999999991456, 10.01041549318726709 ) ) ;
#11965=EDGE_LOOP ( 'NONE', ( #4828, #6429, #6247, #13151 ) ) ;
#11966=CARTESIAN_POINT ( 'NONE',  ( 4.171729424061791924, 25.02999999999999758, -12.83926296998457239 ) ) ;
#11969=CARTESIAN_POINT ( 'NONE',  ( 25.42428528562852819, 5.918584287042170544, 5.441113646577569796 ) ) ;
#11975=CARTESIAN_POINT ( 'NONE',  ( -2.624386480595337190, 10.00000000000000178, -12.78856375561946379 ) ) ;
#11978=DIRECTION ( 'NONE',  ( -0.8660254037844418162, 0.000000000000000000, 0.4999999999999945599 ) ) ;
#11982=EDGE_LOOP ( 'NONE', ( #16111, #7295, #15938, #38 ) ) ;
#11984=VERTEX_POINT ( 'NONE', #11969 ) ;
#11985=CARTESIAN_POINT ( 'NONE',  ( 11.76794919243112680, -12.42000000000000171, -3.823638476888993942 ) ) ;
#11996=DIRECTION ( 'NONE',  ( -0.000000000000000000, -1.000000000000000000, -0.000000000000000000 ) ) ;
#11999=CARTESIAN_POINT ( 'NONE',  ( -13.49999999999999822, 20.78000000000000824, -4.386415899144240349 ) ) ;
#12001=CARTESIAN_POINT ( 'NONE',  ( 0.1739742279209033626, 1.593905776373960292E-15, -12.07604168000139033 ) ) ;
#12004=CARTESIAN_POINT ( 'NONE',  ( -3.636496289402152637, -8.669999999999996376, -11.19198476289190936 ) ) ;
#12006=CARTESIAN_POINT ( 'NONE',  ( 8.343458848123583849, -10.12000000000000277, -11.48378591275253768 ) ) ;
#12008=ADVANCED_FACE ( 'NONE', ( #4925 ), #10323, .F. ) ;
#12016=LINE ( 'NONE', #15888, #15309 ) ;
#12017=AXIS2_PLACEMENT_3D ( 'NONE', #5239, #6218, #15009 ) ;
#12020=CARTESIAN_POINT ( 'NONE',  ( 2.902084407815607718E-14, 5.180000000000006821, -13.50000000000000000 ) ) ;
#12021=CYLINDRICAL_SURFACE ( 'NONE', #4401, 12.00000000000000178 ) ;
#12022=CARTESIAN_POINT ( 'NONE',  ( -7.272992578804310604, 4.379999999999999005, 10.01041549318726709 ) ) ;
#12026=CARTESIAN_POINT ( 'NONE',  ( 10.92172942406178926, -8.869999999999995666, 7.935100905948385908 ) ) ;
#12030=AXIS2_PLACEMENT_3D ( 'NONE', #16163, #1503, #5329 ) ;
#12036=CARTESIAN_POINT ( 'NONE',  ( -12.00000000000000355, 3.913974596215564539, -3.899036354794879866 ) ) ;
#12043=ORIENTED_EDGE ( 'NONE', *, *, #7024, .T. ) ;
#12045=CARTESIAN_POINT ( 'NONE',  ( 7.999999999999904965, 0.000000000000000000, 17.32050807568881368 ) ) ;
#12046=VECTOR ( 'NONE', #518, 1000.000000000000227 ) ;
#12047=ORIENTED_EDGE ( 'NONE', *, *, #2287, .F. ) ;
#12048=VERTEX_POINT ( 'NONE', #9248 ) ;
#12049=CARTESIAN_POINT ( 'NONE',  ( 13.50000000000000355, 18.57999999999999829, -4.386415899144233244 ) ) ;
#12050=LINE ( 'NONE', #1515, #5431 ) ;
#12052=CARTESIAN_POINT ( 'NONE',  ( 2.621994543952811015E-15, 14.18000000000000860, -14.19474002721660355 ) ) ;
#12057=EDGE_CURVE ( 'NONE', #4019, #16001, #15816, .T. ) ;
#12066=ORIENTED_EDGE ( 'NONE', *, *, #4911, .F. ) ;
#12086=CARTESIAN_POINT ( 'NONE',  ( 3.636496289402154414, -10.16999999999999815, 11.19198476289190758 ) ) ;
#12088=CARTESIAN_POINT ( 'NONE',  ( 8.343458848123578520, -5.020000000000003126, 11.48378591275254124 ) ) ;
#12101=CARTESIAN_POINT ( 'NONE',  ( 11.76794919243112325, 14.42999999999999794, 1.734723475976807094E-15 ) ) ;
#12103=DIRECTION ( 'NONE',  ( 0.000000000000000000, 0.000000000000000000, -1.000000000000000000 ) ) ;
#12104=CARTESIAN_POINT ( 'NONE',  ( 9.520470885617717371, -0.2699999999999924682, -6.917026985038131848 ) ) ;
#12108=CARTESIAN_POINT ( 'NONE',  ( 10.92172942406179104, -5.269999999999996909, -7.935100905948385908 ) ) ;
#12110=DIRECTION ( 'NONE',  ( -0.000000000000000000, 1.000000000000000000, -0.000000000000000000 ) ) ;
#12117=CARTESIAN_POINT ( 'NONE',  ( -12.00000000000000178, 9.646025403784440400, -3.899036354794879422 ) ) ;
#12119=CARTESIAN_POINT ( 'NONE',  ( -7.416407864998737054, 3.613974596215562052, -10.20780970022448386 ) ) ;
#12120=CIRCLE ( 'NONE', #14640, 1.999999999999998224 ) ;
#12127=CARTESIAN_POINT ( 'NONE',  ( 11.00000000000001599, 7.773118517290098062, -15.58845726811988364 ) ) ;
#12130=ORIENTED_EDGE ( 'NONE', *, *, #8074, .F. ) ;
#12131=CARTESIAN_POINT ( 'NONE',  ( 4.171729424061789260, 20.83000000000001606, 12.83926296998457239 ) ) ;
#12134=CARTESIAN_POINT ( 'NONE',  ( -10.92172942406178926, 8.629999999999999005, -7.935100905948389460 ) ) ;
#12142=CYLINDRICAL_SURFACE ( 'NONE', #12409, 1.999999999999998224 ) ;
#12145=CARTESIAN_POINT ( 'NONE',  ( 13.50000000000000355, 6.580000000000001847, -4.386415899144233244 ) ) ;
#12150=EDGE_CURVE ( 'NONE', #14160, #14568, #8352, .T. ) ;
#12152=CARTESIAN_POINT ( 'NONE',  ( -3.636496289402152637, 18.33000000000001251, -11.19198476289190936 ) ) ;
#12157=CARTESIAN_POINT ( 'NONE',  ( 9.658320279281740639, 8.027799056124987231, 15.34211313687883660 ) ) ;
#12162=B_SPLINE_CURVE_WITH_KNOTS ( 'NONE', 3,
 ( #13676, #9647, #3071, #14028, #261, #11224, #16329, #8497, #7076, #15080 ),
 .UNSPECIFIED., .F., .F.,
 ( 4, 2, 2, 2, 4 ),
 ( 2.344023999695694731E-07, 0.0005276420589627702547, 0.001055049715525570829, 0.001582457372088371620, 0.002109865028651171977 ),
 .UNSPECIFIED. ) ;
#12166=CARTESIAN_POINT ( 'NONE',  ( -11.76794919243112325, 16.08000000000000895, 3.823638476888994386 ) ) ;
#12171=CARTESIAN_POINT ( 'NONE',  ( -4.171729424061787483, 20.33000000000001606, -12.83926296998457417 ) ) ;
#12173=CARTESIAN_POINT ( 'NONE',  ( -11.58348967342891633, 9.630592963500571476E-15, -5.893907634779756322 ) ) ;
#12176=CARTESIAN_POINT ( 'NONE',  ( 9.520470885617715595, -12.86999999999999922, 6.917026985038135400 ) ) ;
#12178=CARTESIAN_POINT ( 'NONE',  ( 13.50000000000000000, -16.57000000000000028, 1.734723475976807094E-15 ) ) ;
#12191=CARTESIAN_POINT ( 'NONE',  ( -8.291044507619272909E-14, 7.180000000000005045, -13.50000000000000000 ) ) ;
#12192=CARTESIAN_POINT ( 'NONE',  ( -9.520470885617717371, 4.230000000000011084, 6.917026985038133624 ) ) ;
#12196=CARTESIAN_POINT ( 'NONE',  ( -8.343458848123582072, -12.62000000000000277, 11.48378591275254124 ) ) ;
#12199=CARTESIAN_POINT ( 'NONE',  ( 10.99999999999990941, 0.000000000000000000, 15.58845726811995824 ) ) ;
#12211=CARTESIAN_POINT ( 'NONE',  ( -18.71141623506676410, 7.854708462831349713, -1.539237008743911339 ) ) ;
#12215=CARTESIAN_POINT ( 'NONE',  ( 8.343458848123578520, 14.98000000000000043, 11.48378591275254124 ) ) ;
#12221=CARTESIAN_POINT ( 'NONE',  ( 4.171729424061791924, 8.030000000000010019, -12.83926296998457239 ) ) ;
#12231=CARTESIAN_POINT ( 'NONE',  ( 1.156690518843624726, 7.956351059191330677, -18.35912573876699838 ) ) ;
#12237=CARTESIAN_POINT ( 'NONE',  ( 6.714875219186475341, 9.999999999999998224, 11.61066632034327029 ) ) ;
#12239=VERTEX_POINT ( 'NONE', #8440 ) ;
#12241=ORIENTED_EDGE ( 'NONE', *, *, #7816, .F. ) ;
#12245=CARTESIAN_POINT ( 'NONE',  ( 10.35822530491745219, 7.924527530346062498, 15.34527529650336142 ) ) ;
#12254=ORIENTED_EDGE ( 'NONE', *, *, #696, .T. ) ;
#12255=CARTESIAN_POINT ( 'NONE',  ( 5.441113646577481866, 0.000000000000000000, -25.42428528562854595 ) ) ;
#12257=EDGE_LOOP ( 'NONE', ( #5630, #4725, #17076, #12066 ) ) ;
#12259=CARTESIAN_POINT ( 'NONE',  ( -13.41004031202893465, -1.988777493506883524E-15, 1.025385998934613463 ) ) ;
#12262=CARTESIAN_POINT ( 'NONE',  ( -7.272992578804310604, -7.620000000000000995, 10.01041549318726709 ) ) ;
#12264=CARTESIAN_POINT ( 'NONE',  ( 4.171729424061789260, -14.17000000000000171, 12.83926296998457239 ) ) ;
#12269=EDGE_CURVE ( 'NONE', #7861, #5802, #1693, .T. ) ;
#12270=CARTESIAN_POINT ( 'NONE',  ( -16.47957145870423901, 7.956016782093530360, -8.177092975169026445 ) ) ;
#12276=PRODUCT ( 'Nut', 'Nut', '', ( #6630 ) ) ;
#12279=CARTESIAN_POINT ( 'NONE',  ( 9.520470885617717371, 11.73000000000000398, -6.917026985038131848 ) ) ;
#12282=CARTESIAN_POINT ( 'NONE',  ( 13.50000000000000000, 28.43000000000001037, 1.734723475976807094E-15 ) ) ;
#12283=CARTESIAN_POINT ( 'NONE',  ( -11.76794919243112325, -1.920000000000006590, 3.823638476888994386 ) ) ;
#12285=CARTESIAN_POINT ( 'NONE',  ( -13.50000000000000000, -16.06999999999999318, -3.469446951953614189E-15 ) ) ;
#12304=CARTESIAN_POINT ( 'NONE',  ( -1.900613283894433181, 3.122906826104708600, -12.00000000000000000 ) ) ;
#12306=CARTESIAN_POINT ( 'NONE',  ( -8.549982208541774191E-16, 14.68000000000000682, 14.19474002721660355 ) ) ;
#12307=ORIENTED_EDGE ( 'NONE', *, *, #9500, .F. ) ;
#12311=MECHANICAL_DESIGN_GEOMETRIC_PRESENTATION_REPRESENTATION('',(#8657),#3265);
#12312=CARTESIAN_POINT ( 'NONE',  ( 10.92172942406179104, 7.730000000000014637, -7.935100905948385908 ) ) ;
#12313=CARTESIAN_POINT ( 'NONE',  ( -12.00000000000000178, 6.946025403784437557, 3.899036354794875869 ) ) ;
#12321=CARTESIAN_POINT ( 'NONE',  ( 12.00000000000006395, 8.713974596215594559, -3.899036354794894521 ) ) ;
#12327=CARTESIAN_POINT ( 'NONE',  ( -4.928896808027950271, 9.999999999999994671, 11.62321627039424321 ) ) ;
#12328=DIRECTION ( 'NONE',  ( 0.000000000000000000, 0.000000000000000000, 1.000000000000000000 ) ) ;
#12332=CARTESIAN_POINT ( 'NONE',  ( 3.636496289402154414, -13.17000000000000171, 11.19198476289190758 ) ) ;
#12336=CARTESIAN_POINT ( 'NONE',  ( 4.171729424061791924, 1.030000000000003135, -12.83926296998457239 ) ) ;
#12347=EDGE_LOOP ( 'NONE', ( #4728, #1333, #13825 ) ) ;
#12354=CARTESIAN_POINT ( 'NONE',  ( 25.42428528562852819, 5.918584287042170544, 5.441113646577569796 ) ) ;
#12355=CARTESIAN_POINT ( 'NONE',  ( -8.343458848123576743, -12.51999999999999780, -11.48378591275254301 ) ) ;
#12360=CARTESIAN_POINT ( 'NONE',  ( -15.31996850146879652, 8.007813437504038845, -9.831838144771289478 ) ) ;
#12363=CARTESIAN_POINT ( 'NONE',  ( 1.900613283894434735, 4.622906826104707712, 12.00000000000000000 ) ) ;
#12367=CARTESIAN_POINT ( 'NONE',  ( -8.343458848123582072, 0.3799999999999937317, 11.48378591275253768 ) ) ;
#12368=CARTESIAN_POINT ( 'NONE',  ( -1.900613283894433181, 0.1229068261047050609, -12.00000000000000000 ) ) ;
#12370=CARTESIAN_POINT ( 'NONE',  ( -10.92172942406178926, 32.62999999999999545, -7.935100905948389460 ) ) ;
#12371=CARTESIAN_POINT ( 'NONE',  ( -3.636496289402156190, -10.47000000000000064, 11.19198476289190758 ) ) ;
#12374=CARTESIAN_POINT ( 'NONE',  ( 10.92172942406179104, -14.26999999999999780, -7.935100905948385908 ) ) ;
#12377=CARTESIAN_POINT ( 'NONE',  ( 0.000000000000000000, 9.000000000000000000, 0.000000000000000000 ) ) ;
#12382=CARTESIAN_POINT ( 'NONE',  ( -19.29752010712827826, 0.000000000000000000, -17.42428528562878398 ) ) ;
#12384=CARTESIAN_POINT ( 'NONE',  ( 2.445080149700053643E-15, 4.180000000000004157, -13.50000000000000000 ) ) ;
#12391=AXIS2_PLACEMENT_3D ( 'NONE', #1008, #8900, #14427 ) ;
#12394=CARTESIAN_POINT ( 'NONE',  ( -9.708203932499371192, 4.096025403784449459, 7.053423027509678533 ) ) ;
#12396=CARTESIAN_POINT ( 'NONE',  ( -10.92172942406178926, 7.629999999999998117, -7.935100905948389460 ) ) ;
#12402=CARTESIAN_POINT ( 'NONE',  ( 13.50000000000000000, -1.569999999999994955, 1.734723475976807094E-15 ) ) ;
#12409=AXIS2_PLACEMENT_3D ( 'NONE', #4012, #3924, #6943 ) ;
#12415=CARTESIAN_POINT ( 'NONE',  ( 13.50000000000000000, 6.430000000000005045, 1.734723475976807094E-15 ) ) ;
#12417=CARTESIAN_POINT ( 'NONE',  ( 4.935098408141093351, 10.00000000000000000, 12.34347594669868720 ) ) ;
#12419=CARTESIAN_POINT ( 'NONE',  ( -7.409984580736203970E-16, 22.68000000000000327, 12.37355403259654985 ) ) ;
#12420=ORIENTED_EDGE ( 'NONE', *, *, #13794, .F. ) ;
#12424=CARTESIAN_POINT ( 'NONE',  ( -7.272992578804310604, -16.62000000000000099, 10.01041549318726709 ) ) ;
#12439=ORIENTED_EDGE ( 'NONE', *, *, #10408, .T. ) ;
#12441=CARTESIAN_POINT ( 'NONE',  ( -25.42428528562860279, 0.000000000000000000, 5.441113646577211860 ) ) ;
#12446=CARTESIAN_POINT ( 'NONE',  ( -13.50000000000000000, -15.07000000000000028, -3.469446951953614189E-15 ) ) ;
#12450=CARTESIAN_POINT ( 'NONE',  ( -3.636496289402152637, -17.66999999999999815, -11.19198476289190936 ) ) ;
#12455=CARTESIAN_POINT ( 'NONE',  ( 0.000000000000000000, 0.000000000000000000, 0.000000000000000000 ) ) ;
#12460=LINE ( 'NONE', #12631, #11841 ) ;
#12461=DIRECTION ( 'NONE',  ( -0.000000000000000000, 1.000000000000000000, -0.000000000000000000 ) ) ;
#12463=CARTESIAN_POINT ( 'NONE',  ( -8.549982208541774191E-16, 30.68000000000001037, 14.19474002721660355 ) ) ;
#12464=CARTESIAN_POINT ( 'NONE',  ( -3.636496289402156190, -7.469999999999997087, 11.19198476289190758 ) ) ;
#12466=CARTESIAN_POINT ( 'NONE',  ( -17.32050807568884210, 0.000000000000000000, 7.999999999999840128 ) ) ;
#12472=ADVANCED_FACE ( 'NONE', ( #4068 ), #7807, .F. ) ;
#12473=CARTESIAN_POINT ( 'NONE',  ( 2.445080149700053643E-15, 1.180000000000002602, -13.50000000000000000 ) ) ;
#12480=CARTESIAN_POINT ( 'NONE',  ( -18.35881383260822020, 7.956441918454669526, -1.156263389813576792 ) ) ;
#12481=CARTESIAN_POINT ( 'NONE',  ( -11.76794919243112325, 24.78000000000000824, -3.823638476888998827 ) ) ;
#12484=CARTESIAN_POINT ( 'NONE',  ( 2.222800136090958073E-15, 0.04602540378443767399, -12.00000000000000000 ) ) ;
#12486=CARTESIAN_POINT ( 'NONE',  ( -4.171729424061787483, 4.330000000000000071, -12.83926296998457417 ) ) ;
#12491=CARTESIAN_POINT ( 'NONE',  ( -4.171729424061791036, 6.530000000000008242, 12.83926296998457239 ) ) ;
#12501=CARTESIAN_POINT ( 'NONE',  ( 0.000000000000000000, 5.918584287042170544, 0.000000000000000000 ) ) ;
#12504=CARTESIAN_POINT ( 'NONE',  ( -11.03450900954605629, 9.999999999999994671, -5.378144140920507965 ) ) ;
#12506=LINE ( 'NONE', #5354, #5853 ) ;
#12509=CARTESIAN_POINT ( 'NONE',  ( -8.393536083122315361, 8.020663292675294542, -16.10013384871447073 ) ) ;
#12514=CARTESIAN_POINT ( 'NONE',  ( -11.76794919243112325, -17.22000000000000597, -3.823638476888998827 ) ) ;
#12517=CARTESIAN_POINT ( 'NONE',  ( -9.314791131849382566, 8.055324194567102580, 15.43323788540787866 ) ) ;
#12526=ORIENTED_EDGE ( 'NONE', *, *, #13910, .T. ) ;
#12530=CARTESIAN_POINT ( 'NONE',  ( -15.50190989971486921, 7.815224736851130949, 10.85009556066079917 ) ) ;
#12533=CARTESIAN_POINT ( 'NONE',  ( -8.549982208541774191E-16, -11.32000000000000028, 14.19474002721660355 ) ) ;
#12537=CARTESIAN_POINT ( 'NONE',  ( -11.76794919243112325, -17.06999999999999318, -2.602085213965210642E-15 ) ) ;
#12540=CARTESIAN_POINT ( 'NONE',  ( 3.636496289402157078, -2.970000000000000639, -11.19198476289190936 ) ) ;
#12547=CARTESIAN_POINT ( 'NONE',  ( 19.79706521687762688, 7.170682760640494813, 8.000000000000092371 ) ) ;
#12548=DIRECTION ( 'NONE',  ( -0.000000000000000000, -1.000000000000000000, -0.000000000000000000 ) ) ;
#12550=CARTESIAN_POINT ( 'NONE',  ( -4.171729424061787483, 32.32999999999999829, -12.83926296998457417 ) ) ;
#12551=CARTESIAN_POINT ( 'NONE',  ( 7.272992578804308828, -7.020000000000005791, 10.01041549318726709 ) ) ;
#12553=CARTESIAN_POINT ( 'NONE',  ( 4.171729424061789260, -15.16999999999999638, 12.83926296998457239 ) ) ;
#12556=ADVANCED_FACE ( 'NONE', ( #2458 ), #1153, .F. ) ;
#12561=DIRECTION ( 'NONE',  ( 0.000000000000000000, 0.000000000000000000, 1.000000000000000000 ) ) ;
#12563=PLANE ( 'NONE',  #2864 ) ;
#12568=CARTESIAN_POINT ( 'NONE',  ( -7.272992578804310604, 22.38000000000000966, 10.01041549318726709 ) ) ;
#12573=CARTESIAN_POINT ( 'NONE',  ( -8.343458848123576743, 7.480000000000002203, -11.48378591275254301 ) ) ;
#12576=CARTESIAN_POINT ( 'NONE',  ( 1.775737858763662015E-15, 9.999999999999998224, 14.50000000000000000 ) ) ;
#12577=CARTESIAN_POINT ( 'NONE',  ( -8.343458848123576743, -0.5200000000000069011, -11.48378591275254301 ) ) ;
#12578=CARTESIAN_POINT ( 'NONE',  ( -9.708203932499369415, 6.496025403784435603, -7.053423027509682086 ) ) ;
#12590=CARTESIAN_POINT ( 'NONE',  ( -2.219840399520819574, 10.00000000000000711, 12.61519577489909949 ) ) ;
#12591=CYLINDRICAL_SURFACE ( 'NONE', #6634, 26.00000000000000355 ) ;
#12594=AXIS2_PLACEMENT_3D ( 'NONE', #9214, #16067, #3973 ) ;
#12595=ORIENTED_EDGE ( 'NONE', *, *, #16322, .T. ) ;
#12597=ADVANCED_FACE ( 'NONE', ( #13429 ), #1318, .T. ) ;
#12603=CARTESIAN_POINT ( 'NONE',  ( -0.6926531483078592899, 8.027905821154657673, 18.11545820097774850 ) ) ;
#12607=ORIENTED_EDGE ( 'NONE', *, *, #15617, .F. ) ;
#12609=ORIENTED_EDGE ( 'NONE', *, *, #9500, .T. ) ;
#12613=CARTESIAN_POINT ( 'NONE',  ( -10.17530313047220680, 7.957378145380317847, -15.32050807568887940 ) ) ;
#12614=AXIS2_PLACEMENT_3D ( 'NONE', #4782, #7445, #11325 ) ;
#12618=CARTESIAN_POINT ( 'NONE',  ( 3.636496289402154414, 25.83000000000001961, 11.19198476289190758 ) ) ;
#12624=CARTESIAN_POINT ( 'NONE',  ( 7.272992578804308828, -4.019999999999998685, 10.01041549318726709 ) ) ;
#12627=CARTESIAN_POINT ( 'NONE',  ( -7.999999999999776179, 0.000000000000000000, -17.32050807568887762 ) ) ;
#12631=CARTESIAN_POINT ( 'NONE',  ( 8.000000000000023093, 0.000000000000000000, -17.32050807568876394 ) ) ;
#12632=CARTESIAN_POINT ( 'NONE',  ( -7.416407864998737942, 1.246025403784429164, 10.20780970022447853 ) ) ;
#12634=CARTESIAN_POINT ( 'NONE',  ( -11.76794919243112325, -8.070000000000000284, -2.602085213965210642E-15 ) ) ;
#12637=CARTESIAN_POINT ( 'NONE',  ( -10.92172942406178926, -13.36999999999999922, -7.935100905948389460 ) ) ;
#12638=EDGE_CURVE ( 'NONE', #42, #8284, #12900, .T. ) ;
#12650=CARTESIAN_POINT ( 'NONE',  ( 11.76794919243112325, 26.43000000000001037, 1.734723475976807094E-15 ) ) ;
#12657=CARTESIAN_POINT ( 'NONE',  ( -8.000000000000161648, 7.170682760640493925, 19.79706521687760201 ) ) ;
#12658=VECTOR ( 'NONE', #16753, 1000.000000000000000 ) ;
#12659=CARTESIAN_POINT ( 'NONE',  ( -4.171729424061787483, 5.330000000000001847, -12.83926296998457417 ) ) ;
#12669=CARTESIAN_POINT ( 'NONE',  ( -7.779800476318354832E-16, 7.813974596215564006, 12.00000000000000355 ) ) ;
#12671=AXIS2_PLACEMENT_3D ( 'NONE', #4160, #2639, #8070 ) ;
#12674=CARTESIAN_POINT ( 'NONE',  ( 10.00000000000002132, 0.000000000000000000, -17.32050807568876394 ) ) ;
#12676=PLANE ( 'NONE',  #360 ) ;
#12682=CARTESIAN_POINT ( 'NONE',  ( 11.76794919243112680, -18.42000000000000171, -3.823638476888993942 ) ) ;
#12685=CARTESIAN_POINT ( 'NONE',  ( -8.000000000000143885, 7.773118517290097174, 17.32050807568870709 ) ) ;
#12687=( BOUNDED_CURVE ( )  B_SPLINE_CURVE ( 2, ( #1616, #16551, #1526, #1347, #13460, #12321, #298, #16370, #1435, #15214, #4458, #6853, #10912 ),
 .UNSPECIFIED., .F., .T. ) 
 B_SPLINE_CURVE_WITH_KNOTS ( ( 3, 2, 2, 2, 2, 2, 3 ),
 ( 0.01714606201576732852, 0.02090154730321778717, 0.02841251787809168788, 0.03592348845296558513, 0.04343445902783955870, 0.05094542960271345594, 0.05470091489015040803 ),
 .UNSPECIFIED. ) 
 CURVE ( )  GEOMETRIC_REPRESENTATION_ITEM ( )  RATIONAL_B_SPLINE_CURVE ( ( 0.9755282581475768211, 0.9755282581474891135, 1.000000000000000000, 0.9510565162951536422, 1.000000000000000000, 0.9510565162951536422, 1.000000000000000000, 0.9510565162951536422, 1.000000000000000000, 0.9510565162951536422, 1.000000000000000000, 0.9755282581475768211, 0.9755282581475768211 ) ) 
 REPRESENTATION_ITEM ( '' )  );
#12689=EDGE_CURVE ( 'NONE', #15652, #4019, #786, .T. ) ;
#12690=LINE ( 'NONE', #12948, #2019 ) ;
#12693=AXIS2_PLACEMENT_3D ( 'NONE', #6105, #11571, #3691 ) ;
#12694=ORIENTED_EDGE ( 'NONE', *, *, #13650, .F. ) ;
#12696=ORIENTED_EDGE ( 'NONE', *, *, #14898, .F. ) ;
#12697=FACE_OUTER_BOUND ( 'NONE', #5254, .T. ) ;
#12701=LINE ( 'NONE', #4396, #12658 ) ;
#12702=FACE_OUTER_BOUND ( 'NONE', #17011, .T. ) ;
#12705=CARTESIAN_POINT ( 'NONE',  ( 11.76794919243112325, 29.43000000000001037, 1.734723475976807094E-15 ) ) ;
#12709=CARTESIAN_POINT ( 'NONE',  ( 11.76794919243112325, -15.57000000000000028, 1.734723475976807094E-15 ) ) ;
#12711=CARTESIAN_POINT ( 'NONE',  ( -10.00000000000014211, 0.000000000000000000, 17.32050807568869288 ) ) ;
#12712=CARTESIAN_POINT ( 'NONE',  ( 11.76794919243112325, -6.569999999999999396, 1.734723475976807094E-15 ) ) ;
#12714=CARTESIAN_POINT ( 'NONE',  ( 9.708203932499390731, 2.863974596215587365, -7.053423027509691856 ) ) ;
#12719=CARTESIAN_POINT ( 'NONE',  ( 17.42428528562844292, 0.000000000000000000, 19.29752010712858024 ) ) ;
#12721=CARTESIAN_POINT ( 'NONE',  ( 8.671371105899947196, 8.051439890486543405, -15.81984194950172906 ) ) ;
#12722=CARTESIAN_POINT ( 'NONE',  ( -8.343458848123576743, 26.48000000000001464, -11.48378591275254301 ) ) ;
#12723=CARTESIAN_POINT ( 'NONE',  ( -7.272992578804307939, -11.51999999999999957, -10.01041549318726886 ) ) ;
#12739=CARTESIAN_POINT ( 'NONE',  ( 3.636496289402157078, 18.03000000000001890, -11.19198476289190936 ) ) ;
#12740=ORIENTED_EDGE ( 'NONE', *, *, #15825, .F. ) ;
#12744=CARTESIAN_POINT ( 'NONE',  ( 13.49999999999999822, 3.280000000000003801, 4.386415899144237684 ) ) ;
#12745=CARTESIAN_POINT ( 'NONE',  ( 9.520470885617717371, 32.73000000000001108, -6.917026985038131848 ) ) ;
#12756=CARTESIAN_POINT ( 'NONE',  ( 0.1775006636059767717, 8.062177826491092603, 18.00000000000001421 ) ) ;
#12763=ORIENTED_EDGE ( 'NONE', *, *, #7336, .F. ) ;
#12765=VERTEX_POINT ( 'NONE', #12816 ) ;
#12766=ORIENTED_EDGE ( 'NONE', *, *, #10937, .T. ) ;
#12767=CARTESIAN_POINT ( 'NONE',  ( 2.279995255611139653E-15, -17.82000000000000028, -12.37355403259654985 ) ) ;
#12775=CARTESIAN_POINT ( 'NONE',  ( 9.854515491449854281, 2.875466159201984032E-15, -7.259896930270302029 ) ) ;
#12777=LINE ( 'NONE', #4999, #4867 ) ;
#12779=VECTOR ( 'NONE', #4373, 999.9999999999998863 ) ;
#12783=EDGE_LOOP ( 'NONE', ( #15626, #5256, #12694, #8342 ) ) ;
#12784=B_SPLINE_CURVE_WITH_KNOTS ( 'NONE', 3,
 ( #4848, #694, #16686, #4593, #2085, #7510, #15437, #8761, #15261, #12721, #15520, #8927, #14117, #2171, #12892, #7248, #15348, #7429 ),
 .UNSPECIFIED., .F., .F.,
 ( 4, 2, 2, 2, 2, 2, 2, 2, 4 ),
 ( 2.030049010680397696E-07, 0.0003947283216049050393, 0.0007892536383087419768, 0.001183778955012579131, 0.001578304271716416069, 0.001972829588420253223, 0.002367354905124090161, 0.002761880221827927098, 0.003156405538531764036 ),
 .UNSPECIFIED. ) ;
#12787=CARTESIAN_POINT ( 'NONE',  ( -13.49999999999999822, 17.78000000000001535, -4.386415899144240349 ) ) ;
#12790=CARTESIAN_POINT ( 'NONE',  ( -15.49921147158550916, 8.062143943920768052, 9.154805866618353605 ) ) ;
#12791=CARTESIAN_POINT ( 'NONE',  ( 15.67790026899618461, 8.062143948122718839, 8.845307762532291562 ) ) ;
#12794=CARTESIAN_POINT ( 'NONE',  ( 11.76794919243112325, 26.43000000000001037, 1.734723475976807094E-15 ) ) ;
#12799=CARTESIAN_POINT ( 'NONE',  ( -3.636496289402156190, -16.46999999999999886, 11.19198476289190758 ) ) ;
#12801=DIRECTION ( 'NONE',  ( 0.000000000000000000, 1.000000000000000000, 0.000000000000000000 ) ) ;
#12808=CARTESIAN_POINT ( 'NONE',  ( 1.900613283894434735, 7.622906826104705047, 12.00000000000000000 ) ) ;
#12812=CARTESIAN_POINT ( 'NONE',  ( 3.708203932499368527, 4.963974596215562585, 11.41267819554184193 ) ) ;
#12815=EDGE_CURVE ( 'NONE', #17188, #6168, #1268, .T. ) ;
#12816=CARTESIAN_POINT ( 'NONE',  ( -10.99999999999979394, 7.773118517290098950, -15.58845726812003996 ) ) ;
#12819=B_SPLINE_CURVE_WITH_KNOTS ( 'NONE', 3,
 ( #8766, #3519, #14121, #1839 ),
 .UNSPECIFIED., .F., .F.,
 ( 4, 4 ),
 ( 0.008786844460939023313, 0.01643317035798799036 ),
 .UNSPECIFIED. ) ;
#12823=PLANE ( 'NONE',  #5456 ) ;
#12824=CARTESIAN_POINT ( 'NONE',  ( -24.73863375370603634, 0.000000000000000000, 7.999999999999761080 ) ) ;
#12828=CARTESIAN_POINT ( 'NONE',  ( -7.409984580736203970E-16, 7.679999999999995275, 12.37355403259654985 ) ) ;
#12829=LINE ( 'NONE', #13083, #8379 ) ;
#12834=CARTESIAN_POINT ( 'NONE',  ( -13.49999999999999822, -0.9200000000000014833, 4.386415899144235908 ) ) ;
#12835=CARTESIAN_POINT ( 'NONE',  ( -11.76794919243112325, 33.93000000000001393, -2.602085213965210642E-15 ) ) ;
#12837=EDGE_CURVE ( 'NONE', #9800, #6684, #16868, .T. ) ;
#12839=AXIS2_PLACEMENT_3D ( 'NONE', #7601, #7432, #15787 ) ;
#12856=CARTESIAN_POINT ( 'NONE',  ( -13.50000000000000000, 34.93000000000001393, -3.469446951953614189E-15 ) ) ;
#12863=CARTESIAN_POINT ( 'NONE',  ( 9.103919235555860467, 2.197554810170567017E-15, 9.934002182353431465 ) ) ;
#12864=CARTESIAN_POINT ( 'NONE',  ( -1.645540471734166399, 7.815206720109966199, 18.85015970295419407 ) ) ;
#12865=CARTESIAN_POINT ( 'NONE',  ( -5.441113646577659502, 0.000000000000000000, 25.42428528562849976 ) ) ;
#12869=ORIENTED_EDGE ( 'NONE', *, *, #14875, .T. ) ;
#12870=LINE ( 'NONE', #15670, #4720 ) ;
#12876=DIRECTION ( 'NONE',  ( 0.000000000000000000, 1.000000000000000000, 0.000000000000000000 ) ) ;
#12879=CARTESIAN_POINT ( 'NONE',  ( -7.272992578804307939, 30.48000000000000398, -10.01041549318726886 ) ) ;
#12887=DIRECTION ( 'NONE',  ( -0.000000000000000000, 1.000000000000000000, -0.000000000000000000 ) ) ;
#12889=VECTOR ( 'NONE', #3778, 1000.000000000000227 ) ;
#12892=CARTESIAN_POINT ( 'NONE',  ( 9.480101247244204998, 8.043253892159592411, -15.38474694851398183 ) ) ;
#12893=CARTESIAN_POINT ( 'NONE',  ( -13.49999999999999822, 26.78000000000000114, -4.386415899144240349 ) ) ;
#12900=LINE ( 'NONE', #2093, #8552 ) ;
#12912=CARTESIAN_POINT ( 'NONE',  ( -7.409984580736203970E-16, 16.68000000000000327, 12.37355403259654985 ) ) ;
#12913=ORIENTED_EDGE ( 'NONE', *, *, #11125, .F. ) ;
#12917=CARTESIAN_POINT ( 'NONE',  ( -10.92172942406178926, -1.369999999999996110, -7.935100905948389460 ) ) ;
#12918=CARTESIAN_POINT ( 'NONE',  ( 2.279995255611139653E-15, 33.17999999999999972, -12.37355403259654985 ) ) ;
#12929=EDGE_CURVE ( 'NONE', #14960, #8561, #4898, .T. ) ;
#12932=CARTESIAN_POINT ( 'NONE',  ( 0.000000000000000000, 0.000000000000000000, 0.000000000000000000 ) ) ;
#12934=ORIENTED_EDGE ( 'NONE', *, *, #14092, .F. ) ;
#12936=VERTEX_POINT ( 'NONE', #12127 ) ;
#12937=ORIENTED_EDGE ( 'NONE', *, *, #16787, .F. ) ;
#12938=CARTESIAN_POINT ( 'NONE',  ( -8.343458848123576743, 28.48000000000001108, -11.48378591275254301 ) ) ;
#12945=FACE_OUTER_BOUND ( 'NONE', #10725, .T. ) ;
#12946=AXIS2_PLACEMENT_3D ( 'NONE', #6348, #17110, #5268 ) ;
#12948=CARTESIAN_POINT ( 'NONE',  ( 0.000000000000000000, 30.93000000000001393, -13.50000000000000000 ) ) ;
#12953=ORIENTED_EDGE ( 'NONE', *, *, #5661, .T. ) ;
#12954=CARTESIAN_POINT ( 'NONE',  ( -1.732050807569007977, 0.000000000000000000, 18.99999999999998224 ) ) ;
#12955=ORIENTED_EDGE ( 'NONE', *, *, #15929, .F. ) ;
#12958=CIRCLE ( 'NONE', #10435, 26.00000000000000355 ) ;
#12959=DIRECTION ( 'NONE',  ( 0.000000000000000000, 0.000000000000000000, 1.000000000000000000 ) ) ;
#12960=DIRECTION ( 'NONE',  ( -0.000000000000000000, 1.000000000000000000, -0.000000000000000000 ) ) ;
#12962=CARTESIAN_POINT ( 'NONE',  ( -15.58845726811999910, 7.773118517290098950, 10.99999999999985256 ) ) ;
#12974=CARTESIAN_POINT ( 'NONE',  ( 12.00000000000000178, 8.146025403784442176, 3.899036354794877202 ) ) ;
#12976=CARTESIAN_POINT ( 'NONE',  ( -10.92172942406178926, 23.63000000000001322, -7.935100905948389460 ) ) ;
#12983=CARTESIAN_POINT ( 'NONE',  ( 8.343458848123578520, -2.020000000000003126, 11.48378591275254124 ) ) ;
#12985=ADVANCED_FACE ( 'NONE', ( #370 ), #8522, .F. ) ;
#12991=CARTESIAN_POINT ( 'NONE',  ( 12.00000000000000355, 2.446025403784435337, -3.899036354794874093 ) ) ;
#12997=CARTESIAN_POINT ( 'NONE',  ( 9.520470885617715595, 14.13000000000000433, 6.917026985038135400 ) ) ;
#12998=CARTESIAN_POINT ( 'NONE',  ( 0.000000000000000000, 30.93000000000001393, 0.000000000000000000 ) ) ;
#13007=EDGE_CURVE ( 'NONE', #5466, #8460, #16134, .T. ) ;
#13014=DIRECTION ( 'NONE',  ( 0.5000000000000104361, 0.000000000000000000, -0.8660254037844326014 ) ) ;
#13018=CARTESIAN_POINT ( 'NONE',  ( 15.58845726811991916, 7.773118517290098950, -10.99999999999996092 ) ) ;
#13023=CARTESIAN_POINT ( 'NONE',  ( 9.520470885617715595, 8.129999999999999005, 6.917026985038135400 ) ) ;
#13024=ORIENTED_EDGE ( 'NONE', *, *, #3626, .T. ) ;
#13027=CARTESIAN_POINT ( 'NONE',  ( 2.621994543952811015E-15, 34.18000000000000682, -14.19474002721660355 ) ) ;
#13034=ADVANCED_FACE ( 'NONE', ( #15103 ), #6837, .F. ) ;
#13035=DIRECTION ( 'NONE',  ( 0.000000000000000000, 1.000000000000000000, 0.000000000000000000 ) ) ;
#13044=VERTEX_POINT ( 'NONE', #12484 ) ;
#13045=AXIS2_PLACEMENT_3D ( 'NONE', #884, #9133, #14482 ) ;
#13046=CARTESIAN_POINT ( 'NONE',  ( -13.49999999999999822, 16.78000000000001535, -4.386415899144240349 ) ) ;
#13050=CARTESIAN_POINT ( 'NONE',  ( -8.891200544363830713E-16, 1.546025403784439423, 12.00000000000000000 ) ) ;
#13051=CARTESIAN_POINT ( 'NONE',  ( -18.06260399879761636, 6.548267719634618622, 15.28534784291383986 ) ) ;
#13054=AXIS2_PLACEMENT_3D ( 'NONE', #16172, #7016, #16 ) ;
#13055=CYLINDRICAL_SURFACE ( 'NONE', #12946, 1.999999999999997335 ) ;
#13062=CARTESIAN_POINT ( 'NONE',  ( 10.84916736553044991, 7.815485454866775150, -15.50137400600630144 ) ) ;
#13068=CARTESIAN_POINT ( 'NONE',  ( 7.999999999999850786, 5.918584287042170544, 24.73863375370601858 ) ) ;
#13070=CARTESIAN_POINT ( 'NONE',  ( -8.343458848123582072, -8.619999999999997442, 11.48378591275254124 ) ) ;
#13077=CARTESIAN_POINT ( 'NONE',  ( -8.891200544363830713E-16, 1.546025403784439423, 12.00000000000000000 ) ) ;
#13082=CARTESIAN_POINT ( 'NONE',  ( -9.520470885617715595, 12.63000000000000256, -6.917026985038136289 ) ) ;
#13083=CARTESIAN_POINT ( 'NONE',  ( 0.000000000000000000, 9.000000000000000000, -12.00000000000000178 ) ) ;
#13088=CARTESIAN_POINT ( 'NONE',  ( 8.000000000000021316, 7.170682760640493036, -19.79706521687766596 ) ) ;
#13089=CARTESIAN_POINT ( 'NONE',  ( -13.50000000000000000, 1.930000000000015037, -3.469446951953614189E-15 ) ) ;
#13102=DIRECTION ( 'NONE',  ( 0.5000000000000012212, 0.000000000000000000, -0.8660254037844379305 ) ) ;
#13108=CARTESIAN_POINT ( 'NONE',  ( -11.76794919243112325, 3.780000000000002913, -3.823638476888998827 ) ) ;
#13111=ORIENTED_EDGE ( 'NONE', *, *, #14898, .T. ) ;
#13112=CARTESIAN_POINT ( 'NONE',  ( -8.343458848123576743, 25.48000000000001819, -11.48378591275254301 ) ) ;
#13114=CARTESIAN_POINT ( 'NONE',  ( -9.999999999999776179, 0.000000000000000000, -15.32050807568890605 ) ) ;
#13115=DIRECTION ( 'NONE',  ( 0.000000000000000000, 0.000000000000000000, -1.000000000000000000 ) ) ;
#13126=ORIENTED_EDGE ( 'NONE', *, *, #7375, .F. ) ;
#13130=EDGE_CURVE ( 'NONE', #11984, #1191, #7419, .T. ) ;
#13132=CARTESIAN_POINT ( 'NONE',  ( -13.49999999999999822, 13.78000000000000824, -4.386415899144240349 ) ) ;
#13145=CARTESIAN_POINT ( 'NONE',  ( 11.76794919243112325, 20.43000000000000327, 1.734723475976807094E-15 ) ) ;
#13148=EDGE_CURVE ( 'NONE', #2258, #8561, #14951, .T. ) ;
#13151=ORIENTED_EDGE ( 'NONE', *, *, #773, .F. ) ;
#13152=CARTESIAN_POINT ( 'NONE',  ( -15.58845726811999910, 0.000000000000000000, 10.99999999999985256 ) ) ;
#13157=CARTESIAN_POINT ( 'NONE',  ( -8.343458848123576743, -6.520000000000006679, -11.48378591275254301 ) ) ;
#13161=CIRCLE ( 'NONE', #15689, 1.999999999999998224 ) ;
#13165=CARTESIAN_POINT ( 'NONE',  ( 7.416407864998740607, 2.746025403784439600, -10.20780970022447676 ) ) ;
#13167=EDGE_CURVE ( 'NONE', #7861, #1880, #7702, .T. ) ;
#13170=VERTEX_POINT ( 'NONE', #2751 ) ;
#13171=CARTESIAN_POINT ( 'NONE',  ( 11.76794919243112325, 11.42999999999999616, 1.734723475976807094E-15 ) ) ;
#13172=ORIENTED_EDGE ( 'NONE', *, *, #11201, .F. ) ;
#13175=CARTESIAN_POINT ( 'NONE',  ( 8.375056734751542109, 9.999950376471138824, 10.58801762894534271 ) ) ;
#13176=CARTESIAN_POINT ( 'NONE',  ( 10.92172942406178926, 0.1300000000000051115, 7.935100905948385908 ) ) ;
#13178=AXIS2_PLACEMENT_3D ( 'NONE', #9085, #14263, #4917 ) ;
#13194=ORIENTED_EDGE ( 'NONE', *, *, #1628, .T. ) ;
#13197=CARTESIAN_POINT ( 'NONE',  ( -3.636496289402152637, 6.330000000000001847, -11.19198476289190936 ) ) ;
#13200=CARTESIAN_POINT ( 'NONE',  ( 8.343458848123583849, 21.87999999999999545, -11.48378591275253768 ) ) ;
#13207=CARTESIAN_POINT ( 'NONE',  ( 4.171729424061789260, 0.8299999999999974065, 12.83926296998457239 ) ) ;
#13215=VERTEX_POINT ( 'NONE', #6763 ) ;
#13231=CARTESIAN_POINT ( 'NONE',  ( 11.76794919243112325, 17.42999999999999972, 1.734723475976807094E-15 ) ) ;
#13235=CARTESIAN_POINT ( 'NONE',  ( 13.50000000000000355, 19.58000000000001606, -4.386415899144233244 ) ) ;
#13236=ORIENTED_EDGE ( 'NONE', *, *, #8074, .T. ) ;
#13238=CARTESIAN_POINT ( 'NONE',  ( -7.272992578804307939, 27.48000000000001108, -10.01041549318726886 ) ) ;
#13242=CARTESIAN_POINT ( 'NONE',  ( -13.49999999999999822, -5.920000000000003482, 4.386415899144235908 ) ) ;
#13244=CIRCLE ( 'NONE', #5363, 1.999999999999998224 ) ;
#13247=EDGE_CURVE ( 'NONE', #6127, #3432, #14084, .T. ) ;
#13255=CARTESIAN_POINT ( 'NONE',  ( 9.520470885617715595, 14.13000000000000433, 6.917026985038135400 ) ) ;
#13257=VERTEX_POINT ( 'NONE', #4277 ) ;
#13258=CARTESIAN_POINT ( 'NONE',  ( 3.636496289402157078, 3.030000000000004690, -11.19198476289190936 ) ) ;
#13263=CARTESIAN_POINT ( 'NONE',  ( -8.549982208541774191E-16, -9.319999999999998508, 14.19474002721660355 ) ) ;
#13269=EDGE_CURVE ( 'NONE', #6231, #15652, #12687, .T. ) ;
#13283=CARTESIAN_POINT ( 'NONE',  ( -7.272992578804307939, 3.479999999999997762, -10.01041549318726886 ) ) ;
#13284=ORIENTED_EDGE ( 'NONE', *, *, #933, .T. ) ;
#13286=CARTESIAN_POINT ( 'NONE',  ( 10.92172942406178926, 24.13000000000001322, 7.935100905948385908 ) ) ;
#13293=CARTESIAN_POINT ( 'NONE',  ( 4.206197538246302159, 6.548267719634620398, 23.28534784291402104 ) ) ;
#13295=DIRECTION ( 'NONE',  ( -0.000000000000000000, 1.000000000000000000, -0.000000000000000000 ) ) ;
#13299=ORIENTED_EDGE ( 'NONE', *, *, #9339, .F. ) ;
#13302=VERTEX_POINT ( 'NONE', #16281 ) ;
#13313=AXIS2_PLACEMENT_3D ( 'NONE', #10478, #15838, #9331 ) ;
#13319=CARTESIAN_POINT ( 'NONE',  ( 19.00000000000000711, 7.773118517290098062, -1.732050807568807249 ) ) ;
#13322=CARTESIAN_POINT ( 'NONE',  ( -3.636496289402156190, -10.47000000000000064, 11.19198476289190758 ) ) ;
#13324=CARTESIAN_POINT ( 'NONE',  ( -4.171729424061787483, -9.669999999999998153, -12.83926296998457417 ) ) ;
#13335=CIRCLE ( 'NONE', #6303, 26.00000000000000355 ) ;
#13338=CARTESIAN_POINT ( 'NONE',  ( 3.636496289402154414, 1.829999999999998295, 11.19198476289190758 ) ) ;
#13342=CARTESIAN_POINT ( 'NONE',  ( 4.171729424061789260, -6.169999999999994600, 12.83926296998457239 ) ) ;
#13344=CARTESIAN_POINT ( 'NONE',  ( 15.58845726811991916, 7.773118517290098950, -10.99999999999996092 ) ) ;
#13346=DIRECTION ( 'NONE',  ( -0.8660254037844343777, 0.000000000000000000, -0.5000000000000075495 ) ) ;
#13347=( BOUNDED_CURVE ( )  B_SPLINE_CURVE ( 2, ( #1568, #2973, #2884, #7331, #12714, #601, #4500, #6987, #429, #13756, #8579, #13930, #3065 ),
 .UNSPECIFIED., .F., .F. ) 
 B_SPLINE_CURVE_WITH_KNOTS ( ( 3, 2, 2, 2, 2, 2, 3 ),
 ( 0.1673499929175705225, 0.1711054437513025994, 0.1786163454187667532, 0.1861272470862310735, 0.1936381487536952273, 0.2011490504211593811, 0.2049045012548912914 ),
 .UNSPECIFIED. ) 
 CURVE ( )  GEOMETRIC_REPRESENTATION_ITEM ( )  RATIONAL_B_SPLINE_CURVE ( ( 0.9755282581475768211, 0.9755282581475768211, 1.000000000000000000, 0.9510565162951536422, 1.000000000000000000, 0.9510565162951536422, 1.000000000000000000, 0.9510565162951536422, 1.000000000000000000, 0.9510565162951536422, 1.000000000000000000, 0.9755282581475778203, 0.9755282581475768211 ) ) 
 REPRESENTATION_ITEM ( '' )  );
#13349=CARTESIAN_POINT ( 'NONE',  ( -7.999999999999670486, 0.000000000000000000, -24.73863375370606477 ) ) ;
#13353=CARTESIAN_POINT ( 'NONE',  ( 0.000000000000000000, 0.000000000000000000, 0.000000000000000000 ) ) ;
#13354=CARTESIAN_POINT ( 'NONE',  ( -12.00000000000000178, 4.063974596215564894, -2.718289652585034772E-15 ) ) ;
#13363=ORIENTED_EDGE ( 'NONE', *, *, #17277, .T. ) ;
#13365=CARTESIAN_POINT ( 'NONE',  ( -13.49999999999999822, 25.78000000000000469, -4.386415899144240349 ) ) ;
#13368=CARTESIAN_POINT ( 'NONE',  ( -13.49999999999999822, 14.78000000000000647, -4.386415899144240349 ) ) ;
#13377=CARTESIAN_POINT ( 'NONE',  ( 1.686577221131020821, 10.00000000000000000, -13.19627548623512325 ) ) ;
#13382=ORIENTED_EDGE ( 'NONE', *, *, #15118, .F. ) ;
#13386=ADVANCED_FACE ( 'NONE', ( #16983 ), #7547, .F. ) ;
#13389=CARTESIAN_POINT ( 'NONE',  ( 7.999999999999906741, 7.815232041205461222, 17.14738331135997740 ) ) ;
#13395=B_SPLINE_CURVE_WITH_KNOTS ( 'NONE', 3,
 ( #16951, #1922, #4852, #10255 ),
 .UNSPECIFIED., .F., .F.,
 ( 4, 4 ),
 ( 2.376698214958262694E-07, 0.007646667280170310783 ),
 .UNSPECIFIED. ) ;
#13400=CARTESIAN_POINT ( 'NONE',  ( -8.549982208541774191E-16, 21.68000000000000682, 14.19474002721660355 ) ) ;
#13402=CARTESIAN_POINT ( 'NONE',  ( -5.505582777971113728, 2.022510465845309778E-14, -11.21382616413506739 ) ) ;
#13403=LINE ( 'NONE', #2519, #13688 ) ;
#13406=CARTESIAN_POINT ( 'NONE',  ( -10.00000000000014211, 0.000000000000000000, 17.32050807568869288 ) ) ;
#13407=CARTESIAN_POINT ( 'NONE',  ( 4.171729424061789260, -8.169999999999996376, 12.83926296998457239 ) ) ;
#13412=EDGE_CURVE ( 'NONE', #42, #14262, #9950, .T. ) ;
#13417=AXIS2_PLACEMENT_3D ( 'NONE', #8910, #9977, #4743 ) ;
#13421=CARTESIAN_POINT ( 'NONE',  ( -4.171729424061787483, 7.330000000000003624, -12.83926296998457417 ) ) ;
#13422=CARTESIAN_POINT ( 'NONE',  ( -11.76794919243112325, 3.930000000000002824, -2.602085213965210642E-15 ) ) ;
#13426=CARTESIAN_POINT ( 'NONE',  ( 8.343458848123578520, -12.01999999999999780, 11.48378591275254124 ) ) ;
#13429=FACE_OUTER_BOUND ( 'NONE', #7058, .T. ) ;
#13430=AXIS2_PLACEMENT_3D ( 'NONE', #13353, #4073, #16256 ) ;
#13435=CARTESIAN_POINT ( 'NONE',  ( 0.000000000000000000, 9.999999999999998224, -14.50000000000000000 ) ) ;
#13445=DIRECTION ( 'NONE',  ( -0.000000000000000000, 1.000000000000000000, -0.000000000000000000 ) ) ;
#13447=ORIENTED_EDGE ( 'NONE', *, *, #2287, .T. ) ;
#13448=ORIENTED_EDGE ( 'NONE', *, *, #2770, .F. ) ;
#13449=CARTESIAN_POINT ( 'NONE',  ( 2.621994543952811015E-15, 22.18000000000000327, -14.19474002721660355 ) ) ;
#13452=CARTESIAN_POINT ( 'NONE',  ( -13.50000000000000000, 8.929999999999992610, -3.469446951953614189E-15 ) ) ;
#13460=CARTESIAN_POINT ( 'NONE',  ( 9.708203932499419153, 8.863974596215612678, -7.053423027509713172 ) ) ;
#13461=EDGE_CURVE ( 'NONE', #2326, #2565, #15640, .T. ) ;
#13463=FACE_OUTER_BOUND ( 'NONE', #2048, .T. ) ;
#13468=ORIENTED_EDGE ( 'NONE', *, *, #2811, .T. ) ;
#13469=ORIENTED_EDGE ( 'NONE', *, *, #11479, .T. ) ;
#13471=ORIENTED_EDGE ( 'NONE', *, *, #10270, .F. ) ;
#13484=CARTESIAN_POINT ( 'NONE',  ( -9.520470885617715595, 18.63000000000000611, -6.917026985038136289 ) ) ;
#13485=CYLINDRICAL_SURFACE ( 'NONE', #16321, 26.00000000000000355 ) ;
#13487=CARTESIAN_POINT ( 'NONE',  ( 7.347880794884122694E-16, 0.000000000000000000, -18.00000000000000000 ) ) ;
#13490=CARTESIAN_POINT ( 'NONE',  ( -8.808033401071559965, -2.585303254002297467E-15, -9.216900067070168845 ) ) ;
#13493=CARTESIAN_POINT ( 'NONE',  ( -7.409984580736203970E-16, -13.32000000000000028, 12.37355403259654985 ) ) ;
#13494=CARTESIAN_POINT ( 'NONE',  ( 0.000000000000000000, 9.000000000000000000, 0.000000000000000000 ) ) ;
#13507=CARTESIAN_POINT ( 'NONE',  ( 9.520470885617717371, 5.730000000000012861, -6.917026985038131848 ) ) ;
#13511=CARTESIAN_POINT ( 'NONE',  ( 10.92172942406179104, -8.269999999999999574, -7.935100905948385908 ) ) ;
#13524=CARTESIAN_POINT ( 'NONE',  ( 10.00000000000002132, 0.000000000000000000, -15.32050807568876394 ) ) ;
#13528=CARTESIAN_POINT ( 'NONE',  ( -18.18340077413956735, 8.007813497946154158, -0.8546369493910546122 ) ) ;
#13529=ORIENTED_EDGE ( 'NONE', *, *, #8549, .F. ) ;
#13530=CARTESIAN_POINT ( 'NONE',  ( -3.708203932499370303, 4.396025403784443952, 11.41267819554184371 ) ) ;
#13532=CARTESIAN_POINT ( 'NONE',  ( -8.549982208541774191E-16, 11.67999999999999972, 14.19474002721660355 ) ) ;
#13536=EDGE_CURVE ( 'NONE', #13571, #7996, #12690, .T. ) ;
#13538=CARTESIAN_POINT ( 'NONE',  ( 8.343458848123583849, 10.88000000000001322, -11.48378591275253768 ) ) ;
#13539=CARTESIAN_POINT ( 'NONE',  ( -8.891200544363830713E-16, 7.546025403784439867, 12.00000000000000000 ) ) ;
#13545=CARTESIAN_POINT ( 'NONE',  ( 0.8552964561739553329, 8.007719221390678044, -18.18372103750114022 ) ) ;
#13549=CARTESIAN_POINT ( 'NONE',  ( 8.378362625313673817, -1.749711886770878784E-15, 10.58551083881864407 ) ) ;
#13553=DIRECTION ( 'NONE',  ( 0.000000000000000000, 0.000000000000000000, -1.000000000000000000 ) ) ;
#13558=CARTESIAN_POINT ( 'NONE',  ( 3.636496289402154414, -16.16999999999999815, 11.19198476289190758 ) ) ;
#13569=FACE_OUTER_BOUND ( 'NONE', #15101, .T. ) ;
#13571=VERTEX_POINT ( 'NONE', #10140 ) ;
#13574=ORIENTED_EDGE ( 'NONE', *, *, #13148, .T. ) ;
#13576=CARTESIAN_POINT ( 'NONE',  ( -12.44161054033546776, 4.250271015223983793E-15, -4.165684030147709827 ) ) ;
#13579=CARTESIAN_POINT ( 'NONE',  ( -7.272992578804310604, -13.62000000000000632, 10.01041549318726709 ) ) ;
#13580=DIRECTION ( 'NONE',  ( 0.000000000000000000, 0.000000000000000000, 1.000000000000000000 ) ) ;
#13581=CARTESIAN_POINT ( 'NONE',  ( -13.49999999999999822, -17.92000000000000526, 4.386415899144235908 ) ) ;
#13594=DIRECTION ( 'NONE',  ( 0.000000000000000000, -0.000000000000000000, 1.000000000000000000 ) ) ;
#13596=CARTESIAN_POINT ( 'NONE',  ( -3.636496289402152637, 0.3299999999999969624, -11.19198476289190936 ) ) ;
#13599=CARTESIAN_POINT ( 'NONE',  ( -4.171729424061787483, -16.66999999999999815, -12.83926296998457417 ) ) ;
#13600=VECTOR ( 'NONE', #13632, 1000.000000000000000 ) ;
#13601=CARTESIAN_POINT ( 'NONE',  ( -19.00000000000001776, 0.000000000000000000, 1.732050807568674466 ) ) ;
#13617=ORIENTED_EDGE ( 'NONE', *, *, #10473, .T. ) ;
#13618=CARTESIAN_POINT ( 'NONE',  ( 2.222800136090958073E-15, 3.046025403784441643, -12.00000000000000000 ) ) ;
#13624=CARTESIAN_POINT ( 'NONE',  ( -13.49999999999999822, 8.780000000000004690, -4.386415899144240349 ) ) ;
#13625=CIRCLE ( 'NONE', #6031, 1.999999999999998224 ) ;
#13626=CARTESIAN_POINT ( 'NONE',  ( -12.00000000000000178, 6.646025403784432406, -3.899036354794879422 ) ) ;
#13632=DIRECTION ( 'NONE',  ( -0.000000000000000000, -1.000000000000000000, -0.000000000000000000 ) ) ;
#13634=EDGE_CURVE ( 'NONE', #17255, #8460, #3403, .T. ) ;
#13637=CARTESIAN_POINT ( 'NONE',  ( 8.343458848123580296, 5.980000000000005755, 11.48378591275253768 ) ) ;
#13639=DIRECTION ( 'NONE',  ( -0.000000000000000000, 1.000000000000000000, -0.000000000000000000 ) ) ;
#13640=CARTESIAN_POINT ( 'NONE',  ( -9.738246541212287610, 8.018245899431759582, -15.33333167467629821 ) ) ;
#13641=ORIENTED_EDGE ( 'NONE', *, *, #15079, .T. ) ;
#13646=CARTESIAN_POINT ( 'NONE',  ( 13.50000000000000355, 0.5800000000000020695, -4.386415899144233244 ) ) ;
#13650=EDGE_CURVE ( 'NONE', #2674, #7575, #578, .T. ) ;
#13655=VERTEX_POINT ( 'NONE', #754 ) ;
#13656=CARTESIAN_POINT ( 'NONE',  ( 15.34527529650332411, 7.924527530346058057, -10.35822530491750371 ) ) ;
#13660=CARTESIAN_POINT ( 'NONE',  ( -1.271258255638932022, -3.026718717157247666E-15, -12.11055032353875305 ) ) ;
#13664=CARTESIAN_POINT ( 'NONE',  ( 10.92172942406178926, -13.87000000000000099, 7.935100905948385908 ) ) ;
#13669=CARTESIAN_POINT ( 'NONE',  ( -16.17792858571901959, 8.007293667506184320, -8.349340579021800934 ) ) ;
#13672=EDGE_CURVE ( 'NONE', #9583, #5339, #4912, .T. ) ;
#13676=CARTESIAN_POINT ( 'NONE',  ( -1.732050807568877859, 7.773118517290099838, -18.99999999999999645 ) ) ;
#13677=PLANE ( 'NONE',  #5260 ) ;
#13678=CARTESIAN_POINT ( 'NONE',  ( -1.003751346110120011E-07, 3.679997203684337137, 13.49999999999999822 ) ) ;
#13679=CARTESIAN_POINT ( 'NONE',  ( -13.50000000000000000, 32.93000000000001393, -3.469446951953614189E-15 ) ) ;
#13680=CARTESIAN_POINT ( 'NONE',  ( 2.279995255611139653E-15, -8.820000000000000284, -12.37355403259654985 ) ) ;
#13682=CARTESIAN_POINT ( 'NONE',  ( -2.138189944381240881, 2.603118577679737644, 13.49999999999999822 ) ) ;
#13688=VECTOR ( 'NONE', #14545, 1000.000000000000000 ) ;
#13690=EDGE_CURVE ( 'NONE', #9213, #14960, #12777, .T. ) ;
#13692=CARTESIAN_POINT ( 'NONE',  ( -10.92172942406178926, 4.629999999999995453, -7.935100905948389460 ) ) ;
#13693=CARTESIAN_POINT ( 'NONE',  ( -9.708203932499392508, 1.363974596215586033, 7.053423027509694521 ) ) ;
#13697=CARTESIAN_POINT ( 'NONE',  ( -18.85006967243203491, 7.815232008520037077, -1.645488492588025098 ) ) ;
#13700=DIRECTION ( 'NONE',  ( -0.8660254037844382635, 0.000000000000000000, 0.5000000000000008882 ) ) ;
#13702=CARTESIAN_POINT ( 'NONE',  ( -8.343458848123582072, 8.380000000000002558, 11.48378591275254124 ) ) ;
#13707=CIRCLE ( 'NONE', #6116, 26.00000000000000355 ) ;
#13708=CARTESIAN_POINT ( 'NONE',  ( 8.343458848123578520, 6.980000000000003979, 11.48378591275254124 ) ) ;
#13716=DIRECTION ( 'NONE',  ( 0.000000000000000000, 1.000000000000000000, 0.000000000000000000 ) ) ;
#13717=CARTESIAN_POINT ( 'NONE',  ( 1.645540471734042054, 7.815206720109964422, -18.85015970295421894 ) ) ;
#13719=CARTESIAN_POINT ( 'NONE',  ( -11.49634864345504148, 10.00000000000000711, -4.013552247486381397 ) ) ;
#13725=ORIENTED_EDGE ( 'NONE', *, *, #7415, .T. ) ;
#13728=EDGE_LOOP ( 'NONE', ( #13641, #13111, #15522, #9243 ) ) ;
#13729=CARTESIAN_POINT ( 'NONE',  ( 9.520470885617715595, -15.86999999999999567, 6.917026985038135400 ) ) ;
#13732=CARTESIAN_POINT ( 'NONE',  ( -10.18076046065006146, 7.956441901775577641, 15.32106749056508299 ) ) ;
#13740=ORIENTED_EDGE ( 'NONE', *, *, #13690, .T. ) ;
#13742=ORIENTED_EDGE ( 'NONE', *, *, #1488, .T. ) ;
#13744=CARTESIAN_POINT ( 'NONE',  ( -10.35198169125275847, 7.925746654722171769, -15.34401010674823240 ) ) ;
#13749=CARTESIAN_POINT ( 'NONE',  ( 6.750017152462248760, -20.07073847365936814, 11.69133304809444773 ) ) ;
#13754=CARTESIAN_POINT ( 'NONE',  ( -15.34492079894883965, 7.924935932049796072, -10.35602470258078789 ) ) ;
#13756=CARTESIAN_POINT ( 'NONE',  ( 7.416407864998753041, 2.113974596215577595, 10.20780970022449985 ) ) ;
#13761=CARTESIAN_POINT ( 'NONE',  ( 17.32050807568873552, 7.773118517290098062, 8.000000000000083489 ) ) ;
#13762=CARTESIAN_POINT ( 'NONE',  ( 7.347880794884122694E-16, 0.000000000000000000, -20.00000000000000000 ) ) ;
#13764=CARTESIAN_POINT ( 'NONE',  ( -7.272992578804307939, -8.520000000000001350, -10.01041549318726886 ) ) ;
#13771=CIRCLE ( 'NONE', #4762, 26.00000000000000355 ) ;
#13777=CARTESIAN_POINT ( 'NONE',  ( -12.00000000000002842, 1.213974596215577906, 3.899036354794884307 ) ) ;
#13782=AXIS2_PLACEMENT_3D ( 'NONE', #5706, #13716, #9686 ) ;
#13783=CARTESIAN_POINT ( 'NONE',  ( 2.279995255611139653E-15, 21.17999999999998906, -12.37355403259654985 ) ) ;
#13784=ORIENTED_EDGE ( 'NONE', *, *, #17109, .T. ) ;
#13788=CARTESIAN_POINT ( 'NONE',  ( 4.171729424061789260, 5.830000000000001847, 12.83926296998457239 ) ) ;
#13789=ORIENTED_EDGE ( 'NONE', *, *, #14312, .T. ) ;
#13793=CARTESIAN_POINT ( 'NONE',  ( 2.621994543952811015E-15, 5.180000000000002380, -14.19474002721660355 ) ) ;
#13794=EDGE_CURVE ( 'NONE', #2328, #3933, #1459, .T. ) ;
#13803=DIRECTION ( 'NONE',  ( -0.000000000000000000, -1.000000000000000000, -0.000000000000000000 ) ) ;
#13810=CARTESIAN_POINT ( 'NONE',  ( -15.58845726811976817, 0.000000000000000000, -11.00000000000018296 ) ) ;
#13812=ORIENTED_EDGE ( 'NONE', *, *, #11260, .F. ) ;
#13814=VERTEX_POINT ( 'NONE', #1973 ) ;
#13817=CARTESIAN_POINT ( 'NONE',  ( 2.445080149700053643E-15, 4.180000000000004157, -13.50000000000000000 ) ) ;
#13823=EDGE_CURVE ( 'NONE', #2328, #7389, #6328, .T. ) ;
#13825=ORIENTED_EDGE ( 'NONE', *, *, #5848, .F. ) ;
#13826=CARTESIAN_POINT ( 'NONE',  ( 16.17460542229563814, 8.007813505529846054, -8.351563113033689589 ) ) ;
#13829=ORIENTED_EDGE ( 'NONE', *, *, #3626, .F. ) ;
#13832=AXIS2_PLACEMENT_3D ( 'NONE', #3126, #15137, #3034 ) ;
#13835=CARTESIAN_POINT ( 'NONE',  ( 10.92172942406179104, -19.27000000000000313, -7.935100905948385908 ) ) ;
#13841=CARTESIAN_POINT ( 'NONE',  ( 3.636496289402157078, -5.969999999999996199, -11.19198476289190936 ) ) ;
#13844=DIRECTION ( 'NONE',  ( 1.426480712616743416E-14, 0.000000000000000000, -1.000000000000000000 ) ) ;
#13849=DIRECTION ( 'NONE',  ( -0.000000000000000000, 1.000000000000000000, -0.000000000000000000 ) ) ;
#13850=CARTESIAN_POINT ( 'NONE',  ( -13.49999999999999822, 30.07999999999999829, 4.386415899144235908 ) ) ;
#13851=CARTESIAN_POINT ( 'NONE',  ( -9.520470885617717371, -7.769999999999999574, 6.917026985038133624 ) ) ;
#13853=CARTESIAN_POINT ( 'NONE',  ( 9.708203932499371192, 5.863974596215575374, -7.053423027509676757 ) ) ;
#13860=CYLINDRICAL_SURFACE ( 'NONE', #1094, 1.999999999999998224 ) ;
#13869=CARTESIAN_POINT ( 'NONE',  ( 11.76794919243112325, 20.43000000000000327, 1.734723475976807094E-15 ) ) ;
#13872=DIRECTION ( 'NONE',  ( 0.5000000000000007772, 0.000000000000000000, 0.8660254037844381525 ) ) ;
#13874=CARTESIAN_POINT ( 'NONE',  ( 13.50000000000000355, 6.580000000000001847, -4.386415899144233244 ) ) ;
#13877=DIRECTION ( 'NONE',  ( -0.000000000000000000, 1.000000000000000000, -0.000000000000000000 ) ) ;
#13878=CARTESIAN_POINT ( 'NONE',  ( -10.92172942406178926, 5.629999999999996341, -7.935100905948389460 ) ) ;
#13885=VECTOR ( 'NONE', #3573, 1000.000000000000000 ) ;
#13889=( NAMED_UNIT ( * ) PLANE_ANGLE_UNIT ( ) SI_UNIT ( $, .RADIAN. ) );
#13894=DIRECTION ( 'NONE',  ( -0.4999999999999882316, 0.000000000000000000, -0.8660254037844454800 ) ) ;
#13896=CARTESIAN_POINT ( 'NONE',  ( 2.279995255611139653E-15, 24.17999999999999261, -12.37355403259654985 ) ) ;
#13901=CARTESIAN_POINT ( 'NONE',  ( 7.272992578804308828, -16.02000000000000313, 10.01041549318726709 ) ) ;
#13906=( BOUNDED_CURVE ( )  B_SPLINE_CURVE ( 2, ( #13175, #6560, #17321, #1232, #16244 ),
 .UNSPECIFIED., .F., .F. ) 
 B_SPLINE_CURVE_WITH_KNOTS ( ( 3, 2, 3 ),
 ( 0.4326563348871274028, 0.4358520785730354841, 0.4386822870511441486 ),
 .UNSPECIFIED. ) 
 CURVE ( )  GEOMETRIC_REPRESENTATION_ITEM ( )  RATIONAL_B_SPLINE_CURVE ( ( 0.9759364712373530537, 0.9723676117969409782, 1.000000000000000000, 0.9755282566284837475, 0.9755282581475768211 ) ) 
 REPRESENTATION_ITEM ( '' )  );
#13910=EDGE_CURVE ( 'NONE', #5991, #11898, #9342, .T. ) ;
#13912=ORIENTED_EDGE ( 'NONE', *, *, #16694, .T. ) ;
#13915=CARTESIAN_POINT ( 'NONE',  ( 13.50000000000000355, 9.580000000000008953, -4.386415899144233244 ) ) ;
#13922=CARTESIAN_POINT ( 'NONE',  ( -11.76794919243112325, 27.93000000000001037, -2.602085213965210642E-15 ) ) ;
#13927=CARTESIAN_POINT ( 'NONE',  ( -16.97734196418681307, 7.854010772509913529, -8.022095340454654888 ) ) ;
#13928=CARTESIAN_POINT ( 'NONE',  ( 2.279995255611139653E-15, 0.1800000000000001044, -12.37355403259654985 ) ) ;
#13930=CARTESIAN_POINT ( 'NONE',  ( 1.900613283894512451, 1.890856018535849392, 12.00000000000000000 ) ) ;
#13934=CARTESIAN_POINT ( 'NONE',  ( -1.732050807569007977, 0.000000000000000000, 18.99999999999998224 ) ) ;
#13935=DIRECTION ( 'NONE',  ( 4.676985943005715098E-16, -0.000000000000000000, 1.000000000000000000 ) ) ;
#13937=DIRECTION ( 'NONE',  ( 0.000000000000000000, 0.000000000000000000, 1.000000000000000000 ) ) ;
#13939=CARTESIAN_POINT ( 'NONE',  ( -11.76794919243112325, -8.220000000000004192, -3.823638476888998827 ) ) ;
#13941=CARTESIAN_POINT ( 'NONE',  ( -13.49999999999999822, 1.780000000000000471, -4.386415899144240349 ) ) ;
#13945=DIRECTION ( 'NONE',  ( 1.000000000000000000, 0.000000000000000000, 0.000000000000000000 ) ) ;
#13950=DIRECTION ( 'NONE',  ( -0.000000000000000000, 1.000000000000000000, -0.000000000000000000 ) ) ;
#13956=CARTESIAN_POINT ( 'NONE',  ( 3.636496289402154414, 22.83000000000001606, 11.19198476289190758 ) ) ;
#13961=CARTESIAN_POINT ( 'NONE',  ( -10.92172942406179104, 8.230000000000014637, 7.935100905948385908 ) ) ;
#13965=CARTESIAN_POINT ( 'NONE',  ( 4.171729424061789260, 0.8299999999999974065, 12.83926296998457239 ) ) ;
#13985=ORIENTED_EDGE ( 'NONE', *, *, #6292, .F. ) ;
#13986=CARTESIAN_POINT ( 'NONE',  ( 7.272992578804311492, -18.12000000000000455, -10.01041549318726709 ) ) ;
#13993=VECTOR ( 'NONE', #3638, 999.9999999999998863 ) ;
#13998=CARTESIAN_POINT ( 'NONE',  ( 7.272992578804311492, 14.88000000000000078, -10.01041549318726709 ) ) ;
#14001=ORIENTED_EDGE ( 'NONE', *, *, #9656, .T. ) ;
#14002=CARTESIAN_POINT ( 'NONE',  ( -2.734444271416374426E-11, 0.3139745962166686222, -12.00000000000000000 ) ) ;
#14008=DIRECTION ( 'NONE',  ( -0.000000000000000000, -1.000000000000000000, -0.000000000000000000 ) ) ;
#14011=CARTESIAN_POINT ( 'NONE',  ( 11.76794919243112325, 32.43000000000001393, 1.734723475976807094E-15 ) ) ;
#14017=CARTESIAN_POINT ( 'NONE',  ( -3.636496289402152637, -14.66999999999999638, -11.19198476289190936 ) ) ;
#14021=CARTESIAN_POINT ( 'NONE',  ( -3.636496289402152637, -5.669999999999994600, -11.19198476289190936 ) ) ;
#14024=CARTESIAN_POINT ( 'NONE',  ( 19.29752010712840615, 5.918584287042170544, 17.42428528562864898 ) ) ;
#14028=CARTESIAN_POINT ( 'NONE',  ( -1.297534681090767750, 7.924607901204613114, -18.46823281779982295 ) ) ;
#14029=DIRECTION ( 'NONE',  ( -0.000000000000000000, 1.000000000000000000, -0.000000000000000000 ) ) ;
#14031=CARTESIAN_POINT ( 'NONE',  ( -8.343458848123576743, 29.48000000000000753, -11.48378591275254301 ) ) ;
#14032=CARTESIAN_POINT ( 'NONE',  ( 9.520470885617717371, -9.269999999999999574, -6.917026985038131848 ) ) ;
#14035=CARTESIAN_POINT ( 'NONE',  ( 19.29752010712840615, 0.000000000000000000, 17.42428528562864898 ) ) ;
#14038=CARTESIAN_POINT ( 'NONE',  ( 10.92172942406178926, 3.129999999999993676, 7.935100905948385908 ) ) ;
#14049=CARTESIAN_POINT ( 'NONE',  ( 11.76794919243112680, 17.57999999999999829, -3.823638476888993942 ) ) ;
#14050=ADVANCED_FACE ( 'NONE', ( #13463 ), #7836, .F. ) ;
#14051=ORIENTED_EDGE ( 'NONE', *, *, #16787, .T. ) ;
#14055=CARTESIAN_POINT ( 'NONE',  ( -10.92172942406178926, 4.629999999999995453, -7.935100905948389460 ) ) ;
#14056=CARTESIAN_POINT ( 'NONE',  ( 11.76794919243112680, 32.58000000000001251, -3.823638476888993942 ) ) ;
#14058=AXIS2_PLACEMENT_3D ( 'NONE', #10320, #12960, #7495 ) ;
#14059=CARTESIAN_POINT ( 'NONE',  ( 10.92172942406179104, 4.730000000000011973, -7.935100905948385908 ) ) ;
#14068=( NAMED_UNIT ( * ) SI_UNIT ( $, .STERADIAN. ) SOLID_ANGLE_UNIT ( ) );
#14075=ORIENTED_EDGE ( 'NONE', *, *, #10937, .F. ) ;
#14078=CARTESIAN_POINT ( 'NONE',  ( -5.491332954668864730, -19.60957387106639516, 16.75890910139807843 ) ) ;
#14081=VECTOR ( 'NONE', #9253, 1000.000000000000000 ) ;
#14083=CARTESIAN_POINT ( 'NONE',  ( 11.68790604918427789, -2.350847233825327770E-15, -4.414367548897630833 ) ) ;
#14084=B_SPLINE_CURVE_WITH_KNOTS ( 'NONE', 3,
 ( #11090, #5792, #4097, #8184, #13545, #12231, #387, #1701, #13717, #11177 ),
 .UNSPECIFIED., .F., .F.,
 ( 4, 2, 2, 2, 4 ),
 ( 0.002109865028651171977, 0.002636639667304636111, 0.003163414305958100244, 0.003690188944611564378, 0.004216963583265028945 ),
 .UNSPECIFIED. ) ;
#14086=DIRECTION ( 'NONE',  ( 0.000000000000000000, 0.000000000000000000, 1.000000000000000000 ) ) ;
#14090=ORIENTED_EDGE ( 'NONE', *, *, #595, .T. ) ;
#14092=EDGE_CURVE ( 'NONE', #546, #14477, #15846, .T. ) ;
#14094=CARTESIAN_POINT ( 'NONE',  ( 10.92172942406178926, 9.129999999999999005, 7.935100905948385908 ) ) ;
#14099=CARTESIAN_POINT ( 'NONE',  ( 16.64312382832869730, 7.924527542031523097, 8.110285629053034739 ) ) ;
#14100=DIRECTION ( 'NONE',  ( -0.000000000000000000, 1.000000000000000000, -0.000000000000000000 ) ) ;
#14102=CARTESIAN_POINT ( 'NONE',  ( 2.279995255611139653E-15, 27.18000000000000682, -12.37355403259654985 ) ) ;
#14105=B_SPLINE_CURVE_WITH_KNOTS ( 'NONE', 3,
 ( #150, #5556, #10940, #13656, #15059, #4391, #5732, #1639, #1726, #9801, #15147, #3045, #13826, #1809, #839, #17015, #7578, #3495 ),
 .UNSPECIFIED., .F., .F.,
 ( 4, 2, 2, 2, 2, 2, 2, 2, 4 ),
 ( 2.344180274388505431E-07, 0.0005273255548235199555, 0.001054416691619601077, 0.001581507828415682198, 0.002108598965211763536, 0.002635690102007839236, 0.003162781238803915370, 0.003689872375599991070, 0.004216963512396067204 ),
 .UNSPECIFIED. ) ;
#14107=CARTESIAN_POINT ( 'NONE',  ( 7.272992578804311492, -15.12000000000000277, -10.01041549318726709 ) ) ;
#14112=CARTESIAN_POINT ( 'NONE',  ( -4.171729424061787483, 4.330000000000000071, -12.83926296998457417 ) ) ;
#14117=CARTESIAN_POINT ( 'NONE',  ( 9.110082863707074097, 8.062255781930765863, -15.52458835467165699 ) ) ;
#14121=CARTESIAN_POINT ( 'NONE',  ( -19.79706521687757359, 7.170682760640493925, -8.000000000000232703 ) ) ;
#14136=CARTESIAN_POINT ( 'NONE',  ( -11.76794919243112325, 21.77999999999999758, -3.823638476888998827 ) ) ;
#14141=CARTESIAN_POINT ( 'NONE',  ( -4.171729424061791036, 2.530000000000004690, 12.83926296998457239 ) ) ;
#14142=CARTESIAN_POINT ( 'NONE',  ( 9.520470885617715595, 32.13000000000001677, 6.917026985038135400 ) ) ;
#14146=DIRECTION ( 'NONE',  ( -0.000000000000000000, -1.000000000000000000, -0.000000000000000000 ) ) ;
#14149=EDGE_CURVE ( 'NONE', #10231, #5098, #4366, .T. ) ;
#14153=CARTESIAN_POINT ( 'NONE',  ( -9.708203932499367639, 6.763974596215558854, -7.053423027509681198 ) ) ;
#14158=DIRECTION ( 'NONE',  ( 0.5000000000000035527, 0.000000000000000000, -0.8660254037844365982 ) ) ;
#14160=VERTEX_POINT ( 'NONE', #7201 ) ;
#14164=CARTESIAN_POINT ( 'NONE',  ( 8.343458848123583849, 33.87999999999999545, -11.48378591275253768 ) ) ;
#14167=AXIS2_PLACEMENT_3D ( 'NONE', #8728, #920, #14086 ) ;
#14179=ORIENTED_EDGE ( 'NONE', *, *, #3751, .T. ) ;
#14180=CARTESIAN_POINT ( 'NONE',  ( 8.378360550312208943, 10.00007452681958497, 10.58551248116806498 ) ) ;
#14184=DIRECTION ( 'NONE',  ( -0.000000000000000000, 1.000000000000000000, -0.000000000000000000 ) ) ;
#14186=CARTESIAN_POINT ( 'NONE',  ( 15.43494339453338426, 7.854708401161940579, 10.68872673103595794 ) ) ;
#14187=CARTESIAN_POINT ( 'NONE',  ( -8.343458848123582072, 6.380000000000007887, 11.48378591275253768 ) ) ;
#14190=CARTESIAN_POINT ( 'NONE',  ( -7.409984580736203970E-16, 28.67999999999999972, 12.37355403259654985 ) ) ;
#14193=VECTOR ( 'NONE', #5651, 1000.000000000000000 ) ;
#14194=EDGE_CURVE ( 'NONE', #3134, #2050, #805, .T. ) ;
#14196=CARTESIAN_POINT ( 'NONE',  ( 18.02297152527631141, 8.055324227812098670, 0.3502263562676400377 ) ) ;
#14203=CARTESIAN_POINT ( 'NONE',  ( -2.138189944381320373, 2.256881422320268893, -13.49999999999997335 ) ) ;
#14205=CARTESIAN_POINT ( 'NONE',  ( 0.000000000000000000, 9.000000000000000000, -14.50000000000000000 ) ) ;
#14215=DIRECTION ( 'NONE',  ( 0.8660254037844413721, 0.000000000000000000, -0.4999999999999953926 ) ) ;
#14220=CARTESIAN_POINT ( 'NONE',  ( 9.520470885617717371, 11.73000000000000398, -6.917026985038131848 ) ) ;
#14221=CYLINDRICAL_SURFACE ( 'NONE', #10902, 13.50000000000000000 ) ;
#14226=CARTESIAN_POINT ( 'NONE',  ( -8.343458848123576743, -1.519999999999997131, -11.48378591275254301 ) ) ;
#14227=CARTESIAN_POINT ( 'NONE',  ( -9.520470885617715595, 30.63000000000001677, -6.917026985038136289 ) ) ;
#14231=CARTESIAN_POINT ( 'NONE',  ( 1.732050807568875195, 0.000000000000000000, -19.00000000000000000 ) ) ;
#14233=EDGE_CURVE ( 'NONE', #1687, #13257, #2645, .T. ) ;
#14237=DIRECTION ( 'NONE',  ( 0.000000000000000000, -1.000000000000000000, 0.000000000000000000 ) ) ;
#14240=CARTESIAN_POINT ( 'NONE',  ( 17.42428528562844292, 0.000000000000000000, 19.29752010712858024 ) ) ;
#14242=CARTESIAN_POINT ( 'NONE',  ( 19.79695994079629529, 7.170708369609773314, -7.999999999999952927 ) ) ;
#14247=ORIENTED_EDGE ( 'NONE', *, *, #6336, .F. ) ;
#14248=CARTESIAN_POINT ( 'NONE',  ( -3.636496289402152637, -17.66999999999999815, -11.19198476289190936 ) ) ;
#14254=CARTESIAN_POINT ( 'NONE',  ( 10.98232607281872397, -2.350847233825325403E-15, -5.687886418642680297 ) ) ;
#14255=CARTESIAN_POINT ( 'NONE',  ( 2.138189944381158725, 2.103118577679734091, -13.50000000000002487 ) ) ;
#14259=CIRCLE ( 'NONE', #12594, 26.00000000000000355 ) ;
#14262=VERTEX_POINT ( 'NONE', #3088 ) ;
#14263=DIRECTION ( 'NONE',  ( 0.000000000000000000, 1.000000000000000000, 0.000000000000000000 ) ) ;
#14266=B_SPLINE_CURVE_WITH_KNOTS ( 'NONE', 3,
 ( #3129, #16655, #7216, #12603, #11369, #15491, #664, #7483, #12864, #2400 ),
 .UNSPECIFIED., .F., .F.,
 ( 4, 2, 2, 2, 4 ),
 ( 0.002109865028651037970, 0.002636639667304533328, 0.003163414305958029121, 0.003690188944611524913, 0.004216963583265020271 ),
 .UNSPECIFIED. ) ;
#14281=DIRECTION ( 'NONE',  ( 0.000000000000000000, 0.000000000000000000, -1.000000000000000000 ) ) ;
#14283=AXIS2_PLACEMENT_3D ( 'NONE', #8908, #3407, #2152 ) ;
#14289=CARTESIAN_POINT ( 'NONE',  ( 7.312260103668256263E-16, 8.062177826491094379, -18.00000000000000000 ) ) ;
#14294=CARTESIAN_POINT ( 'NONE',  ( 13.50000000000000000, 3.430000000000016591, 1.734723475976807094E-15 ) ) ;
#14305=VERTEX_POINT ( 'NONE', #5506 ) ;
#14306=CARTESIAN_POINT ( 'NONE',  ( -7.272992578804310604, 10.37999999999999901, 10.01041549318726709 ) ) ;
#14311=CARTESIAN_POINT ( 'NONE',  ( 4.171729424061789260, -3.169999999999999041, 12.83926296998457239 ) ) ;
#14312=EDGE_CURVE ( 'NONE', #8209, #9086, #8159, .T. ) ;
#14317=CARTESIAN_POINT ( 'NONE',  ( 8.343458848123580296, 6.980000000000003979, 11.48378591275253768 ) ) ;
#14321=CARTESIAN_POINT ( 'NONE',  ( -19.00000000000001776, 0.000000000000000000, 1.732050807568674466 ) ) ;
#14325=CARTESIAN_POINT ( 'NONE',  ( 1.732050807568875195, 0.000000000000000000, -19.00000000000000000 ) ) ;
#14328=ORIENTED_EDGE ( 'NONE', *, *, #14586, .T. ) ;
#14330=CARTESIAN_POINT ( 'NONE',  ( -7.272992578804307939, 6.480000000000004867, -10.01041549318726886 ) ) ;
#14333=CARTESIAN_POINT ( 'NONE',  ( 5.883994266285501595, -19.07073825016061974, 10.19133159454443494 ) ) ;
#14339=CARTESIAN_POINT ( 'NONE',  ( 12.65542566923570256, 2.367644581053836045E-15, 2.676565841787903466 ) ) ;
#14340=CARTESIAN_POINT ( 'NONE',  ( 13.49999999999999822, 1.279999999999994476, 4.386415899144236796 ) ) ;
#14347=ORIENTED_EDGE ( 'NONE', *, *, #17408, .F. ) ;
#14350=CARTESIAN_POINT ( 'NONE',  ( -13.49999999999999822, 17.08000000000000540, 4.386415899144235908 ) ) ;
#14359=CARTESIAN_POINT ( 'NONE',  ( 18.11581985354938595, 8.027799059190092734, -0.6932941240386443216 ) ) ;
#14370=DIRECTION ( 'NONE',  ( 0.000000000000000000, 0.000000000000000000, -1.000000000000000000 ) ) ;
#14374=PLANE ( 'NONE',  #7403 ) ;
#14376=CARTESIAN_POINT ( 'NONE',  ( 10.92172942406179104, 1.730000000000009308, -7.935100905948385908 ) ) ;
#14390=CARTESIAN_POINT ( 'NONE',  ( 9.520470885617717371, 14.72999999999999332, -6.917026985038131848 ) ) ;
#14391=ORIENTED_EDGE ( 'NONE', *, *, #8898, .F. ) ;
#14402=EDGE_CURVE ( 'NONE', #15651, #16949, #16527, .T. ) ;
#14411=CARTESIAN_POINT ( 'NONE',  ( 17.32050807568878170, 7.773118517290099838, -7.999999999999961808 ) ) ;
#14413=ORIENTED_EDGE ( 'NONE', *, *, #14233, .F. ) ;
#14416=CARTESIAN_POINT ( 'NONE',  ( 7.272992578804308828, 7.980000000000000426, 10.01041549318726709 ) ) ;
#14417=ORIENTED_EDGE ( 'NONE', *, *, #2770, .T. ) ;
#14420=CARTESIAN_POINT ( 'NONE',  ( -4.171729424061791036, 26.52999999999999758, 12.83926296998457239 ) ) ;
#14426=AXIS2_PLACEMENT_3D ( 'NONE', #16095, #8089, #15678 ) ;
#14427=DIRECTION ( 'NONE',  ( 0.000000000000000000, 0.000000000000000000, 1.000000000000000000 ) ) ;
#14428=ADVANCED_FACE ( 'NONE', ( #15620 ), #12563, .F. ) ;
#14432=DIRECTION ( 'NONE',  ( 0.000000000000000000, 0.000000000000000000, 1.000000000000000000 ) ) ;
#14436=ORIENTED_EDGE ( 'NONE', *, *, #11600, .F. ) ;
#14440=CARTESIAN_POINT ( 'NONE',  ( 4.171729424061789260, 14.83000000000000895, 12.83926296998457239 ) ) ;
#14444=FACE_BOUND ( 'NONE', #10361, .T. ) ;
#14454=CARTESIAN_POINT ( 'NONE',  ( -3.636496289402156190, 19.53000000000001890, 11.19198476289190758 ) ) ;
#14459=VERTEX_POINT ( 'NONE', #7527 ) ;
#14460=CARTESIAN_POINT ( 'NONE',  ( -8.891200544363830713E-16, 2.680000000000005045, 13.49999999999999822 ) ) ;
#14464=CARTESIAN_POINT ( 'NONE',  ( -10.92172942406179104, -8.769999999999999574, 7.935100905948385908 ) ) ;
#14477=VERTEX_POINT ( 'NONE', #1848 ) ;
#14478=CARTESIAN_POINT ( 'NONE',  ( 9.520470885617717371, 8.730000000000014637, -6.917026985038131848 ) ) ;
#14479=ORIENTED_EDGE ( 'NONE', *, *, #11296, .T. ) ;
#14482=DIRECTION ( 'NONE',  ( 0.000000000000000000, 0.000000000000000000, 1.000000000000000000 ) ) ;
#14483=CARTESIAN_POINT ( 'NONE',  ( 8.343458848123578520, -3.020000000000000462, 11.48378591275254124 ) ) ;
#14488=CARTESIAN_POINT ( 'NONE',  ( -1.363343349470708815E-11, 9.313974596216114676, -12.00000000000000355 ) ) ;
#14492=LINE ( 'NONE', #14321, #13993 ) ;
#14503=AXIS2_PLACEMENT_3D ( 'NONE', #4284, #7040, #12328 ) ;
#14504=EDGE_LOOP ( 'NONE', ( #14523, #5340, #16472, #3094 ) ) ;
#14505=CARTESIAN_POINT ( 'NONE',  ( -13.49999999999999822, 23.08000000000000185, 4.386415899144235908 ) ) ;
#14513=CARTESIAN_POINT ( 'NONE',  ( 2.970370385949144154, 7.170662809914420066, 21.14483242576215716 ) ) ;
#14523=ORIENTED_EDGE ( 'NONE', *, *, #12638, .T. ) ;
#14524=CARTESIAN_POINT ( 'NONE',  ( 13.50000000000000355, 12.58000000000000007, -4.386415899144233244 ) ) ;
#14527=ADVANCED_FACE ( 'NONE', ( #449 ), #5859, .F. ) ;
#14537=CARTESIAN_POINT ( 'NONE',  ( -11.76794919243112325, 18.93000000000000327, -2.602085213965210642E-15 ) ) ;
#14543=CARTESIAN_POINT ( 'NONE',  ( 0.000000000000000000, 9.000000000000000000, 0.000000000000000000 ) ) ;
#14545=DIRECTION ( 'NONE',  ( -0.000000000000000000, 1.000000000000000000, -0.000000000000000000 ) ) ;
#14547=CARTESIAN_POINT ( 'NONE',  ( 9.520470885617717371, 29.73000000000000753, -6.917026985038131848 ) ) ;
#14551=CARTESIAN_POINT ( 'NONE',  ( 8.343458848123583849, -7.120000000000008988, -11.48378591275253768 ) ) ;
#14556=CIRCLE ( 'NONE', #1035, 1.999999999999998224 ) ;
#14563=CARTESIAN_POINT ( 'NONE',  ( 3.636496289402154414, 13.83000000000000895, 11.19198476289190758 ) ) ;
#14565=ORIENTED_EDGE ( 'NONE', *, *, #16269, .F. ) ;
#14566=CARTESIAN_POINT ( 'NONE',  ( -13.50000000000000000, 7.930000000000006821, -3.469446951953614189E-15 ) ) ;
#14567=CARTESIAN_POINT ( 'NONE',  ( -7.272992578804307939, 12.48000000000000576, -10.01041549318726886 ) ) ;
#14568=VERTEX_POINT ( 'NONE', #6201 ) ;
#14571=CARTESIAN_POINT ( 'NONE',  ( 8.000000000000019540, 5.918584287042170544, -24.73863375370596174 ) ) ;
#14572=CARTESIAN_POINT ( 'NONE',  ( 4.171729424061791924, -7.969999999999997975, -12.83926296998457239 ) ) ;
#14578=( BOUNDED_CURVE ( )  B_SPLINE_CURVE ( 2, ( #4507, #10171, #11309, #9914, #1831, #15606, #6106, #8847, #10087, #16947, #16862, #14203, #3514 ),
 .UNSPECIFIED., .F., .F. ) 
 B_SPLINE_CURVE_WITH_KNOTS ( ( 3, 2, 2, 2, 2, 2, 3 ),
 ( 0.5518906191050926280, 0.5547208272747723434, 0.5603812438796170747, 0.5660416604844616950, 0.5717020770893063153, 0.5773624936941509356, 0.5801927019965731347 ),
 .UNSPECIFIED. ) 
 CURVE ( )  GEOMETRIC_REPRESENTATION_ITEM ( )  RATIONAL_B_SPLINE_CURVE ( ( 0.9755282581475768211, 0.9755282592953513632, 1.000000000000000000, 0.9510565162951535312, 1.000000000000000000, 0.9510565162951535312, 1.000000000000000000, 0.9510565162951535312, 1.000000000000000000, 0.9510565162951535312, 1.000000000000000000, 0.9755282581475777093, 0.9755282581475767101 ) ) 
 REPRESENTATION_ITEM ( '' )  );
#14580=CARTESIAN_POINT ( 'NONE',  ( 17.32050807568873552, 0.000000000000000000, 8.000000000000085265 ) ) ;
#14586=EDGE_CURVE ( 'NONE', #10383, #17140, #15535, .T. ) ;
#14595=CARTESIAN_POINT ( 'NONE',  ( 9.520470885617717371, 5.730000000000012861, -6.917026985038131848 ) ) ;
#14598=CARTESIAN_POINT ( 'NONE',  ( -8.343458848123576743, 22.48000000000000753, -11.48378591275254301 ) ) ;
#14605=DIRECTION ( 'NONE',  ( -0.000000000000000000, -1.000000000000000000, -0.000000000000000000 ) ) ;
#14619=VECTOR ( 'NONE', #4671, 1000.000000000000000 ) ;
#14627=CARTESIAN_POINT ( 'NONE',  ( 3.636496289402154414, 16.83000000000001251, 11.19198476289190758 ) ) ;
#14631=CARTESIAN_POINT ( 'NONE',  ( -8.343458848123576743, 20.47999999999999687, -11.48378591275254301 ) ) ;
#14634=CARTESIAN_POINT ( 'NONE',  ( -3.636496289402152637, 27.32999999999999474, -11.19198476289190936 ) ) ;
#14636=DIRECTION ( 'NONE',  ( 6.313931023057710304E-15, 0.000000000000000000, -1.000000000000000000 ) ) ;
#14638=B_SPLINE_CURVE_WITH_KNOTS ( 'NONE', 3,
 ( #3326, #8741, #1983, #14099, #17019, #3415, #7409, #6089, #12791, #677, #11469, #16845, #8828, #7671, #4923, #14186, #8914, #11555 ),
 .UNSPECIFIED., .F., .F.,
 ( 4, 2, 2, 2, 2, 2, 2, 2, 4 ),
 ( 2.030049010680398490E-07, 0.0005272941439305970247, 0.001054385282960126164, 0.001581476421989655087, 0.002108567561019184227, 0.002635658700048713367, 0.003162749839078242073, 0.003689840978107771213, 0.004216932117137300352 ),
 .UNSPECIFIED. ) ;
#14640=AXIS2_PLACEMENT_3D ( 'NONE', #15518, #11400, #8846 ) ;
#14650=CARTESIAN_POINT ( 'NONE',  ( 7.272992578804308828, 10.98000000000000576, 10.01041549318726709 ) ) ;
#14653=CARTESIAN_POINT ( 'NONE',  ( -7.272992578804307939, 6.480000000000004867, -10.01041549318726886 ) ) ;
#14657=CARTESIAN_POINT ( 'NONE',  ( 10.92172942406179104, -11.26999999999999602, -7.935100905948385908 ) ) ;
#14674=ORIENTED_EDGE ( 'NONE', *, *, #3581, .T. ) ;
#14676=DIRECTION ( 'NONE',  ( 0.000000000000000000, 0.000000000000000000, -1.000000000000000000 ) ) ;
#14677=CARTESIAN_POINT ( 'NONE',  ( -11.76794919243112325, 7.080000000000000959, 3.823638476888994386 ) ) ;
#14679=EDGE_LOOP ( 'NONE', ( #15717, #11742, #10724, #7268 ) ) ;
#14680=CARTESIAN_POINT ( 'NONE',  ( 4.171729424061791924, 19.03000000000001890, -12.83926296998457239 ) ) ;
#14682=CARTESIAN_POINT ( 'NONE',  ( -10.92172942406179104, 15.22999999999999332, 7.935100905948385908 ) ) ;
#14685=B_SPLINE_CURVE_WITH_KNOTS ( 'NONE', 3,
 ( #4936, #7509, #7428, #2344, #13062, #10336 ),
 .UNSPECIFIED., .F., .F.,
 ( 4, 2, 4 ),
 ( 0.003156405538531764036, 0.003686668827834532411, 0.004216932117137300352 ),
 .UNSPECIFIED. ) ;
#14690=CARTESIAN_POINT ( 'NONE',  ( 1.732050807568875195, 0.000000000000000000, -19.00000000000000000 ) ) ;
#14691=CARTESIAN_POINT ( 'NONE',  ( 4.063219964874296153, 10.00000000000000000, -12.84931952050321868 ) ) ;
#14697=VERTEX_POINT ( 'NONE', #3528 ) ;
#14701=CARTESIAN_POINT ( 'NONE',  ( 9.154805866618415777, 8.062143943920768052, 15.49921147158547186 ) ) ;
#14705=B_SPLINE_CURVE_WITH_KNOTS ( 'NONE', 3,
 ( #6887, #9541, #5379, #13319 ),
 .UNSPECIFIED., .F., .F.,
 ( 4, 4 ),
 ( 2.383248697869602982E-07, 0.007646667935218605036 ),
 .UNSPECIFIED. ) ;
#14711=CARTESIAN_POINT ( 'NONE',  ( -7.272992578804307939, 21.48000000000001108, -10.01041549318726886 ) ) ;
#14716=CARTESIAN_POINT ( 'NONE',  ( -4.130660464442061475, 2.022510465845311355E-14, -11.65984581473472836 ) ) ;
#14718=CARTESIAN_POINT ( 'NONE',  ( 13.14483242576204880, 7.170662809914418290, 16.82677684650038330 ) ) ;
#14720=ADVANCED_FACE ( 'NONE', ( #11416 ), #16788, .T. ) ;
#14721=CARTESIAN_POINT ( 'NONE',  ( 10.92172942406178926, -7.869999999999994778, 7.935100905948385908 ) ) ;
#14734=CARTESIAN_POINT ( 'NONE',  ( -3.636496289402152637, 12.33000000000000718, -11.19198476289190936 ) ) ;
#14737=CARTESIAN_POINT ( 'NONE',  ( -9.520470885617715595, 0.6299999999999916778, -6.917026985038136289 ) ) ;
#14741=CARTESIAN_POINT ( 'NONE',  ( -4.171729424061787483, -10.66999999999999815, -12.83926296998457417 ) ) ;
#14743=LINE ( 'NONE', #17487, #654 ) ;
#14745=ADVANCED_FACE ( 'NONE', ( #7444 ), #12823, .F. ) ;
#14751=CARTESIAN_POINT ( 'NONE',  ( -24.73863375370603634, 5.918584287042171432, 7.999999999999761080 ) ) ;
#14752=CARTESIAN_POINT ( 'NONE',  ( 10.00000000000135891, 7.983052681821872554, -15.32050807568352191 ) ) ;
#14763=CARTESIAN_POINT ( 'NONE',  ( -8.343458848123576743, 19.48000000000000043, -11.48378591275254301 ) ) ;
#14766=CARTESIAN_POINT ( 'NONE',  ( 10.92172942406178926, 13.13000000000000256, 7.935100905948385908 ) ) ;
#14767=EDGE_CURVE ( 'NONE', #8561, #1210, #16391, .T. ) ;
#14781=ORIENTED_EDGE ( 'NONE', *, *, #4716, .T. ) ;
#14783=( BOUNDED_CURVE ( )  B_SPLINE_CURVE ( 2, ( #11045, #9729, #15582, #11631, #5665, #1569, #6988, #3490, #4319, #16594, #15075, #12363, #15167 ),
 .UNSPECIFIED., .F., .F. ) 
 B_SPLINE_CURVE_WITH_KNOTS ( ( 3, 2, 2, 2, 2, 2, 3 ),
 ( 0.5138888888888888395, 0.5166666666666667185, 0.5222222222222222543, 0.5277777777777777901, 0.5333333333333333259, 0.5388888888888888618, 0.5416666666666666297 ),
 .UNSPECIFIED. ) 
 CURVE ( )  GEOMETRIC_REPRESENTATION_ITEM ( )  RATIONAL_B_SPLINE_CURVE ( ( 0.9755282581475768211, 0.9755282581475762660, 1.000000000000000000, 0.9510565162951535312, 1.000000000000000000, 0.9510565162951535312, 1.000000000000000000, 0.9510565162951535312, 1.000000000000000000, 0.9510565162951535312, 1.000000000000000000, 0.9755282581475768211, 0.9755282581475768211 ) ) 
 REPRESENTATION_ITEM ( '' )  );
#14784=ORIENTED_EDGE ( 'NONE', *, *, #9164, .T. ) ;
#14787=CARTESIAN_POINT ( 'NONE',  ( 1.653273178848926472E-15, 30.93000000000001393, 13.50000000000000000 ) ) ;
#14795=CARTESIAN_POINT ( 'NONE',  ( -11.76794919243112325, 15.92999999999999972, -2.602085213965210642E-15 ) ) ;
#14797=EDGE_CURVE ( 'NONE', #6661, #9217, #12016, .T. ) ;
#14800=VERTEX_POINT ( 'NONE', #17396 ) ;
#14801=CARTESIAN_POINT ( 'NONE',  ( 1.137810555388867773, -1.046521029022079216E-15, -11.94593600937347055 ) ) ;
#14804=CARTESIAN_POINT ( 'NONE',  ( 7.272992578804308828, -13.02000000000000313, 10.01041549318726709 ) ) ;
#14805=DIRECTION ( 'NONE',  ( 0.000000000000000000, 0.000000000000000000, -1.000000000000000000 ) ) ;
#14806=CARTESIAN_POINT ( 'NONE',  ( 10.92172942406179104, -10.27000000000000135, -7.935100905948385908 ) ) ;
#14816=VECTOR ( 'NONE', #17327, 1000.000000000000000 ) ;
#14820=CARTESIAN_POINT ( 'NONE',  ( -10.92172942406178926, 7.629999999999998117, -7.935100905948389460 ) ) ;
#14821=CARTESIAN_POINT ( 'NONE',  ( 7.272992578804311492, -0.1199999999999976641, -10.01041549318726709 ) ) ;
#14825=CARTESIAN_POINT ( 'NONE',  ( -13.49999999999999822, -10.22000000000000419, -4.386415899144240349 ) ) ;
#14834=DIRECTION ( 'NONE',  ( 0.000000000000000000, 0.000000000000000000, -1.000000000000000000 ) ) ;
#14836=CARTESIAN_POINT ( 'NONE',  ( -19.29752010712827826, 5.918584287042170544, -17.42428528562878398 ) ) ;
#14842=ORIENTED_EDGE ( 'NONE', *, *, #12057, .T. ) ;
#14845=VECTOR ( 'NONE', #15451, 1000.000000000000000 ) ;
#14846=CARTESIAN_POINT ( 'NONE',  ( 8.343458848123578520, 17.98000000000000398, 11.48378591275254124 ) ) ;
#14851=CARTESIAN_POINT ( 'NONE',  ( -4.171729424061791036, 12.53000000000001357, 12.83926296998457239 ) ) ;
#14857=DIRECTION ( 'NONE',  ( 0.000000000000000000, 0.000000000000000000, 1.000000000000000000 ) ) ;
#14859=CARTESIAN_POINT ( 'NONE',  ( -6.935444911370063359, 9.999999999999992895, -10.66458871277817622 ) ) ;
#14861=ADVANCED_FACE ( 'NONE', ( #3025 ), #220, .F. ) ;
#14865=CARTESIAN_POINT ( 'NONE',  ( -8.050004039213265017, 7.892626838387373667, -16.80522879631183031 ) ) ;
#14866=ORIENTED_EDGE ( 'NONE', *, *, #1031, .F. ) ;
#14875=EDGE_CURVE ( 'NONE', #3274, #1725, #11268, .T. ) ;
#14884=CARTESIAN_POINT ( 'NONE',  ( -9.520470885617715595, 21.63000000000000966, -6.917026985038136289 ) ) ;
#14888=VERTEX_POINT ( 'NONE', #1709 ) ;
#14890=CARTESIAN_POINT ( 'NONE',  ( -9.840429937218175382, -2.585303254002297467E-15, -8.208115554517609880 ) ) ;
#14893=CARTESIAN_POINT ( 'NONE',  ( -3.636496289402156190, -7.469999999999997087, 11.19198476289190758 ) ) ;
#14895=CARTESIAN_POINT ( 'NONE',  ( -10.92172942406179104, -17.76999999999999957, 7.935100905948385908 ) ) ;
#14898=EDGE_CURVE ( 'NONE', #17257, #12765, #3293, .T. ) ;
#14908=CARTESIAN_POINT ( 'NONE',  ( -21.14483242576217847, 7.170662809914417402, 2.970370385949070435 ) ) ;
#14909=CARTESIAN_POINT ( 'NONE',  ( 13.49999999999999822, 4.280000000000002025, 4.386415899144236796 ) ) ;
#14911=CARTESIAN_POINT ( 'NONE',  ( 9.520470885617715595, -0.8699999999999957767, 6.917026985038135400 ) ) ;
#14914=CARTESIAN_POINT ( 'NONE',  ( -13.50000000000000000, -13.06999999999999851, -3.469446951953614189E-15 ) ) ;
#14916=FACE_OUTER_BOUND ( 'NONE', #16533, .T. ) ;
#14934=CARTESIAN_POINT ( 'NONE',  ( -12.00000000000000178, 3.796025403784440311, -2.718289652585035561E-15 ) ) ;
#14936=CARTESIAN_POINT ( 'NONE',  ( -13.50000000000000000, 13.92999999999999794, -3.469446951953614189E-15 ) ) ;
#14942=CARTESIAN_POINT ( 'NONE',  ( -13.49999999999999822, 9.079999999999996518, 4.386415899144235908 ) ) ;
#14946=EDGE_CURVE ( 'NONE', #17169, #2565, #5852, .T. ) ;
#14951=LINE ( 'NONE', #9600, #13600 ) ;
#14952=FACE_OUTER_BOUND ( 'NONE', #5276, .T. ) ;
#14959=CARTESIAN_POINT ( 'NONE',  ( -9.111282024567884719, 8.062232123460391975, -15.52398764842096845 ) ) ;
#14960=VERTEX_POINT ( 'NONE', #11183 ) ;
#14965=CARTESIAN_POINT ( 'NONE',  ( 13.50000000000000355, 16.58000000000000185, -4.386415899144233244 ) ) ;
#14966=CARTESIAN_POINT ( 'NONE',  ( -8.704847339800608097, 8.055054264001460851, 15.78643792884161456 ) ) ;
#14970=EDGE_CURVE ( 'NONE', #11029, #14800, #4465, .T. ) ;
#14978=ORIENTED_EDGE ( 'NONE', *, *, #13148, .F. ) ;
#14984=CARTESIAN_POINT ( 'NONE',  ( -13.50000000000000000, -12.06999999999999673, -3.469446951953614189E-15 ) ) ;
#14987=EDGE_CURVE ( 'NONE', #2562, #1172, #8366, .T. ) ;
#14990=DIRECTION ( 'NONE',  ( -1.000000000000000000, 0.000000000000000000, -1.075706766891313654E-14 ) ) ;
#14992=DIRECTION ( 'NONE',  ( 0.000000000000000000, 0.000000000000000000, 1.000000000000000000 ) ) ;
#14998=CARTESIAN_POINT ( 'NONE',  ( -25.42428528562849266, 0.000000000000000000, -5.441113646577748320 ) ) ;
#14999=DIRECTION ( 'NONE',  ( -0.000000000000000000, 1.000000000000000000, -0.000000000000000000 ) ) ;
#15000=CARTESIAN_POINT ( 'NONE',  ( -11.76794919243112325, -7.919999999999998153, 3.823638476888994386 ) ) ;
#15002=CARTESIAN_POINT ( 'NONE',  ( 4.171729424061791924, -13.96999999999999709, -12.83926296998457239 ) ) ;
#15004=VECTOR ( 'NONE', #15299, 1000.000000000000000 ) ;
#15005=CARTESIAN_POINT ( 'NONE',  ( -1.328658795546723038E-07, 9.679996299052479714, 13.49999999999999822 ) ) ;
#15009=DIRECTION ( 'NONE',  ( 0.000000000000000000, 0.000000000000000000, -1.000000000000000000 ) ) ;
#15012=AXIS2_PLACEMENT_3D ( 'NONE', #17484, #13849, #5671 ) ;
#15028=CARTESIAN_POINT ( 'NONE',  ( -8.549982208541774191E-16, 15.68000000000000682, 14.19474002721660355 ) ) ;
#15029=VECTOR ( 'NONE', #5406, 1000.000000000000000 ) ;
#15036=DIRECTION ( 'NONE',  ( 0.000000000000000000, 0.000000000000000000, -1.000000000000000000 ) ) ;
#15043=CARTESIAN_POINT ( 'NONE',  ( 11.76794919243112680, 23.58000000000001961, -3.823638476888993942 ) ) ;
#15044=EDGE_CURVE ( 'NONE', #5339, #16171, #15304, .T. ) ;
#15047=ORIENTED_EDGE ( 'NONE', *, *, #2113, .F. ) ;
#15059=CARTESIAN_POINT ( 'NONE',  ( 15.32135601632709410, 7.956016702382084915, -10.18318151426818297 ) ) ;
#15070=CARTESIAN_POINT ( 'NONE',  ( -9.520470885617715595, -17.36999999999999744, -6.917026985038136289 ) ) ;
#15075=CARTESIAN_POINT ( 'NONE',  ( 3.708203932499368527, 4.696025403784437557, 11.41267819554184371 ) ) ;
#15079=EDGE_CURVE ( 'NONE', #13170, #17257, #16645, .T. ) ;
#15080=CARTESIAN_POINT ( 'NONE',  ( 7.312260103668256263E-16, 8.062177826491094379, -18.00000000000000000 ) ) ;
#15083=CARTESIAN_POINT ( 'NONE',  ( -11.76794919243112325, -5.220000000000004192, -3.823638476888998827 ) ) ;
#15085=CARTESIAN_POINT ( 'NONE',  ( -4.171729424061787483, 1.329999999999997851, -12.83926296998457417 ) ) ;
#15099=CARTESIAN_POINT ( 'NONE',  ( -18.00011380242310821, 8.062143945083761309, 0.1786886709309575549 ) ) ;
#15100=CARTESIAN_POINT ( 'NONE',  ( 11.76794919243112325, 26.28000000000000824, 3.823638476888996163 ) ) ;
#15101=EDGE_LOOP ( 'NONE', ( #9348, #3804, #3763, #10063 ) ) ;
#15103=FACE_OUTER_BOUND ( 'NONE', #110, .T. ) ;
#15105=CARTESIAN_POINT ( 'NONE',  ( 8.343458848123583849, 6.880000000000006999, -11.48378591275253768 ) ) ;
#15110=AXIS2_PLACEMENT_3D ( 'NONE', #2209, #1072, #15730 ) ;
#15111=CARTESIAN_POINT ( 'NONE',  ( 8.343458848123583849, 4.879999999999997229, -11.48378591275253768 ) ) ;
#15112=CARTESIAN_POINT ( 'NONE',  ( -7.416407864998737942, 7.246025403784442709, 10.20780970022447853 ) ) ;
#15118=EDGE_CURVE ( 'NONE', #4526, #16216, #4588, .T. ) ;
#15123=CARTESIAN_POINT ( 'NONE',  ( -6.544256458472538895, 9.999999999999996447, -10.94569060336277211 ) ) ;
#15128=CARTESIAN_POINT ( 'NONE',  ( -6.205905254110084535, 10.00000000000000000, 10.91717878730325353 ) ) ;
#15130=CARTESIAN_POINT ( 'NONE',  ( -3.636496289402156190, 22.52999999999999403, 11.19198476289190758 ) ) ;
#15133=ORIENTED_EDGE ( 'NONE', *, *, #15310, .T. ) ;
#15134=CARTESIAN_POINT ( 'NONE',  ( -7.409984580736203970E-16, -16.32000000000000028, 12.37355403259654985 ) ) ;
#15137=DIRECTION ( 'NONE',  ( 0.8660254037844348218, 0.000000000000000000, 0.5000000000000067724 ) ) ;
#15146=ORIENTED_EDGE ( 'NONE', *, *, #933, .F. ) ;
#15147=CARTESIAN_POINT ( 'NONE',  ( 15.78346433836034990, 8.055324230341707192, -8.708180880075682140 ) ) ;
#15151=VERTEX_POINT ( 'NONE', #7553 ) ;
#15157=CARTESIAN_POINT ( 'NONE',  ( -8.549982208541774191E-16, -17.32000000000000384, 14.19474002721660355 ) ) ;
#15161=CARTESIAN_POINT ( 'NONE',  ( -11.76794919243112325, -17.22000000000000597, -3.823638476888998827 ) ) ;
#15165=CARTESIAN_POINT ( 'NONE',  ( -7.409984580736203970E-16, -1.320000000000003615, 12.37355403259654985 ) ) ;
#15167=CARTESIAN_POINT ( 'NONE',  ( -8.891200544363830713E-16, 4.546025403784440755, 12.00000000000000000 ) ) ;
#15172=CARTESIAN_POINT ( 'NONE',  ( -15.58845726811976995, 7.773118517290098062, -11.00000000000018119 ) ) ;
#15173=CARTESIAN_POINT ( 'NONE',  ( 4.171729424061789260, 3.830000000000000071, 12.83926296998457239 ) ) ;
#15174=CARTESIAN_POINT ( 'NONE',  ( -13.49999999999999822, 32.78000000000001535, -4.386415899144240349 ) ) ;
#15175=CARTESIAN_POINT ( 'NONE',  ( -9.520470885617715595, -11.36999999999999744, -6.917026985038136289 ) ) ;
#15177=CARTESIAN_POINT ( 'NONE',  ( -13.49999999999999822, -16.22000000000000597, -4.386415899144240349 ) ) ;
#15187=CARTESIAN_POINT ( 'NONE',  ( -9.708203932499390731, 0.7639745962155688463, -7.053423027509696297 ) ) ;
#15188=CYLINDRICAL_SURFACE ( 'NONE', #11485, 1.999999999999998224 ) ;
#15192=CIRCLE ( 'NONE', #4775, 26.00000000000000355 ) ;
#15193=CARTESIAN_POINT ( 'NONE',  ( -7.272992578804307939, 21.48000000000001108, -10.01041549318726886 ) ) ;
#15194=ORIENTED_EDGE ( 'NONE', *, *, #5631, .T. ) ;
#15196=CARTESIAN_POINT ( 'NONE',  ( -12.00000000000000178, 3.646025403784438623, -3.899036354794879422 ) ) ;
#15198=CARTESIAN_POINT ( 'NONE',  ( 13.50000000000000000, 6.430000000000005045, 1.734723475976807094E-15 ) ) ;
#15201=CARTESIAN_POINT ( 'NONE',  ( -5.441113646577473872, 0.000000000000000000, -25.42428528562855305 ) ) ;
#15202=CARTESIAN_POINT ( 'NONE',  ( -10.92172942406179104, 0.2300000000000079758, 7.935100905948385908 ) ) ;
#15203=CARTESIAN_POINT ( 'NONE',  ( 25.42428528562852819, 0.000000000000000000, 5.441113646577569796 ) ) ;
#15210=EDGE_CURVE ( 'NONE', #1419, #15151, #7765, .T. ) ;
#15212=AXIS2_PLACEMENT_3D ( 'NONE', #4761, #5686, #8336 ) ;
#15214=CARTESIAN_POINT ( 'NONE',  ( 7.416407864998774357, 8.113974596215598467, 10.20780970022453182 ) ) ;
#15215=CARTESIAN_POINT ( 'NONE',  ( 0.6924984764758361777, 8.027888383433445796, 18.11551784069756721 ) ) ;
#15220=CARTESIAN_POINT ( 'NONE',  ( -9.033826763038382168, 9.999999999999998224, 8.302007722878922635 ) ) ;
#15221=CARTESIAN_POINT ( 'NONE',  ( -9.479632845647650186, 8.043285765338840321, -15.38489371673200878 ) ) ;
#15222=ORIENTED_EDGE ( 'NONE', *, *, #11296, .F. ) ;
#15224=ORIENTED_EDGE ( 'NONE', *, *, #8576, .T. ) ;
#15226=CARTESIAN_POINT ( 'NONE',  ( -3.636496289402152637, -14.66999999999999638, -11.19198476289190936 ) ) ;
#15239=ORIENTED_EDGE ( 'NONE', *, *, #4247, .T. ) ;
#15243=CARTESIAN_POINT ( 'NONE',  ( -15.78346433836042095, 8.055324230341707192, 8.708180880075572006 ) ) ;
#15246=CARTESIAN_POINT ( 'NONE',  ( -7.272992578804310604, 28.38000000000000966, 10.01041549318726709 ) ) ;
#15251=CARTESIAN_POINT ( 'NONE',  ( 0.000000000000000000, 9.000000000000000000, 0.000000000000000000 ) ) ;
#15252=CARTESIAN_POINT ( 'NONE',  ( 11.76794919243112680, -0.4200000000000027045, -3.823638476888993942 ) ) ;
#15260=CARTESIAN_POINT ( 'NONE',  ( -3.708203932499367195, 0.1960254037844345598, -11.41267819554184548 ) ) ;
#15261=CARTESIAN_POINT ( 'NONE',  ( 8.486513546626678561, 8.030919929218461206, -16.00650186718814894 ) ) ;
#15262=CARTESIAN_POINT ( 'NONE',  ( 2.621994543952811015E-15, 29.18000000000000327, -14.19474002721660355 ) ) ;
#15263=CARTESIAN_POINT ( 'NONE',  ( 3.636496289402154414, -4.169999999999999929, 11.19198476289190758 ) ) ;
#15266=UNCERTAINTY_MEASURE_WITH_UNIT (LENGTH_MEASURE( 1.000000000000000082E-05 ), #8539, 'distance_accuracy_value', 'NONE');
#15267=CARTESIAN_POINT ( 'NONE',  ( 10.92172942406178926, -17.86999999999999744, 7.935100905948385908 ) ) ;
#15268=CARTESIAN_POINT ( 'NONE',  ( 7.999999999999885425, 7.170708369609772426, 19.79695994079632726 ) ) ;
#15274=DIRECTION ( 'NONE',  ( -0.000000000000000000, 1.000000000000000000, -0.000000000000000000 ) ) ;
#15281=CARTESIAN_POINT ( 'NONE',  ( -3.636496289402156190, 25.52999999999999758, 11.19198476289190758 ) ) ;
#15282=ORIENTED_EDGE ( 'NONE', *, *, #640, .T. ) ;
#15286=ORIENTED_EDGE ( 'NONE', *, *, #8898, .T. ) ;
#15287=ADVANCED_FACE ( 'NONE', ( #3644 ), #12676, .F. ) ;
#15290=CARTESIAN_POINT ( 'NONE',  ( -4.171729424061787483, 2.329999999999998739, -12.83926296998457417 ) ) ;
#15299=DIRECTION ( 'NONE',  ( -0.000000000000000000, 1.000000000000000000, -0.000000000000000000 ) ) ;
#15304=LINE ( 'NONE', #16559, #8851 ) ;
#15308=EDGE_LOOP ( 'NONE', ( #6061, #16290, #14347, #16174 ) ) ;
#15309=VECTOR ( 'NONE', #17135, 1000.000000000000000 ) ;
#15310=EDGE_CURVE ( 'NONE', #13044, #4352, #34, .T. ) ;
#15311=CARTESIAN_POINT ( 'NONE',  ( 2.621994543952811015E-15, 28.18000000000000682, -14.19474002721660355 ) ) ;
#15321=ORIENTED_EDGE ( 'NONE', *, *, #1110, .F. ) ;
#15323=ORIENTED_EDGE ( 'NONE', *, *, #15617, .T. ) ;
#15329=CARTESIAN_POINT ( 'NONE',  ( 7.999999999999904965, 0.000000000000000000, 17.32050807568881368 ) ) ;
#15333=CARTESIAN_POINT ( 'NONE',  ( 11.76794919243112325, 29.28000000000001180, 3.823638476888996163 ) ) ;
#15337=CARTESIAN_POINT ( 'NONE',  ( -11.76794919243112325, -13.91999999999999815, 3.823638476888994386 ) ) ;
#15340=EDGE_CURVE ( 'NONE', #10383, #14262, #13335, .T. ) ;
#15341=CARTESIAN_POINT ( 'NONE',  ( 3.636496289402157078, 0.03000000000000224709, -11.19198476289190936 ) ) ;
#15346=DIRECTION ( 'NONE',  ( 0.000000000000000000, 1.000000000000000000, 0.000000000000000000 ) ) ;
#15347=CARTESIAN_POINT ( 'NONE',  ( 9.708203932499371192, 8.596025403784453900, -7.053423027509677645 ) ) ;
#15348=CARTESIAN_POINT ( 'NONE',  ( 9.869431986045617222, 8.002175404975853112, -15.32050807568866624 ) ) ;
#15349=CARTESIAN_POINT ( 'NONE',  ( -7.272992578804310604, -7.620000000000000995, 10.01041549318726709 ) ) ;
#15352=CARTESIAN_POINT ( 'NONE',  ( 13.50000000000000355, -17.42000000000000526, -4.386415899144233244 ) ) ;
#15355=CARTESIAN_POINT ( 'NONE',  ( 13.49999999999999822, 3.280000000000003801, 4.386415899144236796 ) ) ;
#15358=CIRCLE ( 'NONE', #16491, 1.999999999999998224 ) ;
#15360=DIRECTION ( 'NONE',  ( 0.000000000000000000, 0.000000000000000000, 1.000000000000000000 ) ) ;
#15363=CARTESIAN_POINT ( 'NONE',  ( -17.32050807568886697, 0.000000000000000000, 9.999999999999838352 ) ) ;
#15367=CARTESIAN_POINT ( 'NONE',  ( -11.76794919243112325, 21.93000000000000682, -2.602085213965210642E-15 ) ) ;
#15372=CARTESIAN_POINT ( 'NONE',  ( 10.92172942406178926, 3.129999999999993676, 7.935100905948385908 ) ) ;
#15373=CARTESIAN_POINT ( 'NONE',  ( -3.636496289402152637, 33.32999999999999829, -11.19198476289190936 ) ) ;
#15375=CARTESIAN_POINT ( 'NONE',  ( 13.49999999999999822, -1.720000000000005302, 4.386415899144237684 ) ) ;
#15379=CIRCLE ( 'NONE', #8371, 2.000000000000001776 ) ;
#15381=CARTESIAN_POINT ( 'NONE',  ( -10.99999999999979394, 0.000000000000000000, -15.58845726812003996 ) ) ;
#15387=CARTESIAN_POINT ( 'NONE',  ( 1.645451467107275745, 7.815250021811909420, 18.85000554241879200 ) ) ;
#15398=CARTESIAN_POINT ( 'NONE',  ( -13.49999999999999822, 34.78000000000001535, -4.386415899144240349 ) ) ;
#15401=DIRECTION ( 'NONE',  ( 0.000000000000000000, -1.000000000000000000, 0.000000000000000000 ) ) ;
#15404=CARTESIAN_POINT ( 'NONE',  ( 9.746503595109638596, -1.242015572811693166E-15, 9.216735997558972215 ) ) ;
#15420=CARTESIAN_POINT ( 'NONE',  ( 0.000000000000000000, 30.93000000000001393, -13.50000000000000000 ) ) ;
#15423=CARTESIAN_POINT ( 'NONE',  ( -9.520470885617715595, 27.63000000000001677, -6.917026985038136289 ) ) ;
#15428=CARTESIAN_POINT ( 'NONE',  ( 0.000000000000000000, 0.000000000000000000, 0.000000000000000000 ) ) ;
#15429=CARTESIAN_POINT ( 'NONE',  ( 3.636496289402154414, -1.170000000000004370, 11.19198476289190758 ) ) ;
#15432=CARTESIAN_POINT ( 'NONE',  ( -1.732050807569007977, 7.773118517290099838, 18.99999999999998224 ) ) ;
#15437=CARTESIAN_POINT ( 'NONE',  ( 8.258382090122001529, 7.982365321444606643, -16.32862261014056671 ) ) ;
#15438=CARTESIAN_POINT ( 'NONE',  ( 8.343458848123578520, 27.98000000000000753, 11.48378591275254124 ) ) ;
#15440=CARTESIAN_POINT ( 'NONE',  ( -7.999999999999670486, 5.918584287042171432, -24.73863375370606477 ) ) ;
#15444=CARTESIAN_POINT ( 'NONE',  ( 1.469576158976824144E-15, 9.000000000000000000, 12.00000000000000178 ) ) ;
#15450=CARTESIAN_POINT ( 'NONE',  ( 0.000000000000000000, 9.000000000000000000, 0.000000000000000000 ) ) ;
#15451=DIRECTION ( 'NONE',  ( -0.000000000000000000, 1.000000000000000000, -0.000000000000000000 ) ) ;
#15455=CARTESIAN_POINT ( 'NONE',  ( -7.272992578804307939, 18.48000000000000398, -10.01041549318726886 ) ) ;
#15456=EDGE_LOOP ( 'NONE', ( #15693, #881, #2566, #5164 ) ) ;
#15460=CARTESIAN_POINT ( 'NONE',  ( -4.171729424061791036, -0.4699999999999981970, 12.83926296998457239 ) ) ;
#15461=CARTESIAN_POINT ( 'NONE',  ( 11.76794919243112325, 32.28000000000000114, 3.823638476888996163 ) ) ;
#15466=LINE ( 'NONE', #8701, #2815 ) ;
#15472=CARTESIAN_POINT ( 'NONE',  ( -9.708203932499369415, 7.363974596215575374, 7.053423027509678533 ) ) ;
#15479=ORIENTED_EDGE ( 'NONE', *, *, #1972, .T. ) ;
#15482=VERTEX_POINT ( 'NONE', #3271 ) ;
#15483=CARTESIAN_POINT ( 'NONE',  ( 4.171729424061789260, 29.82999999999999474, 12.83926296998457239 ) ) ;
#15485=EDGE_CURVE ( 'NONE', #13302, #17169, #1851, .T. ) ;
#15490=CARTESIAN_POINT ( 'NONE',  ( 7.731081879493610032, -5.208608120530584900E-17, -9.234192800205820006 ) ) ;
#15491=CARTESIAN_POINT ( 'NONE',  ( -1.156690518843707549, 7.956351059191337782, 18.35912573876695930 ) ) ;
#15496=DIRECTION ( 'NONE',  ( 0.000000000000000000, 0.000000000000000000, -1.000000000000000000 ) ) ;
#15497=ORIENTED_EDGE ( 'NONE', *, *, #13672, .T. ) ;
#15501=LINE ( 'NONE', #3413, #8046 ) ;
#15507=CARTESIAN_POINT ( 'NONE',  ( 9.520470885617715595, 32.13000000000001677, 6.917026985038135400 ) ) ;
#15511=CARTESIAN_POINT ( 'NONE',  ( 18.18516759496687030, 8.007293617507080796, -0.8582236110267621454 ) ) ;
#15512=CARTESIAN_POINT ( 'NONE',  ( -7.272992578804310604, -1.620000000000001217, 10.01041549318726709 ) ) ;
#15515=CARTESIAN_POINT ( 'NONE',  ( -8.891200544363830713E-16, 5.680000000000002380, 13.49999999999999822 ) ) ;
#15518=CARTESIAN_POINT ( 'NONE',  ( -17.32050807568886697, 0.000000000000000000, 9.999999999999838352 ) ) ;
#15520=CARTESIAN_POINT ( 'NONE',  ( 8.772452899675805327, 8.058014385990555084, -15.73598335365642953 ) ) ;
#15521=CARTESIAN_POINT ( 'NONE',  ( -8.549982208541774191E-16, 24.67999999999999972, 14.19474002721660355 ) ) ;
#15522=ORIENTED_EDGE ( 'NONE', *, *, #6458, .F. ) ;
#15524=DIRECTION ( 'NONE',  ( -0.000000000000000000, 1.000000000000000000, -0.000000000000000000 ) ) ;
#15535=LINE ( 'NONE', #4520, #7151 ) ;
#15536=ADVANCED_BREP_SHAPE_REPRESENTATION ( '', ( #3260, #16654 ), #11308 ) ;
#15541=CARTESIAN_POINT ( 'NONE',  ( -9.520470885617715595, 15.63000000000000433, -6.917026985038136289 ) ) ;
#15542=EDGE_LOOP ( 'NONE', ( #10661, #1854, #1642, #12955 ) ) ;
#15545=CARTESIAN_POINT ( 'NONE',  ( 19.00000000000000711, 0.000000000000000000, -1.732050807568807027 ) ) ;
#15546=CARTESIAN_POINT ( 'NONE',  ( 4.171729424061791924, 1.030000000000003135, -12.83926296998457239 ) ) ;
#15547=CARTESIAN_POINT ( 'NONE',  ( 2.279995255611139653E-15, 30.18000000000001393, -12.37355403259654985 ) ) ;
#15564=VERTEX_POINT ( 'NONE', #10360 ) ;
#15568=CARTESIAN_POINT ( 'NONE',  ( -13.50000000000000000, 28.93000000000001037, -3.469446951953614189E-15 ) ) ;
#15570=VECTOR ( 'NONE', #665, 1000.000000000000000 ) ;
#15575=CARTESIAN_POINT ( 'NONE',  ( 12.78940066181286106, 2.734769208434739636E-15, 0.7471054272073315294 ) ) ;
#15576=CARTESIAN_POINT ( 'NONE',  ( -1.005545769327274827E-13, 2.180000000000013927, -13.50000000000000000 ) ) ;
#15579=CARTESIAN_POINT ( 'NONE',  ( 15.58845726811991916, 0.000000000000000000, -10.99999999999996092 ) ) ;
#15581=AXIS2_PLACEMENT_3D ( 'NONE', #16616, #534, #791 ) ;
#15582=CARTESIAN_POINT ( 'NONE',  ( 3.708203932499371192, 5.896025403784444840, -11.41267819554184548 ) ) ;
#15587=B_SPLINE_CURVE_WITH_KNOTS ( 'NONE', 3,
 ( #99, #2555, #4162, #14751 ),
 .UNSPECIFIED., .F., .F.,
 ( 4, 4 ),
 ( 0.008723199174958470511, 0.01636875612029860955 ),
 .UNSPECIFIED. ) ;
#15588=CARTESIAN_POINT ( 'NONE',  ( 4.988803385412796665, 9.999999999999996447, -12.54439479535357371 ) ) ;
#15592=DIRECTION ( 'NONE',  ( 0.000000000000000000, -1.000000000000000000, 0.000000000000000000 ) ) ;
#15594=CARTESIAN_POINT ( 'NONE',  ( 9.520470885617715595, 29.13000000000001677, 6.917026985038135400 ) ) ;
#15602=CARTESIAN_POINT ( 'NONE',  ( -2.138189944381240881, 5.603118577679734535, 13.49999999999999822 ) ) ;
#15605=CARTESIAN_POINT ( 'NONE',  ( 4.988803385412796665, 9.999999999999996447, -12.54439479535357371 ) ) ;
#15606=CARTESIAN_POINT ( 'NONE',  ( -13.49999999999999822, 3.080000000000010285, 4.386415899144235020 ) ) ;
#15608=CARTESIAN_POINT ( 'NONE',  ( -10.92172942406179104, 9.230000000000002203, 7.935100905948385908 ) ) ;
#15617=EDGE_CURVE ( 'NONE', #4199, #8605, #11659, .T. ) ;
#15620=FACE_OUTER_BOUND ( 'NONE', #11882, .T. ) ;
#15625=CARTESIAN_POINT ( 'NONE',  ( 7.272992578804308828, 10.98000000000000576, 10.01041549318726709 ) ) ;
#15626=ORIENTED_EDGE ( 'NONE', *, *, #6378, .T. ) ;
#15630=CARTESIAN_POINT ( 'NONE',  ( 13.49999999999999822, -2.719999999999995310, 4.386415899144237684 ) ) ;
#15631=CARTESIAN_POINT ( 'NONE',  ( 3.636496289402154414, 28.82999999999999474, 11.19198476289190758 ) ) ;
#15640=LINE ( 'NONE', #4545, #15004 ) ;
#15641=PLANE ( 'NONE',  #11473 ) ;
#15650=CARTESIAN_POINT ( 'NONE',  ( 7.272992578804311492, 5.879999999999995453, -10.01041549318726709 ) ) ;
#15651=VERTEX_POINT ( 'NONE', #16331 ) ;
#15652=VERTEX_POINT ( 'NONE', #2802 ) ;
#15653=CARTESIAN_POINT ( 'NONE',  ( 4.171729424061791924, 28.03000000000000114, -12.83926296998457239 ) ) ;
#15658=ADVANCED_FACE ( 'NONE', ( #8411 ), #1663, .F. ) ;
#15667=CARTESIAN_POINT ( 'NONE',  ( 1.137810555388867773, -1.046521029022079216E-15, -11.94593600937347055 ) ) ;
#15668=CARTESIAN_POINT ( 'NONE',  ( 0.000000000000000000, 30.93000000000001393, 0.000000000000000000 ) ) ;
#15670=CARTESIAN_POINT ( 'NONE',  ( -8.000000000000145661, 0.000000000000000000, 17.32050807568870709 ) ) ;
#15672=CARTESIAN_POINT ( 'NONE',  ( -8.343458848123576743, 16.48000000000000753, -11.48378591275254301 ) ) ;
#15677=CARTESIAN_POINT ( 'NONE',  ( -16.82677684650042593, 7.170662809914419178, 13.14483242576199018 ) ) ;
#15678=DIRECTION ( 'NONE',  ( 0.000000000000000000, 0.000000000000000000, -1.000000000000000000 ) ) ;
#15682=DIRECTION ( 'NONE',  ( 0.000000000000000000, 0.000000000000000000, -1.000000000000000000 ) ) ;
#15683=CARTESIAN_POINT ( 'NONE',  ( 18.85006967243204556, 7.815232008520040630, 1.645488492587892315 ) ) ;
#15689=AXIS2_PLACEMENT_3D ( 'NONE', #12674, #6057, #2125 ) ;
#15693=ORIENTED_EDGE ( 'NONE', *, *, #15485, .T. ) ;
#15695=LINE ( 'NONE', #14035, #4648 ) ;
#15698=DIRECTION ( 'NONE',  ( 1.000000000000000000, 0.000000000000000000, 6.313931023057710304E-15 ) ) ;
#15701=CARTESIAN_POINT ( 'NONE',  ( -13.50000000000000000, 5.930000000000005045, -3.469446951953614189E-15 ) ) ;
#15703=CARTESIAN_POINT ( 'NONE',  ( 2.138189944381238661, 2.756881422320272002, 13.49999999999999822 ) ) ;
#15716=CARTESIAN_POINT ( 'NONE',  ( -11.76794919243112325, 10.08000000000000718, 3.823638476888994386 ) ) ;
#15717=ORIENTED_EDGE ( 'NONE', *, *, #14092, .T. ) ;
#15722=ADVANCED_FACE ( 'NONE', ( #1576 ), #6994, .F. ) ;
#15724=CARTESIAN_POINT ( 'NONE',  ( -2.970370385949294256, 7.170662809914418290, -21.14483242576214295 ) ) ;
#15726=CARTESIAN_POINT ( 'NONE',  ( -11.88920123096388792, 9.999999999999994671, -1.626927807140451154 ) ) ;
#15730=DIRECTION ( 'NONE',  ( 0.000000000000000000, 0.000000000000000000, -1.000000000000000000 ) ) ;
#15735=CARTESIAN_POINT ( 'NONE',  ( 24.73863375370599016, 5.918584287042170544, -7.999999999999936051 ) ) ;
#15740=CARTESIAN_POINT ( 'NONE',  ( 3.636496289402154414, 4.830000000000000959, 11.19198476289190758 ) ) ;
#15741=ORIENTED_EDGE ( 'NONE', *, *, #14797, .T. ) ;
#15744=CARTESIAN_POINT ( 'NONE',  ( -10.92172942406179104, 20.22999999999999687, 7.935100905948385908 ) ) ;
#15751=CARTESIAN_POINT ( 'NONE',  ( 12.44496325052851127, -3.033844236144862824E-15, -2.130170732896519148 ) ) ;
#15752=FACE_OUTER_BOUND ( 'NONE', #2236, .T. ) ;
#15753=AXIS2_PLACEMENT_3D ( 'NONE', #9817, #6985, #14990 ) ;
#15760=ORIENTED_EDGE ( 'NONE', *, *, #6458, .T. ) ;
#15762=ORIENTED_EDGE ( 'NONE', *, *, #16745, .F. ) ;
#15763=CARTESIAN_POINT ( 'NONE',  ( 10.92172942406178926, 15.13000000000000433, 7.935100905948385908 ) ) ;
#15765=AXIS2_PLACEMENT_3D ( 'NONE', #8597, #619, #12561 ) ;
#15766=LINE ( 'NONE', #14787, #17344 ) ;
#15777=CARTESIAN_POINT ( 'NONE',  ( 2.279995255611139653E-15, 21.17999999999998906, -12.37355403259654985 ) ) ;
#15779=ADVANCED_FACE ( 'NONE', ( #8499 ), #16512, .F. ) ;
#15784=CARTESIAN_POINT ( 'NONE',  ( 8.343458848123583849, 22.88000000000001322, -11.48378591275253768 ) ) ;
#15786=DIRECTION ( 'NONE',  ( -0.000000000000000000, -1.000000000000000000, -0.000000000000000000 ) ) ;
#15787=DIRECTION ( 'NONE',  ( 0.000000000000000000, 0.000000000000000000, -1.000000000000000000 ) ) ;
#15792=CARTESIAN_POINT ( 'NONE',  ( 4.171729424061789260, -11.16999999999999993, 12.83926296998457239 ) ) ;
#15807=CARTESIAN_POINT ( 'NONE',  ( 2.279995255611139653E-15, 9.179999999999992610, -12.37355403259654985 ) ) ;
#15812=CARTESIAN_POINT ( 'NONE',  ( 10.92172942406179104, -2.269999999999994245, -7.935100905948385908 ) ) ;
#15816=( BOUNDED_CURVE ( )  B_SPLINE_CURVE ( 2, ( #13539, #1428, #16632, #15112, #9857, #12313, #5612, #13626, #12578, #7108, #207, #11169, #291 ),
 .UNSPECIFIED., .F., .F. ) 
 B_SPLINE_CURVE_WITH_KNOTS ( ( 3, 2, 2, 2, 2, 2, 3 ),
 ( 0.4861111111111111049, 0.4888888888888888729, 0.4944444444444444642, 0.5000000000000000000, 0.5055555555555555358, 0.5111111111111110716, 0.5138888888888888395 ),
 .UNSPECIFIED. ) 
 CURVE ( )  GEOMETRIC_REPRESENTATION_ITEM ( )  RATIONAL_B_SPLINE_CURVE ( ( 0.9755282581475768211, 0.9755282581475768211, 1.000000000000000000, 0.9510565162951535312, 1.000000000000000000, 0.9510565162951535312, 1.000000000000000000, 0.9510565162951535312, 1.000000000000000000, 0.9510565162951535312, 1.000000000000000000, 0.9755282581475772652, 0.9755282581475768211 ) ) 
 REPRESENTATION_ITEM ( '' )  );
#15825=EDGE_CURVE ( 'NONE', #9583, #12239, #7718, .T. ) ;
#15830=ORIENTED_EDGE ( 'NONE', *, *, #14946, .F. ) ;
#15833=CARTESIAN_POINT ( 'NONE',  ( -11.76794919243112325, 6.930000000000005933, -2.602085213965210642E-15 ) ) ;
#15834=ORIENTED_EDGE ( 'NONE', *, *, #277, .F. ) ;
#15837=CARTESIAN_POINT ( 'NONE',  ( -13.49999999999999822, 26.08000000000000895, 4.386415899144235908 ) ) ;
#15838=DIRECTION ( 'NONE',  ( -0.000000000000000000, -1.000000000000000000, -0.000000000000000000 ) ) ;
#15846=LINE ( 'NONE', #3753, #5448 ) ;
#15857=CARTESIAN_POINT ( 'NONE',  ( 10.92172942406179104, 12.73000000000001819, -7.935100905948385908 ) ) ;
#15869=CARTESIAN_POINT ( 'NONE',  ( -7.409984580736203970E-16, 19.68000000000001393, 12.37355403259654985 ) ) ;
#15874=CARTESIAN_POINT ( 'NONE',  ( 10.92172942406178926, 19.13000000000000966, 7.935100905948385908 ) ) ;
#15875=CARTESIAN_POINT ( 'NONE',  ( -10.92172942406178926, 8.629999999999999005, -7.935100905948389460 ) ) ;
#15888=CARTESIAN_POINT ( 'NONE',  ( 1.732050807568740858, 0.000000000000000000, 19.00000000000000355 ) ) ;
#15891=CARTESIAN_POINT ( 'NONE',  ( -11.76794919243112325, 9.780000000000002913, -3.823638476888998827 ) ) ;
#15895=CARTESIAN_POINT ( 'NONE',  ( 3.636496289402154414, 16.83000000000001251, 11.19198476289190758 ) ) ;
#15896=ORIENTED_EDGE ( 'NONE', *, *, #11479, .F. ) ;
#15899=CARTESIAN_POINT ( 'NONE',  ( -13.49999999999999822, -7.220000000000005969, -4.386415899144240349 ) ) ;
#15904=PLANE ( 'NONE',  #4108 ) ;
#15909=CARTESIAN_POINT ( 'NONE',  ( -12.00000000000000355, 4.213974596215569690, 3.899036354794875425 ) ) ;
#15915=VERTEX_POINT ( 'NONE', #4766 ) ;
#15918=CARTESIAN_POINT ( 'NONE',  ( 2.279995255611139653E-15, 3.180000000000006821, -12.37355403259654985 ) ) ;
#15919=ORIENTED_EDGE ( 'NONE', *, *, #17109, .F. ) ;
#15921=EDGE_LOOP ( 'NONE', ( #5079, #10476, #16196, #13236 ) ) ;
#15922=CARTESIAN_POINT ( 'NONE',  ( 13.49999999999999822, 24.28000000000001180, 4.386415899144237684 ) ) ;
#15927=B_SPLINE_CURVE_WITH_KNOTS ( 'NONE', 3,
 ( #4196, #10920, #13640, #15221, #1534, #14959, #8545, #11008, #6950, #12509, #8279, #14865, #1442, #394 ),
 .UNSPECIFIED., .F., .F.,
 ( 4, 2, 2, 2, 2, 2, 4 ),
 ( 0.001064030468739382692, 0.001458147099196469747, 0.001852263729653557019, 0.002246380360110644073, 0.002640496990567731128, 0.003428730251481901768, 0.004216963512396073276 ),
 .UNSPECIFIED. ) ;
#15929=EDGE_CURVE ( 'NONE', #1713, #368, #9988, .T. ) ;
#15930=CARTESIAN_POINT ( 'NONE',  ( -17.32050807568884210, 7.773118517290098950, 7.999999999999840128 ) ) ;
#15934=CARTESIAN_POINT ( 'NONE',  ( 10.99999999999990941, 0.000000000000000000, 15.58845726811995824 ) ) ;
#15937=EDGE_LOOP ( 'NONE', ( #14179, #8691, #1624, #16292 ) ) ;
#15938=ORIENTED_EDGE ( 'NONE', *, *, #11403, .F. ) ;
#15940=ORIENTED_EDGE ( 'NONE', *, *, #848, .T. ) ;
#15943=CARTESIAN_POINT ( 'NONE',  ( 8.351563113033638075, 8.007813505529846054, 16.17460542229567366 ) ) ;
#15956=B_SPLINE_CURVE_WITH_KNOTS ( 'NONE', 3,
 ( #10110, #10281, #12657, #2031 ),
 .UNSPECIFIED., .F., .F.,
 ( 4, 4 ),
 ( 0.008786844460939023313, 0.01643317035798798689 ),
 .UNSPECIFIED. ) ;
#15958=CARTESIAN_POINT ( 'NONE',  ( -8.343458848123582072, 18.38000000000000611, 11.48378591275254124 ) ) ;
#15959=ORIENTED_EDGE ( 'NONE', *, *, #7633, .F. ) ;
#15962=CARTESIAN_POINT ( 'NONE',  ( -9.520470885617715595, 27.63000000000001677, -6.917026985038136289 ) ) ;
#15965=CARTESIAN_POINT ( 'NONE',  ( -9.520470885617715595, -8.369999999999995666, -6.917026985038136289 ) ) ;
#15967=CARTESIAN_POINT ( 'NONE',  ( -8.549982208541774191E-16, -5.320000000000001172, 14.19474002721660355 ) ) ;
#15969=EDGE_CURVE ( 'NONE', #8605, #13571, #14578, .T. ) ;
#15979=CARTESIAN_POINT ( 'NONE',  ( 7.272992578804308828, 13.98000000000000220, 10.01041549318726709 ) ) ;
#15982=CARTESIAN_POINT ( 'NONE',  ( 11.76794919243112680, 2.579999999999996962, -3.823638476888993942 ) ) ;
#15985=CARTESIAN_POINT ( 'NONE',  ( -13.50000000000000000, -4.069999999999997620, -3.469446951953614189E-15 ) ) ;
#16001=VERTEX_POINT ( 'NONE', #7338 ) ;
#16003=LINE ( 'NONE', #12045, #6505 ) ;
#16004=CARTESIAN_POINT ( 'NONE',  ( -7.272992578804310604, 4.379999999999999005, 10.01041549318726709 ) ) ;
#16005=ORIENTED_EDGE ( 'NONE', *, *, #9277, .T. ) ;
#16006=ORIENTED_EDGE ( 'NONE', *, *, #4911, .T. ) ;
#16007=CARTESIAN_POINT ( 'NONE',  ( 4.171729424061789260, 26.83000000000001961, 12.83926296998457239 ) ) ;
#16010=CARTESIAN_POINT ( 'NONE',  ( 10.92172942406178926, 16.13000000000000611, 7.935100905948385908 ) ) ;
#16016=CARTESIAN_POINT ( 'NONE',  ( 18.71141623506677121, 7.854708462831346161, 1.539237008743780555 ) ) ;
#16018=DIRECTION ( 'NONE',  ( 0.000000000000000000, 0.000000000000000000, -1.000000000000000000 ) ) ;
#16023=ORIENTED_EDGE ( 'NONE', *, *, #9474, .T. ) ;
#16024=EDGE_CURVE ( 'NONE', #11876, #9086, #12784, .T. ) ;
#16025=ORIENTED_EDGE ( 'NONE', *, *, #17286, .T. ) ;
#16028=CARTESIAN_POINT ( 'NONE',  ( 2.279995255611139653E-15, -11.81999999999999851, -12.37355403259654985 ) ) ;
#16030=CARTESIAN_POINT ( 'NONE',  ( 10.18318151426813323, 7.956016702382084915, 15.32135601632713673 ) ) ;
#16031=VECTOR ( 'NONE', #10822, 1000.000000000000000 ) ;
#16039=CARTESIAN_POINT ( 'NONE',  ( 11.76794919243112680, 17.57999999999999829, -3.823638476888993942 ) ) ;
#16042=EDGE_CURVE ( 'NONE', #9933, #4018, #3431, .T. ) ;
#16044=ORIENTED_EDGE ( 'NONE', *, *, #16745, .T. ) ;
#16045=DIRECTION ( 'NONE',  ( -0.000000000000000000, 1.000000000000000000, -0.000000000000000000 ) ) ;
#16046=CARTESIAN_POINT ( 'NONE',  ( -5.441113646577659502, 0.000000000000000000, 25.42428528562849976 ) ) ;
#16049=CARTESIAN_POINT ( 'NONE',  ( -11.76794919243112325, -10.92000000000000526, 3.823638476888994386 ) ) ;
#16051=CARTESIAN_POINT ( 'NONE',  ( -8.343458848123576743, -9.520000000000006679, -11.48378591275254301 ) ) ;
#16053=CIRCLE ( 'NONE', #10163, 14.50000000000000000 ) ;
#16065=CARTESIAN_POINT ( 'NONE',  ( -9.520470885617715595, 9.629999999999999005, -6.917026985038136289 ) ) ;
#16067=DIRECTION ( 'NONE',  ( -0.000000000000000000, -1.000000000000000000, -0.000000000000000000 ) ) ;
#16068=CARTESIAN_POINT ( 'NONE',  ( -11.76794919243112325, 0.9300000000000141487, -2.602085213965210642E-15 ) ) ;
#16072=CARTESIAN_POINT ( 'NONE',  ( 13.50000000000000355, -5.419999999999997264, -4.386415899144233244 ) ) ;
#16078=FACE_OUTER_BOUND ( 'NONE', #395, .T. ) ;
#16089=ORIENTED_EDGE ( 'NONE', *, *, #16937, .F. ) ;
#16091=CARTESIAN_POINT ( 'NONE',  ( -10.92172942406178926, 25.63000000000001322, -7.935100905948389460 ) ) ;
#16094=CARTESIAN_POINT ( 'NONE',  ( -8.343458848123582072, 12.37999999999999368, 11.48378591275254124 ) ) ;
#16095=CARTESIAN_POINT ( 'NONE',  ( 0.000000000000000000, 9.000000000000000000, 0.000000000000000000 ) ) ;
#16101=CARTESIAN_POINT ( 'NONE',  ( 1.876532330890708260E-11, 6.313974596214807278, -12.00000000000000355 ) ) ;
#16103=DIRECTION ( 'NONE',  ( -0.000000000000000000, 1.000000000000000000, -0.000000000000000000 ) ) ;
#16108=ORIENTED_EDGE ( 'NONE', *, *, #13247, .F. ) ;
#16109=VERTEX_POINT ( 'NONE', #15005 ) ;
#16111=ORIENTED_EDGE ( 'NONE', *, *, #13461, .T. ) ;
#16121=AXIS2_PLACEMENT_3D ( 'NONE', #12377, #8243, #2898 ) ;
#16127=CARTESIAN_POINT ( 'NONE',  ( -6.381610013855579133, 2.177477983142718114E-15, -10.81467641374194422 ) ) ;
#16130=CARTESIAN_POINT ( 'NONE',  ( -9.520470885617717371, -10.76999999999999424, 6.917026985038133624 ) ) ;
#16132=CARTESIAN_POINT ( 'NONE',  ( -10.92172942406178926, -6.370000000000000995, -7.935100905948389460 ) ) ;
#16134=CIRCLE ( 'NONE', #13054, 26.00000000000000355 ) ;
#16136=SHAPE_DEFINITION_REPRESENTATION ( #3797, #8052 ) ;
#16147=CARTESIAN_POINT ( 'NONE',  ( -9.520470885617717371, 10.23000000000000220, 6.917026985038133624 ) ) ;
#16148=DIRECTION ( 'NONE',  ( 0.000000000000000000, 0.000000000000000000, 1.000000000000000000 ) ) ;
#16149=CARTESIAN_POINT ( 'NONE',  ( -2.138189944381240881, 8.603118577679731871, 13.49999999999999822 ) ) ;
#16150=CARTESIAN_POINT ( 'NONE',  ( 2.279995255611139653E-15, 3.180000000000006821, -12.37355403259654985 ) ) ;
#16154=CARTESIAN_POINT ( 'NONE',  ( 4.171729424061789260, -12.16999999999999993, 12.83926296998457239 ) ) ;
#16163=CARTESIAN_POINT ( 'NONE',  ( 0.000000000000000000, 0.000000000000000000, 0.000000000000000000 ) ) ;
#16164=CARTESIAN_POINT ( 'NONE',  ( -1.900613283894433403, 3.390856018535834515, -12.00000000000000355 ) ) ;
#16169=B_SPLINE_CURVE_WITH_KNOTS ( 'NONE', 3,
 ( #5669, #8409, #12547, #13761 ),
 .UNSPECIFIED., .F., .F.,
 ( 4, 4 ),
 ( 0.008786844460939023313, 0.01643317035798799036 ),
 .UNSPECIFIED. ) ;
#16170=CARTESIAN_POINT ( 'NONE',  ( -18.02388005911709712, 8.055054232036098938, 0.3546005442043826394 ) ) ;
#16171=VERTEX_POINT ( 'NONE', #13344 ) ;
#16172=CARTESIAN_POINT ( 'NONE',  ( 0.000000000000000000, 5.918584287042170544, 0.000000000000000000 ) ) ;
#16174=ORIENTED_EDGE ( 'NONE', *, *, #15340, .T. ) ;
#16178=CARTESIAN_POINT ( 'NONE',  ( 8.343458848123578520, 15.97999999999999332, 11.48378591275254124 ) ) ;
#16194=CARTESIAN_POINT ( 'NONE',  ( -9.520470885617717371, 25.23000000000000398, 6.917026985038133624 ) ) ;
#16196=ORIENTED_EDGE ( 'NONE', *, *, #14875, .F. ) ;
#16198=CARTESIAN_POINT ( 'NONE',  ( 11.76794919243112325, -12.56999999999999851, 1.734723475976807094E-15 ) ) ;
#16216=VERTEX_POINT ( 'NONE', #6731 ) ;
#16217=CARTESIAN_POINT ( 'NONE',  ( -12.24945618364706057, -1.497824325258500411E-15, -4.612754215402016023 ) ) ;
#16220=CARTESIAN_POINT ( 'NONE',  ( -7.272992578804307939, -8.520000000000001350, -10.01041549318726886 ) ) ;
#16222=CARTESIAN_POINT ( 'NONE',  ( 4.171729424061789260, -17.16999999999999815, 12.83926296998457239 ) ) ;
#16237=CARTESIAN_POINT ( 'NONE',  ( 2.222800136090958073E-15, 0.04602540378443767399, -12.00000000000000000 ) ) ;
#16240=CARTESIAN_POINT ( 'NONE',  ( -11.76794919243112325, 1.080000000000000959, 3.823638476888994386 ) ) ;
#16241=EDGE_CURVE ( 'NONE', #201, #13302, #16454, .T. ) ;
#16244=CARTESIAN_POINT ( 'NONE',  ( -1.328658795546723038E-07, 9.679996299052479714, 13.49999999999999822 ) ) ;
#16245=CARTESIAN_POINT ( 'NONE',  ( -10.92172942406178926, -10.36999999999999744, -7.935100905948389460 ) ) ;
#16256=DIRECTION ( 'NONE',  ( 0.000000000000000000, 0.000000000000000000, 1.000000000000000000 ) ) ;
#16263=ORIENTED_EDGE ( 'NONE', *, *, #10680, .F. ) ;
#16267=CARTESIAN_POINT ( 'NONE',  ( -8.343458848123582072, 11.38000000000001144, 11.48378591275254124 ) ) ;
#16269=EDGE_CURVE ( 'NONE', #4638, #9259, #10620, .T. ) ;
#16273=CARTESIAN_POINT ( 'NONE',  ( 13.49999999999999822, 16.28000000000001535, 4.386415899144237684 ) ) ;
#16281=CARTESIAN_POINT ( 'NONE',  ( -7.999999999999776179, 0.000000000000000000, -17.32050807568887762 ) ) ;
#16285=( BOUNDED_CURVE ( )  B_SPLINE_CURVE ( 2, ( #4292, #9704, #12336, #1718, #16388, #13646, #16568, #4474, #2857, #1630, #8638 ),
 .UNSPECIFIED., .F., .F. ) 
 B_SPLINE_CURVE_WITH_KNOTS ( ( 3, 2, 2, 2, 2, 3 ),
 ( 0.6250000000000000000, 0.6277777777777777679, 0.6333333333333333037, 0.6388888888888888395, 0.6444444444444444864, 0.6468607619886460602 ),
 .UNSPECIFIED. ) 
 CURVE ( )  GEOMETRIC_REPRESENTATION_ITEM ( )  RATIONAL_B_SPLINE_CURVE ( ( 0.9755282581475768211, 0.9755282581475768211, 1.000000000000000000, 0.9510565162951535312, 1.000000000000000000, 0.9510565162951535312, 1.000000000000000000, 0.9510565162951535312, 1.000000000000000000, 0.9787126602969342670, 0.9759426306556713282 ) ) 
 REPRESENTATION_ITEM ( '' )  );
#16288=CARTESIAN_POINT ( 'NONE',  ( -7.999999999999705125, 6.548268786306342903, -22.26879735319537090 ) ) ;
#16290=ORIENTED_EDGE ( 'NONE', *, *, #7934, .T. ) ;
#16292=ORIENTED_EDGE ( 'NONE', *, *, #12150, .F. ) ;
#16293=ADVANCED_FACE ( 'NONE', ( #14916 ), #3890, .F. ) ;
#16296=CARTESIAN_POINT ( 'NONE',  ( -11.00000000000012612, 7.773118517290097174, 15.58845726811980725 ) ) ;
#16310=LINE ( 'NONE', #4217, #9291 ) ;
#16313=CARTESIAN_POINT ( 'NONE',  ( 9.520470885617715595, -9.869999999999997442, 6.917026985038135400 ) ) ;
#16315=CARTESIAN_POINT ( 'NONE',  ( -4.171729424061787483, -15.66999999999999638, -12.83926296998457417 ) ) ;
#16320=CARTESIAN_POINT ( 'NONE',  ( -17.32050807568867512, 7.773118517290098062, -8.000000000000207834 ) ) ;
#16321=AXIS2_PLACEMENT_3D ( 'NONE', #6787, #58, #5461 ) ;
#16322=EDGE_CURVE ( 'NONE', #908, #1193, #5589, .T. ) ;
#16329=CARTESIAN_POINT ( 'NONE',  ( -0.6924984764758839173, 8.027888383433452901, -18.11551784069753879 ) ) ;
#16331=CARTESIAN_POINT ( 'NONE',  ( -19.00000000000001776, 0.000000000000000000, 1.732050807568674466 ) ) ;
#16333=CARTESIAN_POINT ( 'NONE',  ( -7.272992578804307939, 0.4799999999999978728, -10.01041549318726886 ) ) ;
#16335=CARTESIAN_POINT ( 'NONE',  ( 13.50000000000000355, -14.41999999999999638, -4.386415899144233244 ) ) ;
#16344=EDGE_CURVE ( 'NONE', #5443, #4638, #14743, .T. ) ;
#16347=CARTESIAN_POINT ( 'NONE',  ( -13.50000000000000000, 4.930000000000004157, -3.469446951953614189E-15 ) ) ;
#16354=ORIENTED_EDGE ( 'NONE', *, *, #10137, .F. ) ;
#16357=ORIENTED_EDGE ( 'NONE', *, *, #10800, .F. ) ;
#16361=CARTESIAN_POINT ( 'NONE',  ( 13.49999999999999822, 13.28000000000001002, 4.386415899144237684 ) ) ;
#16368=B_SPLINE_CURVE_WITH_KNOTS ( 'NONE', 3,
 ( #1731, #12530, #4574, #414, #5822, #7408, #11206, #16581, #12790, #9895, #15243, #588, #3141, #8566, #9981, #7317, #5998, #676 ),
 .UNSPECIFIED., .F., .F.,
 ( 4, 2, 2, 2, 2, 2, 2, 2, 4 ),
 ( 2.344180274388505961E-07, 0.0005273255548235156187, 0.001054416691619592403, 0.001581507828415669187, 0.002108598965211746189, 0.002635690102007825792, 0.003162781238803905395, 0.003689872375599984999, 0.004216963512396064602 ),
 .UNSPECIFIED. ) ;
#16370=CARTESIAN_POINT ( 'NONE',  ( 12.00000000000006217, 8.413974596215602730, 3.899036354794897186 ) ) ;
#16374=CARTESIAN_POINT ( 'NONE',  ( -9.062685027414643102, 10.00000000000000000, -8.691113669179740597 ) ) ;
#16378=CARTESIAN_POINT ( 'NONE',  ( 4.012506912825325678, 10.00000000000000178, 12.61441303195674735 ) ) ;
#16379=FACE_OUTER_BOUND ( 'NONE', #10363, .T. ) ;
#16380=CARTESIAN_POINT ( 'NONE',  ( 11.76794919243112325, 23.28000000000000114, 3.823638476888996163 ) ) ;
#16385=CARTESIAN_POINT ( 'NONE',  ( -11.76794919243112325, -13.91999999999999815, 3.823638476888994386 ) ) ;
#16388=CARTESIAN_POINT ( 'NONE',  ( 10.92172942406179104, 0.7300000000000084199, -7.935100905948385908 ) ) ;
#16391=( BOUNDED_CURVE ( )  B_SPLINE_CURVE ( 2, ( #2100, #2361, #6637, #13165, #7615, #12991, #2535, #3615, #17310, #17224, #874, #6550, #13077 ),
 .UNSPECIFIED., .F., .F. ) 
 B_SPLINE_CURVE_WITH_KNOTS ( ( 3, 2, 2, 2, 2, 2, 3 ),
 ( 0.5694444444444444198, 0.5722222222222221877, 0.5777777777777777235, 0.5833333333333333703, 0.5888888888888889062, 0.5944444444444444420, 0.5972222222222222099 ),
 .UNSPECIFIED. ) 
 CURVE ( )  GEOMETRIC_REPRESENTATION_ITEM ( )  RATIONAL_B_SPLINE_CURVE ( ( 0.9755282581475768211, 0.9755282581475768211, 1.000000000000000000, 0.9510565162951535312, 1.000000000000000000, 0.9510565162951535312, 1.000000000000000000, 0.9510565162951535312, 1.000000000000000000, 0.9510565162951535312, 1.000000000000000000, 0.9755282581475768211, 0.9755282581475768211 ) ) 
 REPRESENTATION_ITEM ( '' )  );
#16392=EDGE_CURVE ( 'NONE', #11282, #11898, #5015, .T. ) ;
#16398=ORIENTED_EDGE ( 'NONE', *, *, #3751, .F. ) ;
#16399=PLANE ( 'NONE',  #2117 ) ;
#16401=ORIENTED_EDGE ( 'NONE', *, *, #10680, .T. ) ;
#16404=CARTESIAN_POINT ( 'NONE',  ( -24.73863375370603634, 0.000000000000000000, 7.999999999999761080 ) ) ;
#16407=PLANE ( 'NONE',  #11430 ) ;
#16408=CARTESIAN_POINT ( 'NONE',  ( 13.50000000000000000, -19.56999999999999673, 1.734723475976807094E-15 ) ) ;
#16412=CARTESIAN_POINT ( 'NONE',  ( 8.050216715958701030, -18.96812692063824812, 8.940658242654158983 ) ) ;
#16425=CARTESIAN_POINT ( 'NONE',  ( -7.272992578804307939, -2.520000000000001794, -10.01041549318726886 ) ) ;
#16427=CARTESIAN_POINT ( 'NONE',  ( -4.171729424061791036, 2.530000000000004690, 12.83926296998457239 ) ) ;
#16428=AXIS2_PLACEMENT_3D ( 'NONE', #12501, #13803, #15036 ) ;
#16438=CARTESIAN_POINT ( 'NONE',  ( -5.441113646577662166, 5.918584287042170544, 25.42428528562851042 ) ) ;
#16439=CARTESIAN_POINT ( 'NONE',  ( -1.900613283894366567, 1.737093173895315257, 12.00000000000004974 ) ) ;
#16448=CARTESIAN_POINT ( 'NONE',  ( -4.171729424061791036, 8.530000000000010019, 12.83926296998457239 ) ) ;
#16453=CARTESIAN_POINT ( 'NONE',  ( -13.50000000000000000, 2.930000000000001936, -3.469446951953614189E-15 ) ) ;
#16454=CIRCLE ( 'NONE', #11948, 1.999999999999998224 ) ;
#16466=DIRECTION ( 'NONE',  ( 0.000000000000000000, 1.000000000000000000, 0.000000000000000000 ) ) ;
#16468=CARTESIAN_POINT ( 'NONE',  ( -17.32050807568867512, 0.000000000000000000, -8.000000000000207834 ) ) ;
#16472=ORIENTED_EDGE ( 'NONE', *, *, #1742, .F. ) ;
#16473=CARTESIAN_POINT ( 'NONE',  ( 11.76794919243112680, -15.41999999999999993, -3.823638476888993942 ) ) ;
#16477=CARTESIAN_POINT ( 'NONE',  ( -17.32050807568867512, 0.000000000000000000, -8.000000000000207834 ) ) ;
#16485=ORIENTED_EDGE ( 'NONE', *, *, #14233, .T. ) ;
#16489=CARTESIAN_POINT ( 'NONE',  ( 1.732050807568740858, 0.000000000000000000, 19.00000000000000355 ) ) ;
#16490=EDGE_CURVE ( 'NONE', #16817, #12936, #504, .T. ) ;
#16491=AXIS2_PLACEMENT_3D ( 'NONE', #13406, #8219, #13580 ) ;
#16495=CARTESIAN_POINT ( 'NONE',  ( -10.92172942406179104, -11.76999999999999602, 7.935100905948385908 ) ) ;
#16501=CARTESIAN_POINT ( 'NONE',  ( 9.520470885617715595, -18.86999999999999744, 6.917026985038135400 ) ) ;
#16503=CYLINDRICAL_SURFACE ( 'NONE', #528, 12.00000000000000178 ) ;
#16512=CYLINDRICAL_SURFACE ( 'NONE', #15012, 1.999999999999998224 ) ;
#16513=CARTESIAN_POINT ( 'NONE',  ( 2.621994543952811015E-15, 32.18000000000000682, -14.19474002721660355 ) ) ;
#16514=CARTESIAN_POINT ( 'NONE',  ( 3.636496289402157078, -5.969999999999996199, -11.19198476289190936 ) ) ;
#16516=CARTESIAN_POINT ( 'NONE',  ( 2.445080149700053643E-15, 1.180000000000002602, -13.50000000000000000 ) ) ;
#16527=LINE ( 'NONE', #1413, #2587 ) ;
#16528=PLANE ( 'NONE',  #12614 ) ;
#16532=CARTESIAN_POINT ( 'NONE',  ( 9.520470885617717371, 23.73000000000000043, -6.917026985038131848 ) ) ;
#16533=EDGE_LOOP ( 'NONE', ( #14479, #9698, #17464, #5606 ) ) ;
#16537=CARTESIAN_POINT ( 'NONE',  ( -13.49999999999999822, 10.77999999999999936, -4.386415899144240349 ) ) ;
#16538=VERTEX_POINT ( 'NONE', #3234 ) ;
#16543=CARTESIAN_POINT ( 'NONE',  ( 4.171729424061789260, 3.830000000000000071, 12.83926296998457239 ) ) ;
#16544=DIRECTION ( 'NONE',  ( -0.000000000000000000, 1.000000000000000000, -0.000000000000000000 ) ) ;
#16551=CARTESIAN_POINT ( 'NONE',  ( 1.900613283887800264, 9.237093173895598142, -12.00000000000222045 ) ) ;
#16552=CARTESIAN_POINT ( 'NONE',  ( -23.28534784291395709, 6.548267719634617734, -4.206197538246709833 ) ) ;
#16559=CARTESIAN_POINT ( 'NONE',  ( 15.58845726811991916, 0.000000000000000000, -10.99999999999996092 ) ) ;
#16565=CARTESIAN_POINT ( 'NONE',  ( -3.636496289402156190, -13.46999999999999531, 11.19198476289190758 ) ) ;
#16568=CARTESIAN_POINT ( 'NONE',  ( 13.50000000000000000, 0.4300000000000137046, 1.734723475976807094E-15 ) ) ;
#16577=EDGE_LOOP ( 'NONE', ( #583, #11115, #10636, #8016 ) ) ;
#16581=CARTESIAN_POINT ( 'NONE',  ( -15.43183772185609826, 8.055054230040788354, 9.319033143234966232 ) ) ;
#16584=CARTESIAN_POINT ( 'NONE',  ( -8.549982208541774191E-16, -14.32000000000000561, 14.19474002721660355 ) ) ;
#16589=DIRECTION ( 'NONE',  ( -0.000000000000000000, -1.000000000000000000, -0.000000000000000000 ) ) ;
#16590=CARTESIAN_POINT ( 'NONE',  ( 9.520470885617717371, -3.269999999999995133, -6.917026985038131848 ) ) ;
#16594=CARTESIAN_POINT ( 'NONE',  ( 7.416407864998737054, 4.846025403784445018, 10.20780970022447853 ) ) ;
#16599=CARTESIAN_POINT ( 'NONE',  ( -12.00000000000000178, 0.9460254037844377795, 3.899036354794875869 ) ) ;
#16601=CARTESIAN_POINT ( 'NONE',  ( 4.171729424061791924, 32.03000000000000114, -12.83926296998457239 ) ) ;
#16602=CARTESIAN_POINT ( 'NONE',  ( -11.76794919243112325, -10.92000000000000526, 3.823638476888994386 ) ) ;
#16605=CARTESIAN_POINT ( 'NONE',  ( 2.621994543952811015E-15, -13.82000000000000028, -14.19474002721660355 ) ) ;
#16613=DIRECTION ( 'NONE',  ( -0.000000000000000000, 1.000000000000000000, -0.000000000000000000 ) ) ;
#16616=CARTESIAN_POINT ( 'NONE',  ( 17.32050807568878170, 0.000000000000000000, -7.999999999999961808 ) ) ;
#16617=FACE_OUTER_BOUND ( 'NONE', #10213, .T. ) ;
#16622=CARTESIAN_POINT ( 'NONE',  ( -11.76794919243112325, 25.08000000000001251, 3.823638476888994386 ) ) ;
#16627=CARTESIAN_POINT ( 'NONE',  ( 13.49999999999999822, 9.280000000000002913, 4.386415899144237684 ) ) ;
#16631=CARTESIAN_POINT ( 'NONE',  ( 13.49999999999999822, 4.280000000000002025, 4.386415899144237684 ) ) ;
#16632=CARTESIAN_POINT ( 'NONE',  ( -3.708203932499370303, 7.396025403784446617, 11.41267819554184371 ) ) ;
#16645=LINE ( 'NONE', #393, #17284 ) ;
#16651=CARTESIAN_POINT ( 'NONE',  ( -9.656730951920790673, 8.027996330223285071, 15.34225977864766932 ) ) ;
#16654=AXIS2_PLACEMENT_3D ( 'NONE', #186, #4335, #13945 ) ;
#16655=CARTESIAN_POINT ( 'NONE',  ( -0.1772876194880645961, 8.062177826491099708, 17.99999999999998934 ) ) ;
#16661=ORIENTED_EDGE ( 'NONE', *, *, #12837, .F. ) ;
#16662=CARTESIAN_POINT ( 'NONE',  ( 4.171729424061789260, 8.830000000000005400, 12.83926296998457239 ) ) ;
#16664=CARTESIAN_POINT ( 'NONE',  ( -13.50000000000000000, 17.92999999999999972, -3.469446951953614189E-15 ) ) ;
#16668=CARTESIAN_POINT ( 'NONE',  ( 0.000000000000000000, 9.000000000000000000, 0.000000000000000000 ) ) ;
#16672=CARTESIAN_POINT ( 'NONE',  ( 7.272992578804311492, 29.88000000000000966, -10.01041549318726709 ) ) ;
#16677=CARTESIAN_POINT ( 'NONE',  ( -15.58845726811976995, 7.773118517290098062, -11.00000000000018119 ) ) ;
#16678=CARTESIAN_POINT ( 'NONE',  ( -7.409984580736203970E-16, -4.320000000000003837, 12.37355403259654985 ) ) ;
#16686=CARTESIAN_POINT ( 'NONE',  ( 8.012470509808036212, 7.834275465301278274, -17.06309263661789544 ) ) ;
#16687=DIRECTION ( 'NONE',  ( 0.000000000000000000, 0.000000000000000000, 1.000000000000000000 ) ) ;
#16688=CARTESIAN_POINT ( 'NONE',  ( 3.636496289402157078, -2.970000000000000639, -11.19198476289190936 ) ) ;
#16691=CARTESIAN_POINT ( 'NONE',  ( 12.00000000000000178, 5.413974596215561874, 3.899036354794877202 ) ) ;
#16694=EDGE_CURVE ( 'NONE', #5339, #14160, #13625, .T. ) ;
#16695=CARTESIAN_POINT ( 'NONE',  ( 10.92172942406179104, 3.730000000000011084, -7.935100905948385908 ) ) ;
#16705=CARTESIAN_POINT ( 'NONE',  ( -7.999999999999776179, 0.000000000000000000, -17.32050807568887762 ) ) ;
#16707=CARTESIAN_POINT ( 'NONE',  ( 9.520470885617715595, 26.13000000000001322, 6.917026985038135400 ) ) ;
#16708=ORIENTED_EDGE ( 'NONE', *, *, #6025, .T. ) ;
#16712=CARTESIAN_POINT ( 'NONE',  ( -13.49999999999999822, 8.079999999999996518, 4.386415899144235908 ) ) ;
#16715=CARTESIAN_POINT ( 'NONE',  ( 10.92172942406179104, -1.269999999999993356, -7.935100905948385908 ) ) ;
#16724=CARTESIAN_POINT ( 'NONE',  ( -12.00000000000000000, 7.063974596215567558, -2.718289652585034772E-15 ) ) ;
#16736=CARTESIAN_POINT ( 'NONE',  ( 8.343458848123583849, 30.88000000000000256, -11.48378591275253768 ) ) ;
#16745=EDGE_CURVE ( 'NONE', #4394, #13814, #6711, .T. ) ;
#16748=ORIENTED_EDGE ( 'NONE', *, *, #10188, .T. ) ;
#16753=DIRECTION ( 'NONE',  ( -0.000000000000000000, 1.000000000000000000, -0.000000000000000000 ) ) ;
#16758=CARTESIAN_POINT ( 'NONE',  ( -3.636496289402156190, 28.53000000000000114, 11.19198476289190758 ) ) ;
#16762=CARTESIAN_POINT ( 'NONE',  ( 3.636496289402154414, -16.16999999999999815, 11.19198476289190758 ) ) ;
#16764=DIRECTION ( 'NONE',  ( 0.000000000000000000, 0.000000000000000000, 1.000000000000000000 ) ) ;
#16765=CARTESIAN_POINT ( 'NONE',  ( 11.76794919243112325, -6.720000000000000639, 3.823638476888996163 ) ) ;
#16768=CARTESIAN_POINT ( 'NONE',  ( -10.92172942406179104, 5.230000000000012861, 7.935100905948385908 ) ) ;
#16774=CARTESIAN_POINT ( 'NONE',  ( -4.171729424061787483, 26.32999999999999119, -12.83926296998457417 ) ) ;
#16775=CARTESIAN_POINT ( 'NONE',  ( -11.76794919243112325, -2.069999999999995399, -2.602085213965210642E-15 ) ) ;
#16777=LINE ( 'NONE', #4686, #5376 ) ;
#16780=B_SPLINE_CURVE_WITH_KNOTS ( 'NONE', 3,
 ( #8518, #4345, #8254, #10807, #9494, #3092, #11070, #16170, #15099, #8164, #2998, #1329, #13528, #12480, #6835, #12211, #13697, #5510 ),
 .UNSPECIFIED., .F., .F.,
 ( 4, 2, 2, 2, 2, 2, 2, 2, 4 ),
 ( 2.344023999656933974E-07, 0.0005273255500080974807, 0.001054416697616229401, 0.001581507845224361213, 0.002108598992832493024, 0.002635690140440624836, 0.003162781288048756214, 0.003689872435656887592, 0.004216963583265018536 ),
 .UNSPECIFIED. ) ;
#16786=CARTESIAN_POINT ( 'NONE',  ( -17.42428528562871293, 5.918584287042171432, 19.29752010712834220 ) ) ;
#16787=EDGE_CURVE ( 'NONE', #3760, #4199, #6045, .T. ) ;
#16788=CYLINDRICAL_SURFACE ( 'NONE', #2879, 26.00000000000000355 ) ;
#16789=CARTESIAN_POINT ( 'NONE',  ( 0.000000000000000000, 9.999999999999998224, 0.000000000000000000 ) ) ;
#16793=CARTESIAN_POINT ( 'NONE',  ( -9.520470885617717371, 19.22999999999999687, 6.917026985038133624 ) ) ;
#16805=CARTESIAN_POINT ( 'NONE',  ( 2.138189944381262642, 8.103118577679731871, -13.49999999999999112 ) ) ;
#16809=CARTESIAN_POINT ( 'NONE',  ( -18.99999999999998224, 7.773118517290098062, -1.732050807569074147 ) ) ;
#16817=VERTEX_POINT ( 'NONE', #3416 ) ;
#16819=VECTOR ( 'NONE', #5883, 1000.000000000000000 ) ;
#16822=CARTESIAN_POINT ( 'NONE',  ( -8.549982208541774191E-16, 32.68000000000000682, 14.19474002721660355 ) ) ;
#16829=CARTESIAN_POINT ( 'NONE',  ( 12.70176803441796309, 1.934905186679871999E-15, -0.6935314968477440667 ) ) ;
#16837=CYLINDRICAL_SURFACE ( 'NONE', #9528, 13.50000000000000000 ) ;
#16838=ORIENTED_EDGE ( 'NONE', *, *, #6355, .T. ) ;
#16841=CARTESIAN_POINT ( 'NONE',  ( 4.171729424061791924, 17.03000000000001890, -12.83926296998457239 ) ) ;
#16845=CARTESIAN_POINT ( 'NONE',  ( 15.34225977864770485, 8.027996330223285071, 9.656730951920737382 ) ) ;
#16846=CARTESIAN_POINT ( 'NONE',  ( 2.902084407815607718E-14, 5.180000000000006821, -13.50000000000000000 ) ) ;
#16849=CARTESIAN_POINT ( 'NONE',  ( 7.272992578804311492, 26.88000000000001677, -10.01041549318726709 ) ) ;
#16852=CARTESIAN_POINT ( 'NONE',  ( -9.520470885617717371, -16.76999999999999957, 6.917026985038133624 ) ) ;
#16854=CARTESIAN_POINT ( 'NONE',  ( 18.46851087777847411, 7.924527533097220022, -1.297848593170553233 ) ) ;
#16855=CARTESIAN_POINT ( 'NONE',  ( -9.520470885617717371, -1.769999999999993801, 6.917026985038133624 ) ) ;
#16862=CARTESIAN_POINT ( 'NONE',  ( -4.171729424061787483, 2.329999999999998739, -12.83926296998457417 ) ) ;
#16868=LINE ( 'NONE', #614, #6865 ) ;
#16869=ADVANCED_FACE ( 'NONE', ( #6434 ), #2072, .F. ) ;
#16877=FACE_BOUND ( 'NONE', #4470, .T. ) ;
#16881=CARTESIAN_POINT ( 'NONE',  ( -11.76794919243112325, 12.92999999999999616, -2.602085213965210642E-15 ) ) ;
#16885=CARTESIAN_POINT ( 'NONE',  ( 0.000000000000000000, 0.000000000000000000, 0.000000000000000000 ) ) ;
#16886=CARTESIAN_POINT ( 'NONE',  ( -3.636496289402152637, 30.32999999999999474, -11.19198476289190936 ) ) ;
#16893=ADVANCED_FACE ( 'NONE', ( #5105 ), #10497, .F. ) ;
#16904=CARTESIAN_POINT ( 'NONE',  ( 22.26879735319529274, 6.548268786306342015, -7.999999999999943157 ) ) ;
#16910=CARTESIAN_POINT ( 'NONE',  ( -8.343458848123582072, 29.38000000000000611, 11.48378591275254124 ) ) ;
#16924=CARTESIAN_POINT ( 'NONE',  ( -1.732050807568877859, 7.773118517290099838, -18.99999999999999645 ) ) ;
#16925=ORIENTED_EDGE ( 'NONE', *, *, #5661, .F. ) ;
#16928=CARTESIAN_POINT ( 'NONE',  ( 10.00000000000002132, 0.000000000000000000, -17.32050807568876394 ) ) ;
#16931=DIRECTION ( 'NONE',  ( 0.000000000000000000, 0.000000000000000000, 1.000000000000000000 ) ) ;
#16932=AXIS2_PLACEMENT_3D ( 'NONE', #16668, #14008, #7496 ) ;
#16934=CARTESIAN_POINT ( 'NONE',  ( 2.279995255611139653E-15, 30.18000000000001393, -12.37355403259654985 ) ) ;
#16937=EDGE_CURVE ( 'NONE', #9259, #11282, #7342, .T. ) ;
#16942=CARTESIAN_POINT ( 'NONE',  ( 1.732050807568739970, 7.773118517290100726, 19.00000000000000355 ) ) ;
#16945=CARTESIAN_POINT ( 'NONE',  ( 7.416407864998737054, 7.846025403784439689, 10.20780970022447853 ) ) ;
#16947=CARTESIAN_POINT ( 'NONE',  ( -8.343458848123578520, 2.479999999999999982, -11.48378591275254124 ) ) ;
#16948=CARTESIAN_POINT ( 'NONE',  ( -13.49999999999999822, 24.08000000000001606, 4.386415899144235908 ) ) ;
#16949=VERTEX_POINT ( 'NONE', #1278 ) ;
#16951=CARTESIAN_POINT ( 'NONE',  ( -11.00000000000012612, 7.773118517290097174, 15.58845726811980725 ) ) ;
#16956=CARTESIAN_POINT ( 'NONE',  ( 2.138189944381242213, 4.103118577679734535, -13.49999999999999822 ) ) ;
#16968=CARTESIAN_POINT ( 'NONE',  ( 11.76794919243112325, 11.27999999999999936, 3.823638476888996163 ) ) ;
#16974=CARTESIAN_POINT ( 'NONE',  ( 13.50000000000000355, 0.5800000000000020695, -4.386415899144233244 ) ) ;
#16975=CARTESIAN_POINT ( 'NONE',  ( 9.520470885617715595, 29.13000000000001677, 6.917026985038135400 ) ) ;
#16983=FACE_OUTER_BOUND ( 'NONE', #9263, .T. ) ;
#16991=ORIENTED_EDGE ( 'NONE', *, *, #10327, .F. ) ;
#16993=ORIENTED_EDGE ( 'NONE', *, *, #13690, .F. ) ;
#16994=ORIENTED_EDGE ( 'NONE', *, *, #6120, .F. ) ;
#16995=CARTESIAN_POINT ( 'NONE',  ( -13.50000000000000000, 31.93000000000001393, -3.469446951953614189E-15 ) ) ;
#16997=AXIS2_PLACEMENT_3D ( 'NONE', #5693, #3002, #7100 ) ;
#17001=CARTESIAN_POINT ( 'NONE',  ( 8.343458848123583849, 1.879999999999997451, -11.48378591275253768 ) ) ;
#17010=EDGE_CURVE ( 'NONE', #7996, #4811, #16285, .T. ) ;
#17011=EDGE_LOOP ( 'NONE', ( #3621, #4445, #282, #13172 ) ) ;
#17014=ORIENTED_EDGE ( 'NONE', *, *, #6481, .F. ) ;
#17015=CARTESIAN_POINT ( 'NONE',  ( 16.97418022790852277, 7.854708479871425730, -8.022689779262671905 ) ) ;
#17019=CARTESIAN_POINT ( 'NONE',  ( 16.47957145870430296, 7.956016782093528583, 8.177092975168907429 ) ) ;
#17020=CARTESIAN_POINT ( 'NONE',  ( -10.92172942406179104, 6.230000000000012861, 7.935100905948385908 ) ) ;
#17024=CARTESIAN_POINT ( 'NONE',  ( 1.732050807568740858, 0.000000000000000000, 19.00000000000000355 ) ) ;
#17034=ORIENTED_EDGE ( 'NONE', *, *, #14149, .T. ) ;
#17035=CARTESIAN_POINT ( 'NONE',  ( -13.49999999999999822, 9.079999999999996518, 4.386415899144235020 ) ) ;
#17036=CARTESIAN_POINT ( 'NONE',  ( 5.441113646577305119, 5.918584287042172321, 25.42428528562857792 ) ) ;
#17038=FACE_OUTER_BOUND ( 'NONE', #15921, .T. ) ;
#17040=CARTESIAN_POINT ( 'NONE',  ( -8.549982208541774191E-16, -2.320000000000000728, 14.19474002721660355 ) ) ;
#17041=DIRECTION ( 'NONE',  ( -0.000000000000000000, 1.000000000000000000, -0.000000000000000000 ) ) ;
#17054=CARTESIAN_POINT ( 'NONE',  ( -11.76794919243112325, 15.78000000000001535, -3.823638476888998827 ) ) ;
#17055=ORIENTED_EDGE ( 'NONE', *, *, #11541, .F. ) ;
#17058=LINE ( 'NONE', #15545, #8767 ) ;
#17059=CARTESIAN_POINT ( 'NONE',  ( -8.343458848123582072, 2.380000000000003002, 11.48378591275254124 ) ) ;
#17062=CARTESIAN_POINT ( 'NONE',  ( -5.441113646577473872, 5.918584287042170544, -25.42428528562855305 ) ) ;
#17063=( BOUNDED_CURVE ( )  B_SPLINE_CURVE ( 2, ( #2979, #4505, #2890, #12367, #4592, #4325, #3157 ),
 .UNSPECIFIED., .F., .F. ) 
 B_SPLINE_CURVE_WITH_KNOTS ( ( 3, 2, 2, 3 ),
 ( 0.6084947812034886550, 0.6113249933232189903, 0.6169854099280641657, 0.6212982611378772280 ),
 .UNSPECIFIED. ) 
 CURVE ( )  GEOMETRIC_REPRESENTATION_ITEM ( )  RATIONAL_B_SPLINE_CURVE ( ( 0.9755282581476212300, 0.9755282251407595417, 1.000000000000000000, 0.9510565162951535312, 1.000000000000000000, 0.9627084051148780963, 0.9822441115907478704 ) ) 
 REPRESENTATION_ITEM ( '' )  );
#17065=CARTESIAN_POINT ( 'NONE',  ( 2.138192650046352394, 6.756881519606005249, 13.49999912087611165 ) ) ;
#17076=ORIENTED_EDGE ( 'NONE', *, *, #16042, .F. ) ;
#17079=CARTESIAN_POINT ( 'NONE',  ( -9.520470885617717371, 4.230000000000011084, 6.917026985038133624 ) ) ;
#17083=CARTESIAN_POINT ( 'NONE',  ( -4.171729424061787483, 31.32999999999999829, -12.83926296998457417 ) ) ;
#17090=DIRECTION ( 'NONE',  ( 0.000000000000000000, 0.000000000000000000, -1.000000000000000000 ) ) ;
#17092=DIRECTION ( 'NONE',  ( -0.000000000000000000, 1.000000000000000000, -0.000000000000000000 ) ) ;
#17099=VERTEX_POINT ( 'NONE', #11275 ) ;
#17100=CARTESIAN_POINT ( 'NONE',  ( 10.92172942406179104, 15.72999999999999332, -7.935100905948385908 ) ) ;
#17109=EDGE_CURVE ( 'NONE', #13215, #10472, #7563, .T. ) ;
#17110=DIRECTION ( 'NONE',  ( -0.000000000000000000, 1.000000000000000000, -0.000000000000000000 ) ) ;
#17118=CARTESIAN_POINT ( 'NONE',  ( 12.00000000000000355, 8.446025403784434005, -3.899036354794874093 ) ) ;
#17120=CARTESIAN_POINT ( 'NONE',  ( 4.171729424061791924, 23.02999999999999403, -12.83926296998457239 ) ) ;
#17123=LINE ( 'NONE', #14205, #977 ) ;
#17126=CARTESIAN_POINT ( 'NONE',  ( 13.49999999999999822, -10.72000000000000242, 4.386415899144237684 ) ) ;
#17135=DIRECTION ( 'NONE',  ( -0.000000000000000000, 1.000000000000000000, -0.000000000000000000 ) ) ;
#17140=VERTEX_POINT ( 'NONE', #16477 ) ;
#17141=CARTESIAN_POINT ( 'NONE',  ( 3.636496289402154414, 13.83000000000000895, 11.19198476289190758 ) ) ;
#17142=ORIENTED_EDGE ( 'NONE', *, *, #53, .T. ) ;
#17146=CARTESIAN_POINT ( 'NONE',  ( 4.171729424061789260, 2.829999999999999183, 12.83926296998457239 ) ) ;
#17152=ADVANCED_FACE ( 'NONE', ( #4382 ), #9790, .F. ) ;
#17164=ORIENTED_EDGE ( 'NONE', *, *, #422, .F. ) ;
#17168=CARTESIAN_POINT ( 'NONE',  ( 11.76794919243112680, 5.580000000000004512, -3.823638476888993942 ) ) ;
#17169=VERTEX_POINT ( 'NONE', #8465 ) ;
#17172=CARTESIAN_POINT ( 'NONE',  ( 4.171729424061789260, 23.83000000000001961, 12.83926296998457239 ) ) ;
#17188=VERTEX_POINT ( 'NONE', #13817 ) ;
#17190=ORIENTED_EDGE ( 'NONE', *, *, #15969, .F. ) ;
#17191=CARTESIAN_POINT ( 'NONE',  ( 4.171729424061791924, 13.03000000000001357, -12.83926296998457239 ) ) ;
#17195=ADVANCED_FACE ( 'NONE', ( #5809 ), #11192, .F. ) ;
#17197=DIRECTION ( 'NONE',  ( -0.000000000000000000, 1.000000000000000000, -0.000000000000000000 ) ) ;
#17201=CIRCLE ( 'NONE', #1950, 26.00000000000000355 ) ;
#17210=ORIENTED_EDGE ( 'NONE', *, *, #11185, .F. ) ;
#17211=CARTESIAN_POINT ( 'NONE',  ( 7.999999999999849010, 0.000000000000000000, 24.73863375370601148 ) ) ;
#17213=DIRECTION ( 'NONE',  ( 0.000000000000000000, 0.000000000000000000, 1.000000000000000000 ) ) ;
#17215=CARTESIAN_POINT ( 'NONE',  ( 10.92172942406179104, -7.269999999999998685, -7.935100905948385908 ) ) ;
#17224=CARTESIAN_POINT ( 'NONE',  ( 7.416407864998737054, 1.846025403784438579, 10.20780970022447853 ) ) ;
#17228=ORIENTED_EDGE ( 'NONE', *, *, #16241, .F. ) ;
#17230=CARTESIAN_POINT ( 'NONE',  ( 9.520470885617715595, 8.129999999999999005, 6.917026985038135400 ) ) ;
#17235=CARTESIAN_POINT ( 'NONE',  ( 8.343458848123578520, -6.020000000000000462, 11.48378591275254124 ) ) ;
#17241=CARTESIAN_POINT ( 'NONE',  ( -1.732050807569007977, 7.773118517290099838, 18.99999999999998224 ) ) ;
#17251=ORIENTED_EDGE ( 'NONE', *, *, #1152, .F. ) ;
#17254=CARTESIAN_POINT ( 'NONE',  ( -7.272992578804310604, 7.380000000000005222, 10.01041549318726709 ) ) ;
#17255=VERTEX_POINT ( 'NONE', #4732 ) ;
#17257=VERTEX_POINT ( 'NONE', #9768 ) ;
#17258=CARTESIAN_POINT ( 'NONE',  ( 10.92172942406178926, 21.13000000000000966, 7.935100905948385908 ) ) ;
#17265=CARTESIAN_POINT ( 'NONE',  ( 2.894739590358088936E-06, 0.6800804143413337055, 13.49999999999938360 ) ) ;
#17267=CARTESIAN_POINT ( 'NONE',  ( 1.204171936209234461, 9.999999999999996447, -13.21877505270804143 ) ) ;
#17277=EDGE_CURVE ( 'NONE', #8869, #13655, #3285, .T. ) ;
#17284=VECTOR ( 'NONE', #2847, 1000.000000000000000 ) ;
#17286=EDGE_CURVE ( 'NONE', #12239, #12048, #15466, .T. ) ;
#17293=CARTESIAN_POINT ( 'NONE',  ( 4.171729424061789260, 18.83000000000001251, 12.83926296998457239 ) ) ;
#17295=CARTESIAN_POINT ( 'NONE',  ( 0.000000000000000000, 9.000000000000000000, 0.000000000000000000 ) ) ;
#17296=CARTESIAN_POINT ( 'NONE',  ( -11.76794919243112325, 27.93000000000001037, -2.602085213965210642E-15 ) ) ;
#17299=CARTESIAN_POINT ( 'NONE',  ( -11.76794919243112325, -11.06999999999999673, -2.602085213965210642E-15 ) ) ;
#17301=CARTESIAN_POINT ( 'NONE',  ( -8.549982208541774191E-16, -8.320000000000009166, 14.19474002721660355 ) ) ;
#17310=CARTESIAN_POINT ( 'NONE',  ( 9.708203932499369415, 1.996025403784430496, 7.053423027509680310 ) ) ;
#17313=CARTESIAN_POINT ( 'NONE',  ( 11.76794919243112325, 11.42999999999999616, 1.734723475976807094E-15 ) ) ;
#17317=CARTESIAN_POINT ( 'NONE',  ( -7.272992578804310604, 7.380000000000005222, 10.01041549318726709 ) ) ;
#17321=CARTESIAN_POINT ( 'NONE',  ( 4.171729424061789260, 9.830000000000005400, 12.83926296998457239 ) ) ;
#17322=CARTESIAN_POINT ( 'NONE',  ( 13.50000000000000000, -8.569999999999994955, 1.734723475976807094E-15 ) ) ;
#17327=DIRECTION ( 'NONE',  ( 0.000000000000000000, -1.000000000000000000, 0.000000000000000000 ) ) ;
#17329=EDGE_CURVE ( 'NONE', #15915, #5802, #10712, .T. ) ;
#17332=CARTESIAN_POINT ( 'NONE',  ( 17.32050807568878170, 0.000000000000000000, -7.999999999999961808 ) ) ;
#17333=CARTESIAN_POINT ( 'NONE',  ( -3.708203932499366751, 3.463974596215561697, -11.41267819554184371 ) ) ;
#17342=CARTESIAN_POINT ( 'NONE',  ( -9.520470885617717371, 1.230000000000008864, 6.917026985038133624 ) ) ;
#17343=ORIENTED_EDGE ( 'NONE', *, *, #8049, .T. ) ;
#17344=VECTOR ( 'NONE', #17448, 1000.000000000000000 ) ;
#17345=ORIENTED_EDGE ( 'NONE', *, *, #160, .F. ) ;
#17346=CARTESIAN_POINT ( 'NONE',  ( -4.171729424061791036, 20.53000000000001890, 12.83926296998457239 ) ) ;
#17349=CARTESIAN_POINT ( 'NONE',  ( 8.343458848123578520, 9.979999999999996874, 11.48378591275254124 ) ) ;
#17359=CARTESIAN_POINT ( 'NONE',  ( 0.000000000000000000, 0.000000000000000000, 0.000000000000000000 ) ) ;
#17362=ORIENTED_EDGE ( 'NONE', *, *, #13247, .T. ) ;
#17363=ORIENTED_EDGE ( 'NONE', *, *, #14149, .F. ) ;
#17365=EDGE_LOOP ( 'NONE', ( #9670, #2517, #8889, #3390 ) ) ;
#17373=ADVANCED_FACE ( 'NONE', ( #4880 ), #7370, .F. ) ;
#17385=CYLINDRICAL_SURFACE ( 'NONE', #4569, 26.00000000000000355 ) ;
#17386=CARTESIAN_POINT ( 'NONE',  ( 3.636496289402157078, -8.969999999999998863, -11.19198476289190936 ) ) ;
#17388=CARTESIAN_POINT ( 'NONE',  ( 10.92172942406179104, -4.269999999999996021, -7.935100905948385908 ) ) ;
#17396=CARTESIAN_POINT ( 'NONE',  ( -19.29752010712827826, 0.000000000000000000, -17.42428528562878398 ) ) ;
#17399=CARTESIAN_POINT ( 'NONE',  ( 3.636496289402154414, 10.83000000000000540, 11.19198476289190758 ) ) ;
#17400=CARTESIAN_POINT ( 'NONE',  ( 2.138189944381283514, 5.103118577679734535, -13.49999999999998401 ) ) ;
#17401=CARTESIAN_POINT ( 'NONE',  ( 11.76794919243112325, 5.430000000000004157, 1.734723475976807094E-15 ) ) ;
#17405=CARTESIAN_POINT ( 'NONE',  ( -4.171729424061787483, -4.669999999999993712, -12.83926296998457417 ) ) ;
#17406=DIRECTION ( 'NONE',  ( 0.000000000000000000, 1.000000000000000000, 0.000000000000000000 ) ) ;
#17408=EDGE_CURVE ( 'NONE', #10383, #9328, #636, .T. ) ;
#17415=CARTESIAN_POINT ( 'NONE',  ( 2.222800136090958861E-15, 3.313974596215566670, -12.00000000000000355 ) ) ;
#17424=ORIENTED_EDGE ( 'NONE', *, *, #15044, .T. ) ;
#17426=CARTESIAN_POINT ( 'NONE',  ( -10.92172942406178926, 22.63000000000000966, -7.935100905948389460 ) ) ;
#17430=CARTESIAN_POINT ( 'NONE',  ( -10.92172942406179104, 12.23000000000000398, 7.935100905948385908 ) ) ;
#17448=DIRECTION ( 'NONE',  ( 0.000000000000000000, -1.000000000000000000, 0.000000000000000000 ) ) ;
#17451=VECTOR ( 'NONE', #3602, 1000.000000000000227 ) ;
#17458=AXIS2_PLACEMENT_3D ( 'NONE', #9362, #10593, #7857 ) ;
#17459=CARTESIAN_POINT ( 'NONE',  ( 3.636496289402154414, 19.83000000000001251, 11.19198476289190758 ) ) ;
#17463=CARTESIAN_POINT ( 'NONE',  ( -13.49999999999999822, 21.08000000000001251, 4.386415899144235908 ) ) ;
#17464=ORIENTED_EDGE ( 'NONE', *, *, #14402, .F. ) ;
#17469=CARTESIAN_POINT ( 'NONE',  ( -7.272992578804310604, -10.62000000000000099, 10.01041549318726709 ) ) ;
#17471=CARTESIAN_POINT ( 'NONE',  ( 4.171729424061791924, -6.969999999999997087, -12.83926296998457239 ) ) ;
#17473=AXIS2_PLACEMENT_3D ( 'NONE', #8922, #602, #14281 ) ;
#17483=CARTESIAN_POINT ( 'NONE',  ( -3.636496289402156190, 10.53000000000001180, 11.19198476289190758 ) ) ;
#17484=CARTESIAN_POINT ( 'NONE',  ( -9.999999999999776179, 0.000000000000000000, -17.32050807568890605 ) ) ;
#17485=CARTESIAN_POINT ( 'NONE',  ( 3.636496289402154414, 4.830000000000000959, 11.19198476289190758 ) ) ;
#17487=CARTESIAN_POINT ( 'NONE',  ( 10.99999999999990941, 0.000000000000000000, 15.58845726811995824 ) ) ;
#17520=COLOUR_RGB('Black',0.12,0.14,0.17);
#17521=FILL_AREA_STYLE_COLOUR('',#17520);
#17522=FILL_AREA_STYLE('',(#17521));
#17523=SURFACE_STYLE_FILL_AREA(#17522);
#17524=SURFACE_SIDE_STYLE('',(#17523));
#17525=SURFACE_STYLE_USAGE(.BOTH.,#17524);
#17526=PRESENTATION_STYLE_ASSIGNMENT((#17525));
ENDSEC;
END-ISO-10303-21;
